ISO-10303-21;
HEADER;
/* Generated by software containing ST-Developer
 * from STEP Tools, Inc. (www.steptools.com) 
 */

FILE_DESCRIPTION(
/* description */ (''),
/* implementation_level */ '2;1');

FILE_NAME(
/* name */ 'ISO 4762 - M3 x 6 - Servo Gear Screw.step',
/* time_stamp */ '2026-10-15T13:29:10-07:00',
/* author */ (''),
/* organization */ (''),
/* preprocessor_version */ 'ST-DEVELOPER v20.2',
/* originating_system */ 'Autodesk Translation Framework v15.15.0.0',
/* authorisation */ '');

FILE_SCHEMA (('AUTOMOTIVE_DESIGN { 1 0 10303 214 3 1 1 }'));
ENDSEC;

DATA;
#10=MECHANICAL_DESIGN_GEOMETRIC_PRESENTATION_REPRESENTATION('',(#937),#83219);
#197=(
BOUNDED_CURVE()
B_SPLINE_CURVE(2,(#49716,#49717,#49718),.UNSPECIFIED.,.F.,.F.)
B_SPLINE_CURVE_WITH_KNOTS((3,3),(0.022587909800489,0.0437523366271109),
 .UNSPECIFIED.)
CURVE()
GEOMETRIC_REPRESENTATION_ITEM()
RATIONAL_B_SPLINE_CURVE((1.0009393918053,1.00090979171719,1.))
REPRESENTATION_ITEM('')
);
#198=(
BOUNDED_CURVE()
B_SPLINE_CURVE(2,(#49730,#49731,#49732),.UNSPECIFIED.,.F.,.F.)
B_SPLINE_CURVE_WITH_KNOTS((3,3),(0.,0.021164426826556),.UNSPECIFIED.)
CURVE()
GEOMETRIC_REPRESENTATION_ITEM()
RATIONAL_B_SPLINE_CURVE((1.,1.0009097917188,1.00093939180696))
REPRESENTATION_ITEM('')
);
#199=(
BOUNDED_CURVE()
B_SPLINE_CURVE(2,(#50025,#50026,#50027),.UNSPECIFIED.,.F.,.F.)
B_SPLINE_CURVE_WITH_KNOTS((3,3),(0.0225879098005002,0.0437523366271109),
 .UNSPECIFIED.)
CURVE()
GEOMETRIC_REPRESENTATION_ITEM()
RATIONAL_B_SPLINE_CURVE((1.00093939180451,1.00090979171643,1.))
REPRESENTATION_ITEM('')
);
#200=(
BOUNDED_CURVE()
B_SPLINE_CURVE(2,(#50034,#50035,#50036),.UNSPECIFIED.,.F.,.F.)
B_SPLINE_CURVE_WITH_KNOTS((3,3),(0.,0.0211644268266061),.UNSPECIFIED.)
CURVE()
GEOMETRIC_REPRESENTATION_ITEM()
RATIONAL_B_SPLINE_CURVE((1.,1.00090979171738,1.0009393918055))
REPRESENTATION_ITEM('')
);
#201=(
BOUNDED_CURVE()
B_SPLINE_CURVE(2,(#50039,#50040,#50041),.UNSPECIFIED.,.F.,.F.)
B_SPLINE_CURVE_WITH_KNOTS((3,3),(0.0225879098006031,0.0437523366271109),
 .UNSPECIFIED.)
CURVE()
GEOMETRIC_REPRESENTATION_ITEM()
RATIONAL_B_SPLINE_CURVE((1.00093939180394,1.00090979171587,1.))
REPRESENTATION_ITEM('')
);
#202=(
BOUNDED_CURVE()
B_SPLINE_CURVE(2,(#50048,#50049,#50050),.UNSPECIFIED.,.F.,.F.)
B_SPLINE_CURVE_WITH_KNOTS((3,3),(0.,0.0211644268265667),.UNSPECIFIED.)
CURVE()
GEOMETRIC_REPRESENTATION_ITEM()
RATIONAL_B_SPLINE_CURVE((1.,1.00090979171289,1.00093939180086))
REPRESENTATION_ITEM('')
);
#203=(
BOUNDED_CURVE()
B_SPLINE_CURVE(2,(#50053,#50054,#50055),.UNSPECIFIED.,.F.,.F.)
B_SPLINE_CURVE_WITH_KNOTS((3,3),(0.0225879098005541,0.0437523366271109),
 .UNSPECIFIED.)
CURVE()
GEOMETRIC_REPRESENTATION_ITEM()
RATIONAL_B_SPLINE_CURVE((1.00093939180201,1.000909791714,1.))
REPRESENTATION_ITEM('')
);
#204=(
BOUNDED_CURVE()
B_SPLINE_CURVE(2,(#50062,#50063,#50064),.UNSPECIFIED.,.F.,.F.)
B_SPLINE_CURVE_WITH_KNOTS((3,3),(0.,0.0211644268265858),.UNSPECIFIED.)
CURVE()
GEOMETRIC_REPRESENTATION_ITEM()
RATIONAL_B_SPLINE_CURVE((1.,1.00090979171717,1.00093939180528))
REPRESENTATION_ITEM('')
);
#205=(
BOUNDED_CURVE()
B_SPLINE_CURVE(2,(#50067,#50068,#50069),.UNSPECIFIED.,.F.,.F.)
B_SPLINE_CURVE_WITH_KNOTS((3,3),(0.0225879098004799,0.0437523366271109),
 .UNSPECIFIED.)
CURVE()
GEOMETRIC_REPRESENTATION_ITEM()
RATIONAL_B_SPLINE_CURVE((1.00093939180147,1.00090979171348,1.))
REPRESENTATION_ITEM('')
);
#206=(
BOUNDED_CURVE()
B_SPLINE_CURVE(2,(#50076,#50077,#50078),.UNSPECIFIED.,.F.,.F.)
B_SPLINE_CURVE_WITH_KNOTS((3,3),(0.,0.0211644268266267),.UNSPECIFIED.)
CURVE()
GEOMETRIC_REPRESENTATION_ITEM()
RATIONAL_B_SPLINE_CURVE((1.,1.00090979171262,1.00093939180058))
REPRESENTATION_ITEM('')
);
#207=(
BOUNDED_CURVE()
B_SPLINE_CURVE(2,(#50081,#50082,#50083),.UNSPECIFIED.,.F.,.F.)
B_SPLINE_CURVE_WITH_KNOTS((3,3),(0.0225879098005392,0.0437523366271109),
 .UNSPECIFIED.)
CURVE()
GEOMETRIC_REPRESENTATION_ITEM()
RATIONAL_B_SPLINE_CURVE((1.00093939179924,1.00090979171132,1.))
REPRESENTATION_ITEM('')
);
#208=(
BOUNDED_CURVE()
B_SPLINE_CURVE(2,(#50090,#50091,#50092),.UNSPECIFIED.,.F.,.F.)
B_SPLINE_CURVE_WITH_KNOTS((3,3),(0.,0.0211644268265472),.UNSPECIFIED.)
CURVE()
GEOMETRIC_REPRESENTATION_ITEM()
RATIONAL_B_SPLINE_CURVE((1.,1.00090979171511,1.00093939180316))
REPRESENTATION_ITEM('')
);
#209=(
BOUNDED_CURVE()
B_SPLINE_CURVE(2,(#50095,#50096,#50097),.UNSPECIFIED.,.F.,.F.)
B_SPLINE_CURVE_WITH_KNOTS((3,3),(0.0225879098005708,0.0437523366271109),
 .UNSPECIFIED.)
CURVE()
GEOMETRIC_REPRESENTATION_ITEM()
RATIONAL_B_SPLINE_CURVE((1.00093939180557,1.00090979171745,1.))
REPRESENTATION_ITEM('')
);
#210=(
BOUNDED_CURVE()
B_SPLINE_CURVE(2,(#50104,#50105,#50106),.UNSPECIFIED.,.F.,.F.)
B_SPLINE_CURVE_WITH_KNOTS((3,3),(0.,0.0211644268265667),.UNSPECIFIED.)
CURVE()
GEOMETRIC_REPRESENTATION_ITEM()
RATIONAL_B_SPLINE_CURVE((1.,1.00090979171694,1.00093939180505))
REPRESENTATION_ITEM('')
);
#211=(
BOUNDED_CURVE()
B_SPLINE_CURVE(2,(#50109,#50110,#50111),.UNSPECIFIED.,.F.,.F.)
B_SPLINE_CURVE_WITH_KNOTS((3,3),(0.0225879098005834,0.0437523366271109),
 .UNSPECIFIED.)
CURVE()
GEOMETRIC_REPRESENTATION_ITEM()
RATIONAL_B_SPLINE_CURVE((1.00093939180667,1.00090979171851,1.))
REPRESENTATION_ITEM('')
);
#212=(
BOUNDED_CURVE()
B_SPLINE_CURVE(2,(#50118,#50119,#50120),.UNSPECIFIED.,.F.,.F.)
B_SPLINE_CURVE_WITH_KNOTS((3,3),(0.,0.021164426826593),.UNSPECIFIED.)
CURVE()
GEOMETRIC_REPRESENTATION_ITEM()
RATIONAL_B_SPLINE_CURVE((1.,1.00090979171443,1.00093939180245))
REPRESENTATION_ITEM('')
);
#213=(
BOUNDED_CURVE()
B_SPLINE_CURVE(2,(#50123,#50124,#50125),.UNSPECIFIED.,.F.,.F.)
B_SPLINE_CURVE_WITH_KNOTS((3,3),(0.0225879098005489,0.0437523366271109),
 .UNSPECIFIED.)
CURVE()
GEOMETRIC_REPRESENTATION_ITEM()
RATIONAL_B_SPLINE_CURVE((1.00093939180192,1.00090979171391,1.))
REPRESENTATION_ITEM('')
);
#214=(
BOUNDED_CURVE()
B_SPLINE_CURVE(2,(#50132,#50133,#50134),.UNSPECIFIED.,.F.,.F.)
B_SPLINE_CURVE_WITH_KNOTS((3,3),(0.,0.0211644268265642),.UNSPECIFIED.)
CURVE()
GEOMETRIC_REPRESENTATION_ITEM()
RATIONAL_B_SPLINE_CURVE((1.,1.00090979171418,1.00093939180219))
REPRESENTATION_ITEM('')
);
#215=(
BOUNDED_CURVE()
B_SPLINE_CURVE(2,(#50137,#50138,#50139),.UNSPECIFIED.,.F.,.F.)
B_SPLINE_CURVE_WITH_KNOTS((3,3),(0.022587909800521,0.0437523366271108),
 .UNSPECIFIED.)
CURVE()
GEOMETRIC_REPRESENTATION_ITEM()
RATIONAL_B_SPLINE_CURVE((1.000939391805,1.00090979171689,1.))
REPRESENTATION_ITEM('')
);
#216=(
BOUNDED_CURVE()
B_SPLINE_CURVE(2,(#50146,#50147,#50148),.UNSPECIFIED.,.F.,.F.)
B_SPLINE_CURVE_WITH_KNOTS((3,3),(0.,0.0211644268266283),.UNSPECIFIED.)
CURVE()
GEOMETRIC_REPRESENTATION_ITEM()
RATIONAL_B_SPLINE_CURVE((1.,1.0009097917149,1.00093939180294))
REPRESENTATION_ITEM('')
);
#217=(
BOUNDED_CURVE()
B_SPLINE_CURVE(2,(#50151,#50152,#50153),.UNSPECIFIED.,.F.,.F.)
B_SPLINE_CURVE_WITH_KNOTS((3,3),(0.0225879098005678,0.0437523366271109),
 .UNSPECIFIED.)
CURVE()
GEOMETRIC_REPRESENTATION_ITEM()
RATIONAL_B_SPLINE_CURVE((1.0009393918065,1.00090979171835,1.))
REPRESENTATION_ITEM('')
);
#218=(
BOUNDED_CURVE()
B_SPLINE_CURVE(2,(#50160,#50161,#50162),.UNSPECIFIED.,.F.,.F.)
B_SPLINE_CURVE_WITH_KNOTS((3,3),(0.,0.0211644268266094),.UNSPECIFIED.)
CURVE()
GEOMETRIC_REPRESENTATION_ITEM()
RATIONAL_B_SPLINE_CURVE((1.,1.00090979171261,1.00093939180057))
REPRESENTATION_ITEM('')
);
#219=(
BOUNDED_CURVE()
B_SPLINE_CURVE(2,(#50165,#50166,#50167),.UNSPECIFIED.,.F.,.F.)
B_SPLINE_CURVE_WITH_KNOTS((3,3),(0.022587909800501,0.0437523366271109),
 .UNSPECIFIED.)
CURVE()
GEOMETRIC_REPRESENTATION_ITEM()
RATIONAL_B_SPLINE_CURVE((1.00093939180006,1.00090979171211,1.))
REPRESENTATION_ITEM('')
);
#220=(
BOUNDED_CURVE()
B_SPLINE_CURVE(2,(#50174,#50175,#50176),.UNSPECIFIED.,.F.,.F.)
B_SPLINE_CURVE_WITH_KNOTS((3,3),(0.,0.0211644268266066),.UNSPECIFIED.)
CURVE()
GEOMETRIC_REPRESENTATION_ITEM()
RATIONAL_B_SPLINE_CURVE((1.,1.00090979171135,1.00093939179927))
REPRESENTATION_ITEM('')
);
#221=(
BOUNDED_CURVE()
B_SPLINE_CURVE(2,(#50179,#50180,#50181),.UNSPECIFIED.,.F.,.F.)
B_SPLINE_CURVE_WITH_KNOTS((3,3),(0.0225879098005609,0.0437523366271108),
 .UNSPECIFIED.)
CURVE()
GEOMETRIC_REPRESENTATION_ITEM()
RATIONAL_B_SPLINE_CURVE((1.00093939180654,1.00090979171839,1.))
REPRESENTATION_ITEM('')
);
#222=(
BOUNDED_CURVE()
B_SPLINE_CURVE(2,(#50188,#50189,#50190),.UNSPECIFIED.,.F.,.F.)
B_SPLINE_CURVE_WITH_KNOTS((3,3),(0.,0.0211644268266203),.UNSPECIFIED.)
CURVE()
GEOMETRIC_REPRESENTATION_ITEM()
RATIONAL_B_SPLINE_CURVE((1.,1.00090979171634,1.00093939180443))
REPRESENTATION_ITEM('')
);
#223=(
BOUNDED_CURVE()
B_SPLINE_CURVE(2,(#50193,#50194,#50195),.UNSPECIFIED.,.F.,.F.)
B_SPLINE_CURVE_WITH_KNOTS((3,3),(0.0225879098005457,0.0437523366271109),
 .UNSPECIFIED.)
CURVE()
GEOMETRIC_REPRESENTATION_ITEM()
RATIONAL_B_SPLINE_CURVE((1.00093939180273,1.0009097917147,1.))
REPRESENTATION_ITEM('')
);
#224=(
BOUNDED_CURVE()
B_SPLINE_CURVE(2,(#50202,#50203,#50204),.UNSPECIFIED.,.F.,.F.)
B_SPLINE_CURVE_WITH_KNOTS((3,3),(0.,0.0211644268265952),.UNSPECIFIED.)
CURVE()
GEOMETRIC_REPRESENTATION_ITEM()
RATIONAL_B_SPLINE_CURVE((1.,1.00090979171439,1.00093939180241))
REPRESENTATION_ITEM('')
);
#225=(
BOUNDED_CURVE()
B_SPLINE_CURVE(2,(#50207,#50208,#50209),.UNSPECIFIED.,.F.,.F.)
B_SPLINE_CURVE_WITH_KNOTS((3,3),(0.0225879098005205,0.0437523366271109),
 .UNSPECIFIED.)
CURVE()
GEOMETRIC_REPRESENTATION_ITEM()
RATIONAL_B_SPLINE_CURVE((1.00093939180427,1.00090979171619,1.))
REPRESENTATION_ITEM('')
);
#226=(
BOUNDED_CURVE()
B_SPLINE_CURVE(2,(#50216,#50217,#50218),.UNSPECIFIED.,.F.,.F.)
B_SPLINE_CURVE_WITH_KNOTS((3,3),(0.,0.0211644268265894),.UNSPECIFIED.)
CURVE()
GEOMETRIC_REPRESENTATION_ITEM()
RATIONAL_B_SPLINE_CURVE((1.,1.00090979171495,1.00093939180299))
REPRESENTATION_ITEM('')
);
#227=(
BOUNDED_CURVE()
B_SPLINE_CURVE(2,(#50221,#50222,#50223),.UNSPECIFIED.,.F.,.F.)
B_SPLINE_CURVE_WITH_KNOTS((3,3),(0.0225879098005011,0.0437523366271109),
 .UNSPECIFIED.)
CURVE()
GEOMETRIC_REPRESENTATION_ITEM()
RATIONAL_B_SPLINE_CURVE((1.00093939180012,1.00090979171217,1.))
REPRESENTATION_ITEM('')
);
#228=(
BOUNDED_CURVE()
B_SPLINE_CURVE(2,(#50230,#50231,#50232),.UNSPECIFIED.,.F.,.F.)
B_SPLINE_CURVE_WITH_KNOTS((3,3),(0.,0.0211644268265743),.UNSPECIFIED.)
CURVE()
GEOMETRIC_REPRESENTATION_ITEM()
RATIONAL_B_SPLINE_CURVE((1.,1.00090979171694,1.00093939180504))
REPRESENTATION_ITEM('')
);
#229=(
BOUNDED_CURVE()
B_SPLINE_CURVE(2,(#50235,#50236,#50237),.UNSPECIFIED.,.F.,.F.)
B_SPLINE_CURVE_WITH_KNOTS((3,3),(0.0225879098005504,0.0437523366271109),
 .UNSPECIFIED.)
CURVE()
GEOMETRIC_REPRESENTATION_ITEM()
RATIONAL_B_SPLINE_CURVE((1.00093939180379,1.00090979171572,1.))
REPRESENTATION_ITEM('')
);
#230=(
BOUNDED_CURVE()
B_SPLINE_CURVE(2,(#50244,#50245,#50246),.UNSPECIFIED.,.F.,.F.)
B_SPLINE_CURVE_WITH_KNOTS((3,3),(0.,0.0211644268265842),.UNSPECIFIED.)
CURVE()
GEOMETRIC_REPRESENTATION_ITEM()
RATIONAL_B_SPLINE_CURVE((1.,1.00090979171899,1.00093939180716))
REPRESENTATION_ITEM('')
);
#231=(
BOUNDED_CURVE()
B_SPLINE_CURVE(2,(#50249,#50250,#50251),.UNSPECIFIED.,.F.,.F.)
B_SPLINE_CURVE_WITH_KNOTS((3,3),(0.0225879098005829,0.0437523366271109),
 .UNSPECIFIED.)
CURVE()
GEOMETRIC_REPRESENTATION_ITEM()
RATIONAL_B_SPLINE_CURVE((1.00093939180477,1.00090979171667,1.))
REPRESENTATION_ITEM('')
);
#232=(
BOUNDED_CURVE()
B_SPLINE_CURVE(2,(#50258,#50259,#50260),.UNSPECIFIED.,.F.,.F.)
B_SPLINE_CURVE_WITH_KNOTS((3,3),(0.,0.0211644268266254),.UNSPECIFIED.)
CURVE()
GEOMETRIC_REPRESENTATION_ITEM()
RATIONAL_B_SPLINE_CURVE((1.,1.00090979171259,1.00093939180055))
REPRESENTATION_ITEM('')
);
#233=(
BOUNDED_CURVE()
B_SPLINE_CURVE(2,(#50263,#50264,#50265),.UNSPECIFIED.,.F.,.F.)
B_SPLINE_CURVE_WITH_KNOTS((3,3),(0.0225879098005341,0.0437523366271108),
 .UNSPECIFIED.)
CURVE()
GEOMETRIC_REPRESENTATION_ITEM()
RATIONAL_B_SPLINE_CURVE((1.00093939180657,1.00090979171842,1.))
REPRESENTATION_ITEM('')
);
#234=(
BOUNDED_CURVE()
B_SPLINE_CURVE(2,(#50272,#50273,#50274),.UNSPECIFIED.,.F.,.F.)
B_SPLINE_CURVE_WITH_KNOTS((3,3),(0.,0.0211644268265998),.UNSPECIFIED.)
CURVE()
GEOMETRIC_REPRESENTATION_ITEM()
RATIONAL_B_SPLINE_CURVE((1.,1.00090979171367,1.00093939180166))
REPRESENTATION_ITEM('')
);
#235=(
BOUNDED_CURVE()
B_SPLINE_CURVE(2,(#50277,#50278,#50279),.UNSPECIFIED.,.F.,.F.)
B_SPLINE_CURVE_WITH_KNOTS((3,3),(0.0225879098005594,0.0437523366271109),
 .UNSPECIFIED.)
CURVE()
GEOMETRIC_REPRESENTATION_ITEM()
RATIONAL_B_SPLINE_CURVE((1.00093939180571,1.00090979171758,1.))
REPRESENTATION_ITEM('')
);
#236=(
BOUNDED_CURVE()
B_SPLINE_CURVE(2,(#50286,#50287,#50288),.UNSPECIFIED.,.F.,.F.)
B_SPLINE_CURVE_WITH_KNOTS((3,3),(0.,0.0211644268265771),.UNSPECIFIED.)
CURVE()
GEOMETRIC_REPRESENTATION_ITEM()
RATIONAL_B_SPLINE_CURVE((1.,1.00090979171472,1.00093939180275))
REPRESENTATION_ITEM('')
);
#237=(
BOUNDED_CURVE()
B_SPLINE_CURVE(2,(#50291,#50292,#50293),.UNSPECIFIED.,.F.,.F.)
B_SPLINE_CURVE_WITH_KNOTS((3,3),(0.0225879098005193,0.0437523366271108),
 .UNSPECIFIED.)
CURVE()
GEOMETRIC_REPRESENTATION_ITEM()
RATIONAL_B_SPLINE_CURVE((1.00093939180378,1.00090979171571,1.))
REPRESENTATION_ITEM('')
);
#238=(
BOUNDED_CURVE()
B_SPLINE_CURVE(2,(#50300,#50301,#50302),.UNSPECIFIED.,.F.,.F.)
B_SPLINE_CURVE_WITH_KNOTS((3,3),(0.,0.0211644268265921),.UNSPECIFIED.)
CURVE()
GEOMETRIC_REPRESENTATION_ITEM()
RATIONAL_B_SPLINE_CURVE((1.,1.00090979171676,1.00093939180485))
REPRESENTATION_ITEM('')
);
#239=(
BOUNDED_CURVE()
B_SPLINE_CURVE(2,(#50305,#50306,#50307),.UNSPECIFIED.,.F.,.F.)
B_SPLINE_CURVE_WITH_KNOTS((3,3),(0.0225879098004847,0.0437523366271108),
 .UNSPECIFIED.)
CURVE()
GEOMETRIC_REPRESENTATION_ITEM()
RATIONAL_B_SPLINE_CURVE((1.00093939180062,1.00090979171266,1.))
REPRESENTATION_ITEM('')
);
#240=(
BOUNDED_CURVE()
B_SPLINE_CURVE(2,(#50314,#50315,#50316),.UNSPECIFIED.,.F.,.F.)
B_SPLINE_CURVE_WITH_KNOTS((3,3),(0.,0.0211644268265503),.UNSPECIFIED.)
CURVE()
GEOMETRIC_REPRESENTATION_ITEM()
RATIONAL_B_SPLINE_CURVE((1.,1.00090979171894,1.00093939180711))
REPRESENTATION_ITEM('')
);
#241=(
BOUNDED_CURVE()
B_SPLINE_CURVE(2,(#50319,#50320,#50321),.UNSPECIFIED.,.F.,.F.)
B_SPLINE_CURVE_WITH_KNOTS((3,3),(0.022587909800518,0.0437523366271109),
 .UNSPECIFIED.)
CURVE()
GEOMETRIC_REPRESENTATION_ITEM()
RATIONAL_B_SPLINE_CURVE((1.00093939180195,1.00090979171394,1.))
REPRESENTATION_ITEM('')
);
#242=(
BOUNDED_CURVE()
B_SPLINE_CURVE(2,(#50328,#50329,#50330),.UNSPECIFIED.,.F.,.F.)
B_SPLINE_CURVE_WITH_KNOTS((3,3),(0.,0.0211644268265849),.UNSPECIFIED.)
CURVE()
GEOMETRIC_REPRESENTATION_ITEM()
RATIONAL_B_SPLINE_CURVE((1.,1.00090979171243,1.00093939180038))
REPRESENTATION_ITEM('')
);
#243=(
BOUNDED_CURVE()
B_SPLINE_CURVE(2,(#50333,#50334,#50335),.UNSPECIFIED.,.F.,.F.)
B_SPLINE_CURVE_WITH_KNOTS((3,3),(0.0225879098005176,0.0437523366271109),
 .UNSPECIFIED.)
CURVE()
GEOMETRIC_REPRESENTATION_ITEM()
RATIONAL_B_SPLINE_CURVE((1.00093939180297,1.00090979171494,1.))
REPRESENTATION_ITEM('')
);
#244=(
BOUNDED_CURVE()
B_SPLINE_CURVE(2,(#50342,#50343,#50344),.UNSPECIFIED.,.F.,.F.)
B_SPLINE_CURVE_WITH_KNOTS((3,3),(0.,0.0211644268266227),.UNSPECIFIED.)
CURVE()
GEOMETRIC_REPRESENTATION_ITEM()
RATIONAL_B_SPLINE_CURVE((1.,1.00090979171573,1.00093939180379))
REPRESENTATION_ITEM('')
);
#245=(
BOUNDED_CURVE()
B_SPLINE_CURVE(2,(#50347,#50348,#50349),.UNSPECIFIED.,.F.,.F.)
B_SPLINE_CURVE_WITH_KNOTS((3,3),(0.0225879098005391,0.0437523366271109),
 .UNSPECIFIED.)
CURVE()
GEOMETRIC_REPRESENTATION_ITEM()
RATIONAL_B_SPLINE_CURVE((1.00093939180643,1.00090979171828,1.))
REPRESENTATION_ITEM('')
);
#246=(
BOUNDED_CURVE()
B_SPLINE_CURVE(2,(#50356,#50357,#50358),.UNSPECIFIED.,.F.,.F.)
B_SPLINE_CURVE_WITH_KNOTS((3,3),(0.,0.0211644268265862),.UNSPECIFIED.)
CURVE()
GEOMETRIC_REPRESENTATION_ITEM()
RATIONAL_B_SPLINE_CURVE((1.,1.00090979171409,1.0009393918021))
REPRESENTATION_ITEM('')
);
#247=(
BOUNDED_CURVE()
B_SPLINE_CURVE(2,(#50361,#50362,#50363),.UNSPECIFIED.,.F.,.F.)
B_SPLINE_CURVE_WITH_KNOTS((3,3),(0.0225879098005106,0.0437523366271109),
 .UNSPECIFIED.)
CURVE()
GEOMETRIC_REPRESENTATION_ITEM()
RATIONAL_B_SPLINE_CURVE((1.0009393918006,1.00090979171264,1.))
REPRESENTATION_ITEM('')
);
#248=(
BOUNDED_CURVE()
B_SPLINE_CURVE(2,(#50370,#50371,#50372),.UNSPECIFIED.,.F.,.F.)
B_SPLINE_CURVE_WITH_KNOTS((3,3),(0.,0.0211644268265897),.UNSPECIFIED.)
CURVE()
GEOMETRIC_REPRESENTATION_ITEM()
RATIONAL_B_SPLINE_CURVE((1.,1.00090979171702,1.00093939180512))
REPRESENTATION_ITEM('')
);
#249=(
BOUNDED_CURVE()
B_SPLINE_CURVE(2,(#50375,#50376,#50377),.UNSPECIFIED.,.F.,.F.)
B_SPLINE_CURVE_WITH_KNOTS((3,3),(0.0225879098004859,0.0437523366271109),
 .UNSPECIFIED.)
CURVE()
GEOMETRIC_REPRESENTATION_ITEM()
RATIONAL_B_SPLINE_CURVE((1.0009393918034,1.00090979171535,1.))
REPRESENTATION_ITEM('')
);
#250=(
BOUNDED_CURVE()
B_SPLINE_CURVE(2,(#50384,#50385,#50386),.UNSPECIFIED.,.F.,.F.)
B_SPLINE_CURVE_WITH_KNOTS((3,3),(0.,0.021164426826622),.UNSPECIFIED.)
CURVE()
GEOMETRIC_REPRESENTATION_ITEM()
RATIONAL_B_SPLINE_CURVE((1.,1.0009097917149,1.00093939180294))
REPRESENTATION_ITEM('')
);
#251=(
BOUNDED_CURVE()
B_SPLINE_CURVE(2,(#50389,#50390,#50391),.UNSPECIFIED.,.F.,.F.)
B_SPLINE_CURVE_WITH_KNOTS((3,3),(0.0225879098005208,0.0437523366271109),
 .UNSPECIFIED.)
CURVE()
GEOMETRIC_REPRESENTATION_ITEM()
RATIONAL_B_SPLINE_CURVE((1.00093939180214,1.00090979171413,1.))
REPRESENTATION_ITEM('')
);
#252=(
BOUNDED_CURVE()
B_SPLINE_CURVE(2,(#50398,#50399,#50400),.UNSPECIFIED.,.F.,.F.)
B_SPLINE_CURVE_WITH_KNOTS((3,3),(0.,0.021164426826624),.UNSPECIFIED.)
CURVE()
GEOMETRIC_REPRESENTATION_ITEM()
RATIONAL_B_SPLINE_CURVE((1.,1.00090979171573,1.00093939180379))
REPRESENTATION_ITEM('')
);
#253=(
BOUNDED_CURVE()
B_SPLINE_CURVE(2,(#50403,#50404,#50405),.UNSPECIFIED.,.F.,.F.)
B_SPLINE_CURVE_WITH_KNOTS((3,3),(0.0225879098005246,0.0437523366271109),
 .UNSPECIFIED.)
CURVE()
GEOMETRIC_REPRESENTATION_ITEM()
RATIONAL_B_SPLINE_CURVE((1.00093939179848,1.00090979171058,1.))
REPRESENTATION_ITEM('')
);
#254=(
BOUNDED_CURVE()
B_SPLINE_CURVE(2,(#50412,#50413,#50414),.UNSPECIFIED.,.F.,.F.)
B_SPLINE_CURVE_WITH_KNOTS((3,3),(0.,0.0211644268266093),.UNSPECIFIED.)
CURVE()
GEOMETRIC_REPRESENTATION_ITEM()
RATIONAL_B_SPLINE_CURVE((1.,1.00090979171292,1.00093939180089))
REPRESENTATION_ITEM('')
);
#255=(
BOUNDED_CURVE()
B_SPLINE_CURVE(2,(#50417,#50418,#50419),.UNSPECIFIED.,.F.,.F.)
B_SPLINE_CURVE_WITH_KNOTS((3,3),(0.0225879098005556,0.0437523366271108),
 .UNSPECIFIED.)
CURVE()
GEOMETRIC_REPRESENTATION_ITEM()
RATIONAL_B_SPLINE_CURVE((1.00093939180208,1.00090979171407,1.))
REPRESENTATION_ITEM('')
);
#256=(
BOUNDED_CURVE()
B_SPLINE_CURVE(2,(#50426,#50427,#50428),.UNSPECIFIED.,.F.,.F.)
B_SPLINE_CURVE_WITH_KNOTS((3,3),(0.,0.0211644268265253),.UNSPECIFIED.)
CURVE()
GEOMETRIC_REPRESENTATION_ITEM()
RATIONAL_B_SPLINE_CURVE((1.,1.00090979171634,1.00093939180442))
REPRESENTATION_ITEM('')
);
#257=(
BOUNDED_CURVE()
B_SPLINE_CURVE(2,(#50431,#50432,#50433),.UNSPECIFIED.,.F.,.F.)
B_SPLINE_CURVE_WITH_KNOTS((3,3),(0.0225879098004964,0.0437523366271109),
 .UNSPECIFIED.)
CURVE()
GEOMETRIC_REPRESENTATION_ITEM()
RATIONAL_B_SPLINE_CURVE((1.00093939180221,1.00090979171419,1.))
REPRESENTATION_ITEM('')
);
#258=(
BOUNDED_CURVE()
B_SPLINE_CURVE(2,(#50440,#50441,#50442),.UNSPECIFIED.,.F.,.F.)
B_SPLINE_CURVE_WITH_KNOTS((3,3),(0.,0.0211644268265929),.UNSPECIFIED.)
CURVE()
GEOMETRIC_REPRESENTATION_ITEM()
RATIONAL_B_SPLINE_CURVE((1.,1.00090979171394,1.00093939180195))
REPRESENTATION_ITEM('')
);
#259=(
BOUNDED_CURVE()
B_SPLINE_CURVE(2,(#50445,#50446,#50447),.UNSPECIFIED.,.F.,.F.)
B_SPLINE_CURVE_WITH_KNOTS((3,3),(0.0225879098005457,0.0437523366271109),
 .UNSPECIFIED.)
CURVE()
GEOMETRIC_REPRESENTATION_ITEM()
RATIONAL_B_SPLINE_CURVE((1.00093939180273,1.0009097917147,1.))
REPRESENTATION_ITEM('')
);
#260=(
BOUNDED_CURVE()
B_SPLINE_CURVE(2,(#50454,#50455,#50456),.UNSPECIFIED.,.F.,.F.)
B_SPLINE_CURVE_WITH_KNOTS((3,3),(0.,0.0211644268265952),.UNSPECIFIED.)
CURVE()
GEOMETRIC_REPRESENTATION_ITEM()
RATIONAL_B_SPLINE_CURVE((1.,1.00090979171439,1.00093939180241))
REPRESENTATION_ITEM('')
);
#261=(
BOUNDED_CURVE()
B_SPLINE_CURVE(2,(#50459,#50460,#50461),.UNSPECIFIED.,.F.,.F.)
B_SPLINE_CURVE_WITH_KNOTS((3,3),(0.0225879098005144,0.0437523366271109),
 .UNSPECIFIED.)
CURVE()
GEOMETRIC_REPRESENTATION_ITEM()
RATIONAL_B_SPLINE_CURVE((1.00093939180272,1.00090979171469,1.))
REPRESENTATION_ITEM('')
);
#262=(
BOUNDED_CURVE()
B_SPLINE_CURVE(2,(#50468,#50469,#50470),.UNSPECIFIED.,.F.,.F.)
B_SPLINE_CURVE_WITH_KNOTS((3,3),(0.,0.0211644268265596),.UNSPECIFIED.)
CURVE()
GEOMETRIC_REPRESENTATION_ITEM()
RATIONAL_B_SPLINE_CURVE((1.,1.00090979171197,1.00093939179992))
REPRESENTATION_ITEM('')
);
#263=(
BOUNDED_CURVE()
B_SPLINE_CURVE(2,(#50473,#50474,#50475),.UNSPECIFIED.,.F.,.F.)
B_SPLINE_CURVE_WITH_KNOTS((3,3),(0.0225879098005319,0.0437523366271109),
 .UNSPECIFIED.)
CURVE()
GEOMETRIC_REPRESENTATION_ITEM()
RATIONAL_B_SPLINE_CURVE((1.00093939180304,1.000909791715,1.))
REPRESENTATION_ITEM('')
);
#264=(
BOUNDED_CURVE()
B_SPLINE_CURVE(2,(#50482,#50483,#50484),.UNSPECIFIED.,.F.,.F.)
B_SPLINE_CURVE_WITH_KNOTS((3,3),(0.,0.0211644268266268),.UNSPECIFIED.)
CURVE()
GEOMETRIC_REPRESENTATION_ITEM()
RATIONAL_B_SPLINE_CURVE((1.,1.00090979171561,1.00093939180367))
REPRESENTATION_ITEM('')
);
#265=(
BOUNDED_CURVE()
B_SPLINE_CURVE(2,(#50487,#50488,#50489),.UNSPECIFIED.,.F.,.F.)
B_SPLINE_CURVE_WITH_KNOTS((3,3),(0.0225879098005574,0.0437523366271109),
 .UNSPECIFIED.)
CURVE()
GEOMETRIC_REPRESENTATION_ITEM()
RATIONAL_B_SPLINE_CURVE((1.00093939180693,1.00090979171876,1.))
REPRESENTATION_ITEM('')
);
#266=(
BOUNDED_CURVE()
B_SPLINE_CURVE(2,(#50496,#50497,#50498),.UNSPECIFIED.,.F.,.F.)
B_SPLINE_CURVE_WITH_KNOTS((3,3),(0.,0.0211644268265904),.UNSPECIFIED.)
CURVE()
GEOMETRIC_REPRESENTATION_ITEM()
RATIONAL_B_SPLINE_CURVE((1.,1.0009097917121,1.00093939180005))
REPRESENTATION_ITEM('')
);
#267=(
BOUNDED_CURVE()
B_SPLINE_CURVE(2,(#50501,#50502,#50503),.UNSPECIFIED.,.F.,.F.)
B_SPLINE_CURVE_WITH_KNOTS((3,3),(0.0225879098005213,0.0437523366271109),
 .UNSPECIFIED.)
CURVE()
GEOMETRIC_REPRESENTATION_ITEM()
RATIONAL_B_SPLINE_CURVE((1.00093939180114,1.00090979171316,1.))
REPRESENTATION_ITEM('')
);
#268=(
BOUNDED_CURVE()
B_SPLINE_CURVE(2,(#50510,#50511,#50512),.UNSPECIFIED.,.F.,.F.)
B_SPLINE_CURVE_WITH_KNOTS((3,3),(0.,0.0211644268266229),.UNSPECIFIED.)
CURVE()
GEOMETRIC_REPRESENTATION_ITEM()
RATIONAL_B_SPLINE_CURVE((1.,1.00090979171429,1.00093939180231))
REPRESENTATION_ITEM('')
);
#269=(
BOUNDED_CURVE()
B_SPLINE_CURVE(2,(#50525,#50526,#50527),.UNSPECIFIED.,.F.,.F.)
B_SPLINE_CURVE_WITH_KNOTS((3,3),(0.,0.0126130588257639),.UNSPECIFIED.)
CURVE()
GEOMETRIC_REPRESENTATION_ITEM()
RATIONAL_B_SPLINE_CURVE((1.,1.00234596681253,1.0032929802757))
REPRESENTATION_ITEM('')
);
#270=(
BOUNDED_CURVE()
B_SPLINE_CURVE(2,(#50531,#50532,#50533),.UNSPECIFIED.,.F.,.F.)
B_SPLINE_CURVE_WITH_KNOTS((3,3),(0.0296897347922131,0.0423027936179769),
 .UNSPECIFIED.)
CURVE()
GEOMETRIC_REPRESENTATION_ITEM()
RATIONAL_B_SPLINE_CURVE((1.00329298027569,1.00234596681253,1.))
REPRESENTATION_ITEM('')
);
#271=(
BOUNDED_CURVE()
B_SPLINE_CURVE(2,(#50535,#50536,#50537),.UNSPECIFIED.,.F.,.F.)
B_SPLINE_CURVE_WITH_KNOTS((3,3),(0.,0.0126130588257639),.UNSPECIFIED.)
CURVE()
GEOMETRIC_REPRESENTATION_ITEM()
RATIONAL_B_SPLINE_CURVE((1.,1.00234596681251,1.00329298027567))
REPRESENTATION_ITEM('')
);
#272=(
BOUNDED_CURVE()
B_SPLINE_CURVE(2,(#50541,#50542,#50543),.UNSPECIFIED.,.F.,.F.)
B_SPLINE_CURVE_WITH_KNOTS((3,3),(0.0296897347922128,0.0423027936179769),
 .UNSPECIFIED.)
CURVE()
GEOMETRIC_REPRESENTATION_ITEM()
RATIONAL_B_SPLINE_CURVE((1.00329298027567,1.00234596681251,1.))
REPRESENTATION_ITEM('')
);
#273=(
BOUNDED_CURVE()
B_SPLINE_CURVE(2,(#50545,#50546,#50547),.UNSPECIFIED.,.F.,.F.)
B_SPLINE_CURVE_WITH_KNOTS((3,3),(0.,0.0126130588257636),.UNSPECIFIED.)
CURVE()
GEOMETRIC_REPRESENTATION_ITEM()
RATIONAL_B_SPLINE_CURVE((1.,1.00234596681253,1.00329298027569))
REPRESENTATION_ITEM('')
);
#274=(
BOUNDED_CURVE()
B_SPLINE_CURVE(2,(#50551,#50552,#50553),.UNSPECIFIED.,.F.,.F.)
B_SPLINE_CURVE_WITH_KNOTS((3,3),(0.0296897347922129,0.0423027936179769),
 .UNSPECIFIED.)
CURVE()
GEOMETRIC_REPRESENTATION_ITEM()
RATIONAL_B_SPLINE_CURVE((1.00329298027566,1.0023459668125,1.))
REPRESENTATION_ITEM('')
);
#275=(
BOUNDED_CURVE()
B_SPLINE_CURVE(2,(#50555,#50556,#50557),.UNSPECIFIED.,.F.,.F.)
B_SPLINE_CURVE_WITH_KNOTS((3,3),(0.,0.0126130588257639),.UNSPECIFIED.)
CURVE()
GEOMETRIC_REPRESENTATION_ITEM()
RATIONAL_B_SPLINE_CURVE((1.,1.00234596681251,1.00329298027567))
REPRESENTATION_ITEM('')
);
#276=(
BOUNDED_CURVE()
B_SPLINE_CURVE(2,(#50561,#50562,#50563),.UNSPECIFIED.,.F.,.F.)
B_SPLINE_CURVE_WITH_KNOTS((3,3),(0.0296897347922131,0.0423027936179769),
 .UNSPECIFIED.)
CURVE()
GEOMETRIC_REPRESENTATION_ITEM()
RATIONAL_B_SPLINE_CURVE((1.00329298027568,1.00234596681252,1.))
REPRESENTATION_ITEM('')
);
#277=(
BOUNDED_CURVE()
B_SPLINE_CURVE(2,(#50565,#50566,#50567),.UNSPECIFIED.,.F.,.F.)
B_SPLINE_CURVE_WITH_KNOTS((3,3),(0.,0.0126130588257641),.UNSPECIFIED.)
CURVE()
GEOMETRIC_REPRESENTATION_ITEM()
RATIONAL_B_SPLINE_CURVE((1.,1.00234596681251,1.00329298027567))
REPRESENTATION_ITEM('')
);
#278=(
BOUNDED_CURVE()
B_SPLINE_CURVE(2,(#50571,#50572,#50573),.UNSPECIFIED.,.F.,.F.)
B_SPLINE_CURVE_WITH_KNOTS((3,3),(0.0296897347922131,0.0423027936179769),
 .UNSPECIFIED.)
CURVE()
GEOMETRIC_REPRESENTATION_ITEM()
RATIONAL_B_SPLINE_CURVE((1.0032929802757,1.00234596681253,1.))
REPRESENTATION_ITEM('')
);
#279=(
BOUNDED_CURVE()
B_SPLINE_CURVE(2,(#50575,#50576,#50577),.UNSPECIFIED.,.F.,.F.)
B_SPLINE_CURVE_WITH_KNOTS((3,3),(0.,0.0126130588257639),.UNSPECIFIED.)
CURVE()
GEOMETRIC_REPRESENTATION_ITEM()
RATIONAL_B_SPLINE_CURVE((1.,1.00234596681251,1.00329298027567))
REPRESENTATION_ITEM('')
);
#280=(
BOUNDED_CURVE()
B_SPLINE_CURVE(2,(#50580,#50581,#50582),.UNSPECIFIED.,.F.,.F.)
B_SPLINE_CURVE_WITH_KNOTS((3,3),(0.029689734792213,0.0423027936179769),
 .UNSPECIFIED.)
CURVE()
GEOMETRIC_REPRESENTATION_ITEM()
RATIONAL_B_SPLINE_CURVE((1.00329298027566,1.00234596681251,1.))
REPRESENTATION_ITEM('')
);
#503=TOROIDAL_SURFACE('',#27630,1.5635,0.1);
#504=TOROIDAL_SURFACE('',#27822,2.55,0.2);
#572=B_SPLINE_CURVE_WITH_KNOTS('',3,(#42119,#42120,#42121,#42122,#42123,
#42124,#42125,#42126,#42127,#42128,#42129,#42130,#42131,#42132,#42133,#42134,
#42135,#42136,#42137,#42138,#42139,#42140,#42141,#42142,#42143,#42144,#42145,
#42146,#42147,#42148,#42149,#42150,#42151,#42152,#42153,#42154,#42155,#42156,
#42157,#42158,#42159,#42160,#42161,#42162,#42163,#42164,#42165,#42166,#42167,
#42168,#42169,#42170,#42171,#42172,#42173,#42174,#42175,#42176,#42177,#42178,
#42179,#42180,#42181,#42182,#42183,#42184,#42185,#42186,#42187,#42188,#42189,
#42190,#42191,#42192,#42193,#42194,#42195,#42196,#42197,#42198,#42199,#42200,
#42201,#42202,#42203,#42204,#42205,#42206,#42207,#42208,#42209,#42210,#42211,
#42212,#42213,#42214,#42215),.UNSPECIFIED.,.F.,.F.,(4,3,3,3,3,3,3,3,3,3,
3,3,3,3,3,3,3,3,3,3,3,3,3,3,3,3,3,3,3,3,3,3,4),(10.375658882214,10.4940757531313,
10.6123285343078,10.7304723820773,10.8485622595653,10.9667391963694,11.0849569770027,
11.2034015018678,11.2943915536004,11.4190730285709,11.5387903701137,11.6583914925965,
11.7779288428205,11.8974547568011,12.0171050008759,12.1368293768595,12.2567726910946,
12.2918433533645,12.416524828335,12.535895449855,12.655144429834,12.7743249216265,
12.8934899602376,13.0127760613286,13.1321339785519,13.2517111469998,13.2892951531286,
13.4090351474352,13.5285879960393,13.6480165300828,13.7673687408495,13.8867531641114,
13.9755457854933),.UNSPECIFIED.);
#573=B_SPLINE_CURVE_WITH_KNOTS('',3,(#42218,#42219,#42220,#42221,#42222,
#42223,#42224,#42225,#42226,#42227,#42228,#42229,#42230,#42231,#42232,#42233,
#42234,#42235,#42236,#42237,#42238,#42239,#42240,#42241,#42242,#42243,#42244,
#42245,#42246,#42247,#42248,#42249,#42250,#42251,#42252,#42253,#42254,#42255,
#42256,#42257,#42258,#42259,#42260,#42261,#42262,#42263,#42264,#42265,#42266,
#42267,#42268,#42269,#42270,#42271,#42272,#42273,#42274,#42275,#42276,#42277,
#42278),.UNSPECIFIED.,.F.,.F.,(4,3,3,3,3,3,3,3,3,3,3,3,3,3,3,3,3,3,3,3,
4),(11.6159397475002,11.7406212224707,11.8630161036116,11.9853820192075,
12.1077619590757,12.2341693561229,12.3568053456408,12.4850984464526,12.6133915472643,
12.7380730222348,12.8564493642578,12.9746907770413,13.092852164952,13.2109882875043,
13.3292381165421,13.4475540306047,13.5660912434974,13.6108433470284,13.7306772169464,
13.8535403363031,13.9764034556599),.UNSPECIFIED.);
#574=B_SPLINE_CURVE_WITH_KNOTS('',3,(#42284,#42285,#42286,#42287,#42288,
#42289,#42290,#42291),.UNSPECIFIED.,.F.,.F.,(4,1,1,1,1,4),(15.707963267949,
16.2816505524208,17.2791023521849,18.2765541519489,19.274005951713,20.2591548474271),
 .UNSPECIFIED.);
#575=B_SPLINE_CURVE_WITH_KNOTS('',3,(#42292,#42293,#42294,#42295,#42296,
#42297,#42298,#42299,#42300,#42301,#42302,#42303,#42304,#42305,#42306,#42307,
#42308,#42309,#42310,#42311,#42312,#42313,#42314,#42315,#42316,#42317,#42318,
#42319,#42320,#42321,#42322,#42323,#42324,#42325,#42326,#42327,#42328,#42329,
#42330,#42331,#42332,#42333,#42334,#42335,#42336,#42337,#42338,#42339,#42340),
 .UNSPECIFIED.,.F.,.F.,(4,3,3,3,3,3,3,3,3,3,3,3,3,3,3,3,4),(13.9755457854933,
14.0950474522977,14.2147780392736,14.2867469528926,14.4114284278631,14.5309629044171,
14.6503778549302,14.7697261077932,14.8890603761317,15.0085166358431,15.1280454520991,
15.2477928763345,15.2841987526567,15.4149977650239,15.5453793024121,15.6751404895075,
15.707963267949),.UNSPECIFIED.);
#576=B_SPLINE_CURVE_WITH_KNOTS('',3,(#42342,#42343,#42344,#42345,#42346,
#42347,#42348,#42349,#42350,#42351,#42352,#42353,#42354,#42355,#42356,#42357,
#42358,#42359,#42360,#42361,#42362,#42363,#42364,#42365,#42366,#42367,#42368,
#42369,#42370,#42371,#42372,#42373,#42374,#42375,#42376,#42377,#42378,#42379,
#42380,#42381,#42382,#42383,#42384,#42385,#42386,#42387,#42388,#42389,#42390),
 .UNSPECIFIED.,.F.,.F.,(4,3,3,3,3,3,3,3,3,3,3,3,3,3,3,3,4),(13.9764034556599,
14.0958475312092,14.2152765458788,14.3348246052786,14.4544439781282,14.5742776798784,
14.6082951467925,14.732976621763,14.8526939294842,14.9722950172258,15.0918323318563,
15.2113582094568,15.3310084162456,15.4507327543743,15.5706760302905,15.6057469465565,
15.707963267949),.UNSPECIFIED.);
#577=B_SPLINE_CURVE_WITH_KNOTS('',3,(#42391,#42392,#42393,#42394,#42395,
#42396,#42397,#42398,#42399,#42400,#42401,#42402,#42403,#42404,#42405,#42406,
#42407,#42408,#42409,#42410,#42411,#42412,#42413,#42414,#42415,#42416,#42417,
#42418,#42419,#42420,#42421,#42422,#42423,#42424,#42425,#42426,#42427,#42428,
#42429,#42430,#42431,#42432,#42433,#42434,#42435,#42436,#42437,#42438,#42439,
#42440,#42441,#42442,#42443,#42444,#42445,#42446,#42447,#42448,#42449,#42450,
#42451,#42452,#42453,#42454,#42455,#42456,#42457,#42458,#42459,#42460,#42461,
#42462,#42463,#42464,#42465,#42466,#42467,#42468,#42469,#42470,#42471,#42472,
#42473,#42474,#42475,#42476,#42477,#42478,#42479,#42480,#42481,#42482,#42483,
#42484,#42485,#42486,#42487,#42488,#42489,#42490,#42491,#42492,#42493,#42494,
#42495,#42496,#42497,#42498,#42499,#42500,#42501,#42502,#42503,#42504,#42505,
#42506,#42507,#42508,#42509,#42510,#42511,#42512,#42513,#42514,#42515,#42516,
#42517,#42518,#42519,#42520,#42521,#42522),.UNSPECIFIED.,.F.,.F.,(4,2,2,
2,2,2,2,2,2,2,2,2,2,2,2,2,2,2,2,2,2,2,2,2,2,2,2,2,2,2,2,2,2,2,2,2,2,2,2,
2,2,2,2,2,2,2,2,2,2,2,2,2,2,2,2,2,2,2,2,2,2,2,2,2,2,4),(-1.4844552026344,
-1.4687011027748,-1.44918397915652,-1.44256183555755,-1.43903750723833,
-1.43605059148294,-1.43240348709774,-1.42536314863845,-1.39659887439657,
-1.38770269719831,-1.38202502955999,-1.37970402710656,-1.37799993621768,
-1.37597493952397,-1.37216460249553,-1.35415839979739,-1.33678878154718,
-1.32633578172632,-1.32217004114304,-1.31910561777712,-1.31582777999402,
-1.31053219723985,-1.28253713340363,-1.27130417776362,-1.26675415588416,
-1.263239795581,-1.26129440045607,-1.25955561692127,-1.25744215010448,-1.25204579873155,
-1.22788915726227,-1.21371449333436,-1.20700536901352,-1.20344927278234,
-1.20044123866201,-1.19677420197572,-1.18947140855754,-1.16322223138289,
-1.15299657988415,-1.14676844006402,-1.1443565384256,-1.14263564515379,
-1.14065300064361,-1.13703741418214,-1.11526709117371,-1.09576750079987,
-1.08913123132775,-1.08559192209381,-1.08258745843083,-1.07891171828405,
-1.07178573968222,-1.04544936146396,-1.03520056552958,-1.02896468341169,
-1.02655299984568,-1.02483256359335,-1.02284935705574,-1.01923551350903,
-0.992909690546232,-0.974649809101956,-0.969804634397468,-0.966621120941967,
-0.96354867336833,-0.959827504685779,-0.950405395849426,-0.946967500878228),
 .UNSPECIFIED.);
#578=B_SPLINE_CURVE_WITH_KNOTS('',3,(#42528,#42529,#42530,#42531,#42532,
#42533,#42534,#42535,#42536,#42537,#42538,#42539,#42540,#42541,#42542,#42543,
#42544,#42545,#42546,#42547,#42548,#42549,#42550,#42551,#42552,#42553,#42554,
#42555,#42556,#42557,#42558,#42559,#42560,#42561,#42562,#42563,#42564,#42565,
#42566,#42567,#42568,#42569,#42570,#42571,#42572,#42573,#42574,#42575,#42576,
#42577,#42578,#42579,#42580,#42581,#42582,#42583,#42584,#42585,#42586,#42587,
#42588,#42589,#42590,#42591,#42592,#42593,#42594,#42595,#42596,#42597,#42598,
#42599,#42600,#42601,#42602,#42603,#42604,#42605,#42606,#42607,#42608,#42609,
#42610,#42611,#42612,#42613,#42614,#42615,#42616,#42617,#42618,#42619,#42620,
#42621,#42622,#42623,#42624,#42625,#42626,#42627,#42628,#42629,#42630,#42631,
#42632,#42633,#42634,#42635,#42636,#42637,#42638,#42639,#42640,#42641,#42642,
#42643,#42644,#42645,#42646,#42647,#42648,#42649,#42650,#42651),
 .UNSPECIFIED.,.F.,.F.,(4,3,3,3,3,3,3,3,3,3,3,3,3,3,3,3,3,3,3,3,3,3,3,3,
3,3,3,3,3,3,3,3,3,3,3,3,3,3,3,3,3,4),(21.9911485751285,22.1403488486178,
22.2663613510052,22.3910428259757,22.5105544745963,22.6299461484162,22.7492707221346,
22.8685809545573,22.9880128266408,23.1075170226214,23.2272397326252,23.2638131507693,
23.3884946257398,23.5080061717731,23.6273977426734,23.7467222133455,23.8660323428005,
23.9854641128103,24.1049682071207,24.224690817093,24.2612649505334,24.3859464255039,
24.5054579125581,24.6248494232083,24.7441738324787,24.8634838994978,24.982915605997,
25.102419636098,25.2221421814788,25.2587167502974,25.3833982252679,25.5029097714894,
25.622301342095,25.7416258119897,25.8609359401839,25.9803677082202,26.0998718001396,
26.2195944071251,26.2561685500615,26.3758980412773,26.49541998721,26.5429554215432),
 .UNSPECIFIED.);
#579=B_SPLINE_CURVE_WITH_KNOTS('',3,(#42652,#42653,#42654,#42655,#42656,
#42657),.UNSPECIFIED.,.F.,.F.,(4,1,1,4),(20.2591548474271,20.2714577514771,
21.2689095512411,21.9911485751285),.UNSPECIFIED.);
#580=B_SPLINE_CURVE_WITH_KNOTS('',3,(#42658,#42659,#42660,#42661,#42662,
#42663,#42664,#42665,#42666,#42667,#42668,#42669,#42670,#42671,#42672,#42673,
#42674,#42675,#42676,#42677,#42678,#42679,#42680,#42681,#42682,#42683,#42684,
#42685,#42686,#42687,#42688,#42689,#42690,#42691,#42692,#42693,#42694,#42695,
#42696,#42697,#42698,#42699,#42700,#42701,#42702,#42703,#42704,#42705,#42706,
#42707,#42708,#42709,#42710,#42711,#42712,#42713,#42714,#42715,#42716,#42717,
#42718,#42719,#42720,#42721,#42722,#42723,#42724,#42725,#42726,#42727,#42728,
#42729,#42730,#42731,#42732,#42733,#42734,#42735,#42736,#42737,#42738,#42739,
#42740,#42741,#42742,#42743,#42744,#42745,#42746,#42747,#42748,#42749,#42750,
#42751,#42752,#42753,#42754,#42755,#42756,#42757,#42758,#42759,#42760,#42761,
#42762,#42763,#42764,#42765,#42766,#42767,#42768,#42769,#42770,#42771,#42772,
#42773,#42774,#42775,#42776,#42777,#42778,#42779,#42780,#42781,#42782,#42783,
#42784,#42785,#42786,#42787,#42788,#42789,#42790,#42791,#42792,#42793,#42794,
#42795,#42796,#42797,#42798,#42799,#42800,#42801,#42802,#42803,#42804,#42805,
#42806,#42807,#42808,#42809,#42810,#42811,#42812,#42813,#42814,#42815,#42816,
#42817,#42818,#42819,#42820,#42821,#42822,#42823,#42824,#42825,#42826,#42827,
#42828,#42829,#42830,#42831,#42832,#42833,#42834,#42835),.UNSPECIFIED.,
 .F.,.F.,(4,2,2,2,2,2,2,2,2,2,2,2,2,2,2,2,2,2,2,2,2,2,2,2,2,2,2,2,2,2,2,
2,2,2,2,2,2,2,2,2,2,2,2,2,2,2,2,2,2,2,2,2,2,2,2,2,2,2,2,2,2,2,2,2,2,2,2,
2,2,2,2,2,2,2,2,2,2,2,2,2,2,2,2,2,2,2,2,2,4),(-0.946967500878228,-0.922468381690924,
-0.9154497701354,-0.910623957938968,-0.908431352505289,-0.906728346015609,
-0.904587904538674,-0.900053005137895,-0.877656795984915,-0.863912309720635,
-0.854825984971083,-0.850861003386889,-0.847829553977103,-0.844475295835823,
-0.838783116619881,-0.814017640143533,-0.795421493232167,-0.791998583472935,
-0.790076333873346,-0.78835448338196,-0.785825473887368,-0.779220455523365,
-0.756333432072061,-0.742490702556759,-0.736452638884795,-0.732691638190658,
-0.72968033513473,-0.726202818948079,-0.719893697788476,-0.711793903380419,
-0.689064812622101,-0.676898828139983,-0.673877130821646,-0.672040096985284,
-0.670247592003958,-0.667436559693061,-0.657525906745013,-0.632781276830887,
-0.620497135619826,-0.616020208073954,-0.612938375214289,-0.609768497229987,
-0.604991286731526,-0.587983419408895,-0.566370404228104,-0.558453727339228,
-0.555757057426252,-0.55416241386504,-0.552346877506135,-0.54942650625239,
-0.538007567037238,-0.523231383622395,-0.503753954143981,-0.498796130489219,
-0.495590539120956,-0.492498210231896,-0.488135856670422,-0.476038041351705,
-0.452682391769221,-0.441262258631334,-0.438270575162246,-0.436439791116939,
-0.434641737719111,-0.431804121868399,-0.421558482683881,-0.394402140799076,
-0.384280571523664,-0.38006974107086,-0.377002865800729,-0.373750673545418,
-0.368561547521138,-0.362325469483097,-0.348724021782114,-0.326744854498311,
-0.322227696775696,-0.32005298073731,-0.318319520768126,-0.316422919866036,
-0.313122529392659,-0.294157839183677,-0.269596750480482,-0.263891141771936,
-0.260534051336492,-0.257503056534744,-0.253543047323409,-0.244490680461125,
-0.230827395743105,-0.20867538173197,-0.204951810495098),.UNSPECIFIED.);
#581=B_SPLINE_CURVE_WITH_KNOTS('',3,(#42841,#42842,#42843,#42844,#42845,
#42846,#42847,#42848,#42849,#42850,#42851,#42852,#42853,#42854,#42855,#42856,
#42857,#42858,#42859,#42860,#42861,#42862,#42863,#42864,#42865,#42866,#42867,
#42868,#42869,#42870,#42871,#42872,#42873,#42874,#42875,#42876,#42877,#42878,
#42879,#42880,#42881,#42882,#42883,#42884,#42885,#42886,#42887,#42888,#42889,
#42890,#42891,#42892,#42893,#42894,#42895,#42896,#42897,#42898,#42899,#42900,
#42901,#42902,#42903,#42904,#42905,#42906,#42907,#42908,#42909,#42910,#42911,
#42912,#42913,#42914,#42915,#42916,#42917,#42918,#42919,#42920,#42921,#42922,
#42923,#42924,#42925,#42926,#42927,#42928,#42929,#42930,#42931,#42932,#42933,
#42934,#42935,#42936,#42937,#42938,#42939,#42940,#42941,#42942,#42943,#42944,
#42945,#42946,#42947,#42948,#42949,#42950,#42951,#42952,#42953,#42954,#42955,
#42956,#42957,#42958,#42959,#42960,#42961,#42962,#42963,#42964,#42965,#42966,
#42967,#42968,#42969,#42970,#42971,#42972,#42973,#42974,#42975,#42976),
 .UNSPECIFIED.,.F.,.F.,(4,2,2,2,2,2,2,2,2,2,2,2,2,2,2,2,2,2,2,2,2,2,2,2,
2,2,2,2,2,2,2,2,2,2,2,2,2,2,2,2,2,2,2,2,2,2,2,2,2,2,2,2,2,2,2,2,2,2,2,2,
2,2,2,2,2,2,2,4),(-0.537798266923256,-0.537506177459864,-0.531828068379447,
-0.528476355256648,-0.525443664043516,-0.521471867161082,-0.512343872931895,
-0.49849892361335,-0.47582306554166,-0.47155583492274,-0.469464843665186,
-0.467930616541699,-0.465780794147544,-0.461194588604739,-0.454660833371519,
-0.431721753353976,-0.417784759497364,-0.413092174304632,-0.410253500056579,
-0.407171279366293,-0.402868930199637,-0.391294205042398,-0.370114387362929,
-0.356068269150041,-0.352971699200996,-0.351118368510108,-0.34933777418127,
-0.346585987814439,-0.33736871064637,-0.316618981244855,-0.300306726738104,
-0.295478867603218,-0.292298808074558,-0.289188091770254,-0.284724252264618,
-0.271670552930376,-0.242972075436281,-0.236923170882173,-0.234478471263787,
-0.232752178756607,-0.230783658570783,-0.227139109909182,-0.222361304504011,
-0.210140098101275,-0.183923339213203,-0.178379309571443,-0.175054630686975,
-0.172014250956594,-0.167984732748016,-0.158473319658752,-0.14367931676018,
-0.12143378486745,-0.117854328944166,-0.115878250468057,-0.114154047461705,
-0.111724251984774,-0.105370515420435,-0.0948209917293399,-0.0672337401268089,
-0.0611511488656624,-0.0576837640980859,-0.0546703587498685,-0.0508923214782159,
-0.0429597972058361,-0.0317796072960284,-0.00405094180321479,-0.00172829229899956,
-0.000347817018397109),.UNSPECIFIED.);
#582=B_SPLINE_CURVE_WITH_KNOTS('',3,(#42977,#42978,#42979,#42980,#42981,
#42982,#42983,#42984,#42985,#42986,#42987,#42988,#42989,#42990,#42991,#42992,
#42993,#42994,#42995,#42996,#42997,#42998,#42999,#43000,#43001,#43002,#43003,
#43004,#43005,#43006,#43007,#43008,#43009,#43010,#43011,#43012,#43013,#43014,
#43015,#43016,#43017,#43018,#43019,#43020,#43021,#43022,#43023,#43024,#43025),
 .UNSPECIFIED.,.F.,.F.,(4,3,3,3,3,3,3,3,3,3,3,3,3,3,3,3,4),(26.5429554215432,
26.662316983425,26.7816302714825,26.9010405400129,27.0204926839711,27.1401882500657,
27.2536203498256,27.3783018247961,27.4978133478951,27.6172048951266,27.7365293414421,
27.8558394458981,27.9752711901376,28.0947752581988,28.2144978414786,28.2510721495896,
28.2743338823081),.UNSPECIFIED.);
#583=B_SPLINE_CURVE_WITH_KNOTS('',3,(#43027,#43028,#43029,#43030,#43031,
#43032,#43033,#43034,#43035,#43036,#43037,#43038,#43039,#43040,#43041,#43042,
#43043,#43044,#43045,#43046,#43047,#43048,#43049,#43050,#43051,#43052,#43053,
#43054,#43055,#43056,#43057,#43058,#43059,#43060,#43061,#43062,#43063,#43064,
#43065,#43066,#43067,#43068,#43069,#43070,#43071,#43072,#43073,#43074,#43075,
#43076,#43077,#43078,#43079,#43080,#43081,#43082,#43083,#43084),
 .UNSPECIFIED.,.F.,.F.,(4,2,2,2,2,2,2,2,2,2,2,2,2,2,2,2,2,2,2,2,2,2,2,2,
2,2,2,2,4),(-0.204951810495098,-0.203866411973684,-0.201677215860401,-0.19997466997083,
-0.197832178585648,-0.193285796636486,-0.186830922190499,-0.164570720576338,
-0.149832570566503,-0.145128439035206,-0.14228798365646,-0.139207791737628,
-0.134915838393065,-0.123426758250936,-0.102575518544609,-0.0881021819418686,
-0.0849945881575372,-0.0831390340203034,-0.0813604380740051,-0.0786179340158351,
-0.0695181708168154,-0.0493400313179309,-0.0322943140846844,-0.0274741063806191,
-0.0242958061789282,-0.0211844177002832,-0.0180756740011476,-0.0114983792101034,
-0.000347679328245713),.UNSPECIFIED.);
#584=B_SPLINE_CURVE_WITH_KNOTS('',3,(#43085,#43086,#43087,#43088,#43089,
#43090,#43091,#43092,#43093,#43094,#43095,#43096,#43097,#43098,#43099,#43100,
#43101,#43102,#43103,#43104,#43105,#43106,#43107,#43108,#43109,#43110,#43111,
#43112,#43113,#43114,#43115,#43116,#43117,#43118,#43119,#43120,#43121,#43122,
#43123,#43124,#43125,#43126,#43127,#43128,#43129,#43130,#43131,#43132,#43133,
#43134,#43135,#43136,#43137,#43138,#43139,#43140,#43141,#43142,#43143,#43144,
#43145,#43146,#43147,#43148,#43149,#43150,#43151,#43152,#43153,#43154,#43155,
#43156,#43157,#43158,#43159,#43160,#43161,#43162,#43163,#43164,#43165,#43166,
#43167,#43168,#43169,#43170,#43171,#43172,#43173,#43174,#43175,#43176,#43177,
#43178,#43179,#43180,#43181,#43182,#43183,#43184,#43185,#43186,#43187,#43188,
#43189,#43190,#43191,#43192,#43193,#43194,#43195,#43196,#43197,#43198,#43199,
#43200,#43201,#43202,#43203,#43204,#43205,#43206,#43207,#43208,#43209,#43210,
#43211,#43212,#43213,#43214,#43215,#43216,#43217,#43218),.UNSPECIFIED.,
 .F.,.F.,(4,2,2,2,2,2,2,2,2,2,2,2,2,2,2,2,2,2,2,2,2,2,2,2,2,2,2,2,2,2,2,
2,2,2,2,2,2,2,2,2,2,2,2,2,2,2,2,2,2,2,2,2,2,2,2,2,2,2,2,2,2,2,2,2,2,2,4),
(-1.48424114304962,-1.45604830120501,-1.45378992240823,-1.45089582985086,
-1.4490862183476,-1.44748832179174,-1.44477148214394,-1.43666243918882,
-1.4152524700204,-1.40391645806674,-1.39590905713369,-1.39211920263731,
-1.38913352407874,-1.3856871257414,-1.37970053019196,-1.34959551788675,
-1.34054677256897,-1.33655821862586,-1.3333790029775,-1.33150834333437,
-1.32976132477736,-1.32708995194451,-1.31938996172512,-1.29979482818213,
-1.28074995764395,-1.27586985834611,-1.27268006380297,-1.26961349564257,
-1.26591420844108,-1.25665984176262,-1.2285012221601,-1.21813033006686,
-1.21528316827322,-1.21348325667859,-1.2116549800296,-1.20867453763984,
-1.19738117055466,-1.17393361909052,-1.16181821780584,-1.15745437878462,
-1.15436201404728,-1.15115724093523,-1.14620250992566,-1.1267277110755,
-1.10867429175684,-1.10003980983029,-1.0973431720958,-1.09557375209416,
-1.09370495614477,-1.09053485040334,-1.07281567825276,-1.05479576455955,
-1.04727433373738,-1.04130064784165,-1.03788967846321,-1.03486973065885,
-1.03100774115379,-1.02257121807353,-0.993940066231286,-0.986307563268444,
-0.981189491840714,-0.978947672249757,-0.977405866271079,-0.975387956099528,
-0.971611167607907,-0.952423986733965,-0.946896429152393),.UNSPECIFIED.);
#585=B_SPLINE_CURVE_WITH_KNOTS('',3,(#43223,#43224,#43225,#43226,#43227,
#43228,#43229,#43230,#43231,#43232,#43233,#43234,#43235,#43236,#43237,#43238,
#43239,#43240,#43241,#43242,#43243,#43244,#43245,#43246,#43247,#43248,#43249,
#43250,#43251,#43252,#43253,#43254,#43255,#43256,#43257,#43258,#43259,#43260,
#43261,#43262,#43263,#43264,#43265,#43266,#43267,#43268,#43269,#43270,#43271,
#43272,#43273,#43274,#43275,#43276,#43277,#43278,#43279,#43280,#43281,#43282,
#43283,#43284,#43285,#43286,#43287,#43288,#43289,#43290,#43291,#43292,#43293,
#43294,#43295,#43296,#43297,#43298,#43299,#43300,#43301,#43302,#43303,#43304,
#43305,#43306,#43307,#43308,#43309,#43310,#43311,#43312,#43313,#43314,#43315,
#43316,#43317,#43318,#43319,#43320,#43321,#43322,#43323,#43324,#43325,#43326,
#43327,#43328,#43329,#43330,#43331,#43332,#43333,#43334,#43335,#43336,#43337,
#43338,#43339,#43340,#43341,#43342,#43343,#43344,#43345,#43346,#43347,#43348,
#43349,#43350,#43351,#43352,#43353,#43354,#43355,#43356,#43357,#43358,#43359,
#43360,#43361,#43362,#43363,#43364,#43365,#43366,#43367,#43368,#43369,#43370,
#43371,#43372,#43373,#43374,#43375,#43376,#43377,#43378,#43379,#43380,#43381,
#43382,#43383,#43384,#43385,#43386,#43387,#43388,#43389,#43390,#43391,#43392,
#43393,#43394),.UNSPECIFIED.,.F.,.F.,(4,2,2,2,2,2,2,2,2,2,2,2,2,2,2,2,2,
2,2,2,2,2,2,2,2,2,2,2,2,2,2,2,2,2,2,2,2,2,2,2,2,2,2,2,2,2,2,2,2,2,2,2,2,
2,2,2,2,2,2,2,2,2,2,2,2,2,2,2,2,2,2,2,2,2,2,2,2,2,2,2,2,2,2,2,2,4),(-1.27966179244307,
-1.25432717498015,-1.24158842886276,-1.2371574925959,-1.2340531215572,-1.230865718625,
-1.22599879383902,-1.20863462638208,-1.18878268537098,-1.17974795108809,
-1.17701303955952,-1.17523602989445,-1.17337834488173,-1.17026057131706,
-1.15477728216396,-1.14126503865543,-1.13009250046016,-1.12216360894302,
-1.11838673713112,-1.11537396990238,-1.11190699758364,-1.10582434286145,
-1.07321315589925,-1.06228504618835,-1.05939720603118,-1.0575885328328,
-1.05576912087322,-1.05283101130116,-1.042165278365,-1.0181625283419,-1.00592840967352,
-1.00155107299411,-0.99845596497942,-0.995254117715596,-0.990315806241641,
-0.97096163951348,-0.956362066789855,-0.944624942034149,-0.941684404284013,
-0.939864510715884,-0.938272617597187,-0.935591697269273,-0.927813272939215,
-0.901041368883797,-0.888286906079143,-0.883854085520051,-0.880749188036927,
-0.877561907294845,-0.872696513530942,-0.855396477001483,-0.8354872592761,
-0.826440120405065,-0.823703904789483,-0.821926535121514,-0.820299941522499,
-0.817429748403217,-0.807925467898566,-0.782888236627016,-0.770446084880686,
-0.766046329086853,-0.762947409578457,-0.760128455756349,-0.755549687091231,
-0.742209132301279,-0.718619495801313,-0.708938212870643,-0.706072629149713,
-0.704446909773715,-0.70266865940466,-0.699928157616893,-0.690833355869004,
-0.670688859175166,-0.653687280382199,-0.648832169237673,-0.645646882679134,
-0.642540424940144,-0.638099238427744,-0.625266498095185,-0.598035051358098,
-0.590673835796256,-0.58804340024516,-0.586303653107998,-0.584418742815152,
-0.581174035884805,-0.562400442600069,-0.537798266923256),.UNSPECIFIED.);
#586=B_SPLINE_CURVE_WITH_KNOTS('',3,(#43395,#43396,#43397,#43398,#43399,
#43400,#43401,#43402,#43403,#43404,#43405,#43406,#43407,#43408,#43409,#43410,
#43411,#43412,#43413,#43414,#43415,#43416,#43417,#43418,#43419,#43420,#43421,
#43422,#43423,#43424,#43425,#43426,#43427,#43428,#43429,#43430,#43431,#43432,
#43433,#43434,#43435,#43436,#43437,#43438,#43439,#43440,#43441,#43442,#43443,
#43444,#43445,#43446,#43447,#43448,#43449,#43450,#43451,#43452,#43453,#43454,
#43455,#43456,#43457,#43458,#43459,#43460,#43461,#43462,#43463,#43464,#43465,
#43466,#43467,#43468,#43469,#43470,#43471,#43472,#43473,#43474,#43475,#43476,
#43477,#43478,#43479,#43480,#43481,#43482,#43483,#43484,#43485,#43486,#43487,
#43488,#43489,#43490,#43491,#43492,#43493,#43494,#43495,#43496,#43497,#43498,
#43499,#43500,#43501,#43502,#43503,#43504,#43505,#43506,#43507,#43508,#43509,
#43510,#43511,#43512,#43513,#43514,#43515,#43516,#43517,#43518,#43519,#43520,
#43521,#43522,#43523,#43524,#43525,#43526,#43527,#43528,#43529,#43530,#43531,
#43532,#43533,#43534,#43535,#43536,#43537,#43538,#43539,#43540,#43541,#43542,
#43543,#43544,#43545,#43546,#43547,#43548,#43549,#43550,#43551,#43552,#43553,
#43554,#43555,#43556,#43557,#43558,#43559,#43560,#43561,#43562,#43563,#43564,
#43565,#43566,#43567,#43568,#43569,#43570,#43571,#43572,#43573,#43574),
 .UNSPECIFIED.,.F.,.F.,(4,2,2,2,2,2,2,2,2,2,2,2,2,2,2,2,2,2,2,2,2,2,2,2,
2,2,2,2,2,2,2,2,2,2,2,2,2,2,2,2,2,2,2,2,2,2,2,2,2,2,2,2,2,2,2,2,2,2,2,2,
2,2,2,2,2,2,2,2,2,2,2,2,2,2,2,2,2,2,2,2,2,2,2,2,2,2,2,2,2,4),(-0.946896429152393,
-0.935842993036999,-0.925667135350627,-0.921543726905473,-0.918490479732483,
-0.915206420376403,-0.909860056159538,-0.878666036446273,-0.869470750707056,
-0.865441875260651,-0.862238073896102,-0.860361933680669,-0.858617532695414,
-0.855961512331845,-0.848392397106035,-0.821390886709287,-0.808596590695199,
-0.804159511298146,-0.801053857304842,-0.797867696746628,-0.793007940488407,
-0.775902769465838,-0.758062947926695,-0.747047635991104,-0.744153776794232,
-0.742343881263691,-0.740525987880981,-0.737594727649649,-0.726004914285177,
-0.711299885231577,-0.691912226532235,-0.686968316133644,-0.683765414514044,
-0.680671158006654,-0.676298327255101,-0.664107267223547,-0.640323824407185,
-0.629373892365169,-0.626419761938131,-0.624596948961982,-0.622791564500296,
-0.619919320312464,-0.609210400316061,-0.577821792500602,-0.570876153331307,
-0.567233633494638,-0.564227199620881,-0.560651367644482,-0.553835042197994,
-0.537625984015797,-0.516897578586285,-0.510574211193969,-0.508085876193291,
-0.506353295857856,-0.50440631757677,-0.500865282665242,-0.483657092636642,
-0.457470251759231,-0.451922636834185,-0.448597667376053,-0.445558219757716,
-0.441531780187535,-0.432038120329208,-0.417288952292675,-0.394954804695401,
-0.391383788395766,-0.389409766908238,-0.387685497361857,-0.385253175592056,
-0.378879091347329,-0.368276097846622,-0.340470326342199,-0.334552944295256,
-0.331120680243266,-0.328405549661733,-0.324729312773739,-0.317370994331972,
-0.288257050103309,-0.276071876122829,-0.273049223859322,-0.271211782379053,
-0.269419243667921,-0.266608375613737,-0.256700962337173,-0.231980086619663,
-0.219672029865783,-0.215192207549624,-0.212109813356784,-0.208940536423249,
-0.204814060717158),.UNSPECIFIED.);
#587=B_SPLINE_CURVE_WITH_KNOTS('',3,(#43580,#43581,#43582,#43583,#43584,
#43585,#43586,#43587,#43588,#43589,#43590,#43591,#43592,#43593,#43594,#43595,
#43596,#43597,#43598,#43599,#43600,#43601,#43602,#43603,#43604,#43605,#43606,
#43607,#43608,#43609,#43610,#43611,#43612,#43613,#43614,#43615,#43616,#43617,
#43618,#43619,#43620,#43621,#43622,#43623,#43624,#43625,#43626,#43627,#43628,
#43629,#43630,#43631,#43632,#43633,#43634,#43635,#43636,#43637,#43638,#43639,
#43640,#43641,#43642,#43643,#43644,#43645,#43646,#43647,#43648,#43649,#43650,
#43651,#43652,#43653,#43654,#43655,#43656,#43657,#43658,#43659,#43660,#43661,
#43662,#43663,#43664,#43665,#43666,#43667,#43668,#43669,#43670,#43671,#43672,
#43673,#43674,#43675,#43676,#43677,#43678,#43679,#43680,#43681,#43682,#43683,
#43684,#43685,#43686,#43687,#43688,#43689,#43690,#43691,#43692,#43693,#43694,
#43695,#43696,#43697,#43698,#43699,#43700,#43701,#43702,#43703,#43704,#43705,
#43706,#43707,#43708,#43709),.UNSPECIFIED.,.F.,.F.,(4,2,2,2,2,2,2,2,2,2,
2,2,2,2,2,2,2,2,2,2,2,2,2,2,2,2,2,2,2,2,2,2,2,2,2,2,2,2,2,2,2,2,2,2,2,2,
2,2,2,2,2,2,2,2,2,2,2,2,2,2,2,2,2,2,4),(-0.537776489716364,-0.534198513703777,
-0.52103880817225,-0.517975708792139,-0.516129398949848,-0.514343229570971,
-0.511564537665593,-0.502044724931717,-0.479685058663251,-0.4650862917619,
-0.46037386413174,-0.457531440826043,-0.454451372287482,-0.450163793312434,
-0.438716588464773,-0.418023263243845,-0.403348000688067,-0.400236089950503,
-0.398379310035032,-0.396600727053666,-0.393859877240925,-0.384765717702204,
-0.364629473374132,-0.347609664737636,-0.342753020577864,-0.339566955288556,
-0.336459904990986,-0.33201816515001,-0.319186530878157,-0.291973217950856,
-0.284587916690818,-0.281954092550411,-0.28021345836489,-0.278329107447126,
-0.27508823695252,-0.256411419357537,-0.231381764138882,-0.225713760365959,
-0.222363627386267,-0.219329715902291,-0.215352458514932,-0.20619229086423,
-0.192271411725321,-0.169374160836966,-0.165316050793369,-0.163264831626422,
-0.161555085887664,-0.159250430226323,-0.153746726175966,-0.145264839539994,
-0.119316067387194,-0.11021533613045,-0.10653845342432,-0.103476209136044,
-0.100276211392115,-0.0953498031450175,-0.0751294366217575,-0.0534188318608297,
-0.0482609969301123,-0.0461655263615747,-0.0444325672152798,-0.042484323128687,
-0.0389390292264036,-0.0146040278328785,-0.000347987605346437),
 .UNSPECIFIED.);
#588=B_SPLINE_CURVE_WITH_KNOTS('',3,(#43710,#43711,#43712,#43713,#43714,
#43715,#43716,#43717,#43718,#43719,#43720,#43721,#43722,#43723,#43724,#43725,
#43726,#43727,#43728,#43729,#43730,#43731,#43732,#43733,#43734,#43735,#43736,
#43737,#43738,#43739,#43740,#43741,#43742,#43743,#43744,#43745,#43746,#43747,
#43748,#43749,#43750,#43751,#43752,#43753,#43754,#43755,#43756,#43757,#43758,
#43759,#43760,#43761,#43762,#43763,#43764,#43765,#43766,#43767,#43768,#43769),
 .UNSPECIFIED.,.F.,.F.,(4,2,2,2,2,2,2,2,2,2,2,2,2,2,2,2,2,2,2,2,2,2,2,2,
2,2,2,2,2,4),(-1.4841886454229,-1.47940069237929,-1.47549041408193,-1.47244534473254,
-1.46959525256703,-1.46641335063947,-1.46157478749194,-1.44411610319639,
-1.42625695166726,-1.41554489031622,-1.41267248613528,-1.4108671759522,
-1.40904449329911,-1.40609063216606,-1.3951333211173,-1.37138855096943,
-1.35920971863448,-1.35483872415153,-1.35174491660862,-1.34854170222424,
-1.34359564740901,-1.3241801964729,-1.30944087487755,-1.29790114529091,
-1.29497302760088,-1.29315588500588,-1.29156242598973,-1.28887205891143,
-1.28100926508778,-1.27966179244307),.UNSPECIFIED.);
#589=B_SPLINE_CURVE_WITH_KNOTS('',3,(#43771,#43772,#43773,#43774,#43775,
#43776,#43777,#43778,#43779,#43780,#43781,#43782,#43783,#43784,#43785,#43786,
#43787,#43788,#43789,#43790,#43791,#43792,#43793,#43794,#43795,#43796,#43797,
#43798,#43799,#43800,#43801,#43802,#43803,#43804,#43805,#43806,#43807,#43808,
#43809,#43810,#43811,#43812,#43813,#43814,#43815,#43816,#43817,#43818,#43819,
#43820),.UNSPECIFIED.,.F.,.F.,(4,2,2,2,2,2,2,2,2,2,2,2,2,2,2,2,2,2,2,2,
2,2,2,2,4),(-0.204814060717158,-0.204166609680667,-0.187215917834386,-0.165816146214042,
-0.157668351142534,-0.154946746566997,-0.153347665623864,-0.15153847245285,
-0.14864814877196,-0.137682112602079,-0.108778642902585,-0.100318642772258,
-0.0964526102798113,-0.0934319757398673,-0.0900228099528017,-0.0840594167740254,
-0.0765548085537383,-0.0573560458344415,-0.0419804058744758,-0.0381441985147878,
-0.0361137299898091,-0.0344178346005035,-0.032094638147647,-0.0264692456979172,
-0.000347917537283366),.UNSPECIFIED.);
#590=B_SPLINE_CURVE_WITH_KNOTS('',3,(#43821,#43822,#43823,#43824,#43825,
#43826,#43827,#43828,#43829,#43830,#43831,#43832,#43833,#43834,#43835,#43836,
#43837,#43838,#43839,#43840,#43841,#43842,#43843,#43844,#43845,#43846,#43847,
#43848,#43849,#43850,#43851,#43852,#43853,#43854,#43855,#43856,#43857,#43858,
#43859,#43860,#43861,#43862,#43863,#43864,#43865,#43866,#43867,#43868,#43869,
#43870,#43871,#43872,#43873,#43874,#43875,#43876,#43877,#43878,#43879,#43880,
#43881,#43882,#43883,#43884,#43885,#43886,#43887,#43888,#43889,#43890,#43891,
#43892,#43893,#43894,#43895,#43896,#43897,#43898,#43899,#43900,#43901,#43902,
#43903,#43904,#43905,#43906,#43907,#43908,#43909,#43910,#43911,#43912,#43913,
#43914,#43915,#43916,#43917,#43918,#43919,#43920,#43921,#43922,#43923,#43924,
#43925,#43926,#43927,#43928,#43929,#43930,#43931,#43932,#43933,#43934,#43935,
#43936,#43937,#43938,#43939,#43940,#43941,#43942,#43943,#43944,#43945,#43946,
#43947,#43948,#43949,#43950),.UNSPECIFIED.,.F.,.F.,(4,2,2,2,2,2,2,2,2,2,
2,2,2,2,2,2,2,2,2,2,2,2,2,2,2,2,2,2,2,2,2,2,2,2,2,2,2,2,2,2,2,2,2,2,2,2,
2,2,2,2,2,2,2,2,2,2,2,2,2,2,2,2,2,2,4),(-1.48422776005814,-1.47313386088049,
-1.46656213293468,-1.46345549907946,-1.46034567045354,-1.45716791219661,
-1.45234645931115,-1.43524767424402,-1.41510713073786,-1.40601550622607,
-1.40327431232798,-1.40149641561978,-1.3996413756044,-1.39653435055193,
-1.38201921101944,-1.36123076358577,-1.34976145861204,-1.34547298846352,
-1.34239416073621,-1.33955416351908,-1.33484897705716,-1.32031076266756,
-1.29787871881556,-1.29140299357479,-1.28684684144652,-1.28470299019188,
-1.28316971808169,-1.28107519164268,-1.2767863312319,-1.25415083719961,
-1.24032371616758,-1.23120356317904,-1.22723401446115,-1.22420262816217,
-1.22085198138127,-1.21517493004383,-1.19025670760812,-1.17147896937039,
-1.16823757337857,-1.16635382954829,-1.16461454636331,-1.16198408125417,
-1.15461732365704,-1.12741318748726,-1.11458880234348,-1.11014964182435,
-1.10704436714992,-1.10386012497405,-1.09900638818332,-1.08203829039826,
-1.06184523177728,-1.05273989569101,-1.04999886908596,-1.04822094435502,
-1.04636572578455,-1.04325814328873,-1.0287220277255,-1.0079481971626,-0.996482490150635,
-0.992194304677656,-0.989115407141688,-0.986275159095789,-0.981569112867491,
-0.967492830556251,-0.946819715823378),.UNSPECIFIED.);
#591=B_SPLINE_CURVE_WITH_KNOTS('',3,(#43955,#43956,#43957,#43958,#43959,
#43960,#43961,#43962,#43963,#43964,#43965,#43966,#43967,#43968,#43969,#43970,
#43971,#43972,#43973,#43974,#43975,#43976,#43977,#43978,#43979,#43980,#43981,
#43982,#43983,#43984,#43985,#43986,#43987,#43988,#43989,#43990,#43991,#43992,
#43993,#43994,#43995,#43996,#43997,#43998,#43999,#44000,#44001,#44002,#44003,
#44004,#44005,#44006,#44007,#44008,#44009,#44010,#44011,#44012,#44013,#44014,
#44015,#44016,#44017,#44018,#44019,#44020,#44021,#44022,#44023,#44024,#44025,
#44026,#44027,#44028,#44029,#44030,#44031,#44032,#44033,#44034,#44035,#44036,
#44037,#44038,#44039,#44040,#44041,#44042,#44043,#44044,#44045,#44046,#44047,
#44048,#44049,#44050,#44051,#44052,#44053,#44054,#44055,#44056,#44057,#44058,
#44059,#44060,#44061,#44062,#44063,#44064,#44065,#44066,#44067,#44068,#44069,
#44070,#44071,#44072,#44073,#44074,#44075,#44076,#44077,#44078,#44079,#44080,
#44081,#44082,#44083,#44084,#44085,#44086,#44087,#44088,#44089,#44090,#44091,
#44092,#44093,#44094,#44095,#44096,#44097,#44098,#44099,#44100,#44101,#44102,
#44103,#44104,#44105,#44106,#44107,#44108,#44109,#44110,#44111,#44112,#44113,
#44114,#44115,#44116,#44117,#44118,#44119,#44120,#44121,#44122,#44123,#44124,
#44125,#44126,#44127,#44128,#44129,#44130,#44131,#44132,#44133,#44134),
 .UNSPECIFIED.,.F.,.F.,(4,2,2,2,2,2,2,2,2,2,2,2,2,2,2,2,2,2,2,2,2,2,2,2,
2,2,2,2,2,2,2,2,2,2,2,2,2,2,2,2,2,2,2,2,2,2,2,2,2,2,2,2,2,2,2,2,2,2,2,2,
2,2,2,2,2,2,2,2,2,2,2,2,2,2,2,2,2,2,2,2,2,2,2,2,2,2,2,2,2,4),(-1.27980850632928,
-1.27760533835833,-1.27202400355896,-1.24611093649757,-1.22869009499228,
-1.22513691135587,-1.22318718483132,-1.22145497831031,-1.21936252476966,
-1.21422187449833,-1.18980813348732,-1.17555817832044,-1.16884423297993,
-1.16528746138688,-1.16227985960788,-1.1586146109491,-1.15155555990615,
-1.12514953797021,-1.11488751227358,-1.10864533370155,-1.10623098369459,
-1.10450887174509,-1.10252454383414,-1.09890703173291,-1.07714016506507,
-1.0576408461584,-1.05100093532538,-1.04745835761557,-1.04445023580903,
-1.04076869989509,-1.03338403181038,-1.00725094959236,-0.997057566574456,
-0.990842310947649,-0.98843176089814,-0.986710165402452,-0.984723815926787,
-0.981096858518842,-0.959476954769453,-0.9443465784611,-0.934704038503723,
-0.930655288161407,-0.927612124994902,-0.924295706468068,-0.918793080749838,
-0.892200275205504,-0.88016266695316,-0.873264695418516,-0.870762543215849,
-0.869027460866021,-0.867085875578691,-0.863572197940217,-0.840357004955942,
-0.826083239451038,-0.816778620106407,-0.81277975525902,-0.80974325775482,
-0.806403958164091,-0.800788746354681,-0.775187405426704,-0.757119737238613,
-0.75379055254264,-0.75188756155927,-0.750156351888907,-0.747992531102661,
-0.742373700943728,-0.733308050256024,-0.703048005436398,-0.697171720781083,
-0.69374756147312,-0.691030517810713,-0.687340693368818,-0.679910401741977,
-0.669740234184557,-0.65590759122521,-0.640288952476128,-0.636439345855426,
-0.634405829272063,-0.632709976205251,-0.630390158255074,-0.62478842292603,
-0.616081811044127,-0.588534007849584,-0.580572312185066,-0.576789239067628,
-0.573775365067762,-0.570311301098227,-0.564074295972497,-0.556100784075032,
-0.537776489716364),.UNSPECIFIED.);
#592=B_SPLINE_CURVE_WITH_KNOTS('',3,(#44135,#44136,#44137,#44138,#44139,
#44140,#44141,#44142,#44143,#44144,#44145,#44146,#44147,#44148,#44149,#44150,
#44151,#44152,#44153,#44154,#44155,#44156,#44157,#44158,#44159,#44160,#44161,
#44162,#44163,#44164,#44165,#44166,#44167,#44168,#44169,#44170,#44171,#44172,
#44173,#44174,#44175,#44176,#44177,#44178,#44179,#44180,#44181,#44182,#44183,
#44184,#44185,#44186,#44187,#44188,#44189,#44190,#44191,#44192,#44193,#44194,
#44195,#44196,#44197,#44198,#44199,#44200,#44201,#44202,#44203,#44204,#44205,
#44206,#44207,#44208,#44209,#44210,#44211,#44212,#44213,#44214,#44215,#44216,
#44217,#44218,#44219,#44220,#44221,#44222,#44223,#44224,#44225,#44226,#44227,
#44228,#44229,#44230,#44231,#44232,#44233,#44234,#44235,#44236,#44237,#44238,
#44239,#44240,#44241,#44242,#44243,#44244,#44245,#44246,#44247,#44248,#44249,
#44250,#44251,#44252,#44253,#44254,#44255,#44256,#44257,#44258,#44259,#44260,
#44261,#44262,#44263,#44264,#44265,#44266,#44267,#44268,#44269,#44270,#44271,
#44272,#44273,#44274,#44275,#44276,#44277,#44278,#44279,#44280,#44281,#44282,
#44283,#44284,#44285,#44286,#44287,#44288,#44289,#44290,#44291,#44292,#44293,
#44294,#44295,#44296,#44297,#44298,#44299,#44300,#44301,#44302,#44303,#44304,
#44305,#44306,#44307,#44308,#44309,#44310,#44311,#44312,#44313,#44314,#44315,
#44316,#44317,#44318,#44319,#44320,#44321,#44322),.UNSPECIFIED.,.F.,.F.,
(4,2,2,2,2,2,2,2,2,2,2,2,2,2,2,2,2,2,2,2,2,2,2,2,2,2,2,2,2,2,2,2,2,2,2,
2,2,2,2,2,2,2,2,2,2,2,2,2,2,2,2,2,2,2,2,2,2,2,2,2,2,2,2,2,2,2,2,2,2,2,2,
2,2,2,2,2,2,2,2,2,2,2,2,2,2,2,2,2,2,2,2,2,2,4),(-0.946819715823378,-0.944676539999871,
-0.935076828038626,-0.932292076290245,-0.930505316705579,-0.928889090752232,
-0.926071942353666,-0.916881483189701,-0.891504469725059,-0.878998296090072,
-0.874592534986822,-0.871493295580457,-0.868676647070157,-0.864107604048417,
-0.850872411149378,-0.827100572834544,-0.817341449412502,-0.814543299147451,
-0.81275380795323,-0.810913986593012,-0.807878394495823,-0.795293230791608,
-0.772939415035423,-0.764898993792395,-0.758623664436144,-0.755153180680186,
-0.752141708206595,-0.748372244106774,-0.742302342198529,-0.727623535650372,
-0.701102900562991,-0.697522563918068,-0.695546785226429,-0.693823469602608,
-0.691395878611511,-0.685053685381215,-0.674532593703952,-0.647063413207413,
-0.640893185733333,-0.637408414405273,-0.634398072474785,-0.630647714502164,
-0.622869592828021,-0.612004485384715,-0.599054768639518,-0.583764540586666,
-0.579933276122199,-0.577904173494799,-0.576208601054083,-0.573884764731901,
-0.56825267410162,-0.559474394781421,-0.531398598766086,-0.523864120927975,
-0.520156844101676,-0.517149029385311,-0.513631118177445,-0.507113610239251,
-0.49864538529204,-0.473157169991846,-0.464060753103059,-0.46125124283949,
-0.459636384436826,-0.45784789805943,-0.45505513997049,-0.445360404148334,
-0.421972869851715,-0.408371971523109,-0.403771542685049,-0.400949395119775,
-0.397854853428461,-0.393476856731378,-0.381231570422997,-0.357183016218841,
-0.346545791215524,-0.34360951195502,-0.341790832733748,-0.339982494335379,
-0.337094783929389,-0.326158788437954,-0.294858651238629,-0.28802652325261,
-0.284407072230248,-0.281401714403851,-0.27780583378705,-0.270880043155716,
-0.238549072877998,-0.22863218022941,-0.225743671118562,-0.224113771967344,
-0.222340105173282,-0.219621574969192,-0.210758836892982,-0.204933271960559),
 .UNSPECIFIED.);
#593=B_SPLINE_CURVE_WITH_KNOTS('',3,(#44328,#44329,#44330,#44331,#44332,
#44333,#44334,#44335),.UNSPECIFIED.,.F.,.F.,(4,1,1,1,1,4),(53.4070764126742,
54.1848189434555,55.1822707432196,56.1797225429836,57.1771743427477,57.9574404719481),
 .UNSPECIFIED.);
#594=B_SPLINE_CURVE_WITH_KNOTS('',3,(#44336,#44337,#44338,#44339,#44340,
#44341,#44342,#44343,#44344,#44345,#44346,#44347,#44348,#44349,#44350,#44351,
#44352,#44353,#44354,#44355,#44356,#44357,#44358,#44359,#44360,#44361,#44362,
#44363,#44364,#44365,#44366,#44367,#44368,#44369,#44370,#44371,#44372,#44373,
#44374,#44375,#44376,#44377,#44378,#44379,#44380,#44381,#44382,#44383,#44384,
#44385,#44386,#44387,#44388,#44389),.UNSPECIFIED.,.F.,.F.,(4,2,2,2,2,2,
2,2,2,2,2,2,2,2,2,2,2,2,2,2,2,2,2,2,2,2,4),(-1.48420160976377,-1.46442302160507,
-1.46177965705685,-1.45945977695506,-1.45776409714973,-1.45573100399282,
-1.45188281404087,-1.43516050495058,-1.4169622897526,-1.40625631497045,
-1.40205626670841,-1.39899079202854,-1.39573420029934,-1.39052476860652,
-1.36183780261404,-1.35084074448908,-1.34431803830977,-1.34186519269882,
-1.34013776811861,-1.33817340543135,-1.33464796804164,-1.31190142067794,
-1.29738895903596,-1.28798870265809,-1.28397574080648,-1.28093759263062,
-1.27980850632928),.UNSPECIFIED.);
#595=B_SPLINE_CURVE_WITH_KNOTS('',3,(#44391,#44392,#44393,#44394,#44395,
#44396,#44397,#44398,#44399,#44400,#44401,#44402,#44403,#44404,#44405,#44406,
#44407,#44408,#44409,#44410,#44411,#44412,#44413,#44414,#44415,#44416,#44417,
#44418,#44419,#44420,#44421,#44422,#44423,#44424,#44425,#44426,#44427,#44428,
#44429,#44430,#44431,#44432,#44433,#44434,#44435,#44436),.UNSPECIFIED.,
 .F.,.F.,(4,2,2,2,2,2,2,2,2,2,2,2,2,2,2,2,2,2,2,2,2,2,4),(-0.204933271960559,
-0.193610744071927,-0.173609752213875,-0.168619346997917,-0.165407512488029,
-0.162319690211239,-0.157981592593195,-0.146094999274754,-0.123657667876321,
-0.111154201353178,-0.108114289236958,-0.106273326207953,-0.104484102155178,
-0.101688499279261,-0.091962803369415,-0.0683916817828056,-0.0549692722591983,
-0.0503840172232408,-0.0475641962116398,-0.0444667589965546,-0.0400740093147337,
-0.0276969669859353,-0.000348048528551123),.UNSPECIFIED.);
#596=B_SPLINE_CURVE_WITH_KNOTS('',3,(#44437,#44438,#44439,#44440,#44441,
#44442,#44443,#44444,#44445,#44446,#44447,#44448,#44449,#44450,#44451,#44452,
#44453,#44454,#44455,#44456,#44457,#44458,#44459,#44460,#44461,#44462,#44463,
#44464,#44465,#44466,#44467,#44468,#44469,#44470,#44471,#44472,#44473,#44474,
#44475,#44476,#44477,#44478,#44479,#44480,#44481,#44482,#44483,#44484,#44485,
#44486,#44487,#44488,#44489,#44490,#44491,#44492,#44493,#44494,#44495,#44496,
#44497,#44498,#44499,#44500,#44501,#44502,#44503,#44504,#44505,#44506,#44507,
#44508,#44509,#44510,#44511,#44512,#44513,#44514,#44515,#44516,#44517,#44518,
#44519,#44520,#44521,#44522,#44523,#44524,#44525,#44526,#44527,#44528,#44529,
#44530,#44531,#44532,#44533,#44534,#44535,#44536,#44537,#44538,#44539,#44540,
#44541,#44542,#44543,#44544,#44545,#44546,#44547,#44548,#44549,#44550,#44551,
#44552,#44553,#44554,#44555,#44556,#44557,#44558,#44559,#44560,#44561,#44562,
#44563,#44564,#44565,#44566,#44567,#44568,#44569,#44570),.UNSPECIFIED.,
 .F.,.F.,(4,2,2,2,2,2,2,2,2,2,2,2,2,2,2,2,2,2,2,2,2,2,2,2,2,2,2,2,2,2,2,
2,2,2,2,2,2,2,2,2,2,2,2,2,2,2,2,2,2,2,2,2,2,2,2,2,2,2,2,2,2,2,2,2,2,2,4),
(-1.48430166607142,-1.47889192298633,-1.47529624805926,-1.4735682429476,
-1.47191690410003,-1.46995830580524,-1.4664577751231,-1.45041785091773,
-1.43284714499154,-1.42065567768791,-1.41628357434739,-1.41318989829041,
-1.40998764063816,-1.40504485665597,-1.38564972040756,-1.3709383577164,
-1.35934261495105,-1.35641116887526,-1.35459347556701,-1.35300080675906,
-1.35031405421988,-1.34248172221607,-1.31576207622309,-1.3030162681603,
-1.29858488322316,-1.29548075354232,-1.29229410238292,-1.28742943295573,
-1.27013735491797,-1.24455416434874,-1.23982938758071,-1.23765512330591,
-1.23595297366096,-1.23379673766841,-1.22917327113744,-1.20686195338864,
-1.19314628642084,-1.18407187511922,-1.18010879638047,-1.17707767033437,
-1.17372264365296,-1.1680262731,-1.14332349154197,-1.12468305174694,-1.12125810824455,
-1.1193353868194,-1.11761352652868,-1.11508512112894,-1.10848631069315,
-1.08800488269144,-1.07495625118098,-1.06616600206954,-1.0622469985798,
-1.05922083654373,-1.05584218653558,-1.05002996954381,-1.02995476766433,
-1.01362235263153,-1.00802780286182,-1.00393075188198,-1.00187240562504,
-1.00016424924206,-0.99791134675134,-0.992793649928703,-0.962952904346267,
-0.949751005501392,-0.946940986422606),.UNSPECIFIED.);
#597=B_SPLINE_CURVE_WITH_KNOTS('',3,(#44576,#44577,#44578,#44579,#44580,
#44581,#44582,#44583,#44584,#44585,#44586,#44587,#44588,#44589,#44590,#44591,
#44592,#44593,#44594,#44595,#44596,#44597,#44598,#44599,#44600,#44601,#44602,
#44603,#44604,#44605,#44606,#44607,#44608,#44609,#44610,#44611,#44612,#44613,
#44614,#44615,#44616,#44617,#44618,#44619,#44620,#44621,#44622,#44623,#44624,
#44625,#44626,#44627,#44628,#44629,#44630,#44631,#44632,#44633,#44634,#44635,
#44636,#44637,#44638,#44639,#44640,#44641,#44642,#44643,#44644,#44645,#44646,
#44647,#44648,#44649,#44650,#44651,#44652,#44653,#44654,#44655,#44656,#44657,
#44658,#44659,#44660,#44661,#44662,#44663,#44664,#44665,#44666,#44667,#44668,
#44669,#44670,#44671,#44672,#44673,#44674,#44675,#44676,#44677,#44678,#44679,
#44680,#44681,#44682,#44683,#44684,#44685,#44686,#44687,#44688,#44689,#44690,
#44691,#44692,#44693,#44694,#44695,#44696,#44697,#44698,#44699,#44700,#44701,
#44702,#44703,#44704,#44705,#44706,#44707),.UNSPECIFIED.,.F.,.F.,(4,2,2,
2,2,2,2,2,2,2,2,2,2,2,2,2,2,2,2,2,2,2,2,2,2,2,2,2,2,2,2,2,2,2,2,2,2,2,2,
2,2,2,2,2,2,2,2,2,2,2,2,2,2,2,2,2,2,2,2,2,2,2,2,2,2,4),(-0.537894309400619,
-0.533213023061253,-0.530146767499444,-0.528299718798876,-0.526513942106161,
-0.523737506313799,-0.514245033064368,-0.492040195169155,-0.477283299942744,
-0.472556031510676,-0.469710903305401,-0.4666325925218,-0.462356285683449,
-0.451003884271354,-0.430660626675176,-0.41552074734285,-0.412403153331535,
-0.410545094255675,-0.408767235546628,-0.406030368929641,-0.396980563888222,
-0.377059427124444,-0.359785895119985,-0.354920900350778,-0.351733055542335,
-0.348626984053177,-0.344191413696158,-0.331421255928584,-0.304586585746469,
-0.296839343142064,-0.29416142786641,-0.292569704049276,-0.290748153301413,
-0.287801726779752,-0.275975268433924,-0.261471724955338,-0.242132862770731,
-0.23719417371081,-0.233991537569654,-0.230895255952026,-0.226515573942646,
-0.214270844514413,-0.190238637442558,-0.179571531704665,-0.176632253726846,
-0.174812200456691,-0.173002919717492,-0.1701142396868,-0.159181724509775,
-0.127151370184006,-0.121302249952503,-0.117592966019391,-0.11458328867609,
-0.111062890349529,-0.104539639292293,-0.0875154561512914,-0.066232950840203,
-0.0605865857542987,-0.0584200588427744,-0.0566881374008508,-0.0547862963146238,
-0.051463008905974,-0.0335559941265448,-0.00733093514828557,-0.0031099699046096,
-0.00036640004475231),.UNSPECIFIED.);
#598=B_SPLINE_CURVE_WITH_KNOTS('',3,(#44708,#44709,#44710,#44711,#44712,
#44713),.UNSPECIFIED.,.F.,.F.,(4,1,1,4),(57.9574404719481,58.1746261425118,
59.1720779422758,59.690260418206),.UNSPECIFIED.);
#599=B_SPLINE_CURVE_WITH_KNOTS('',3,(#44714,#44715,#44716,#44717,#44718,
#44719,#44720,#44721,#44722,#44723,#44724,#44725,#44726,#44727,#44728,#44729,
#44730,#44731,#44732,#44733,#44734,#44735,#44736,#44737,#44738,#44739,#44740,
#44741,#44742,#44743,#44744,#44745,#44746,#44747,#44748,#44749,#44750,#44751,
#44752,#44753,#44754,#44755,#44756,#44757,#44758,#44759,#44760,#44761,#44762,
#44763,#44764,#44765,#44766,#44767,#44768,#44769,#44770,#44771,#44772,#44773,
#44774,#44775,#44776,#44777,#44778,#44779,#44780,#44781,#44782,#44783,#44784,
#44785,#44786,#44787,#44788,#44789,#44790,#44791,#44792,#44793,#44794,#44795,
#44796,#44797,#44798,#44799,#44800,#44801,#44802,#44803,#44804,#44805,#44806,
#44807,#44808,#44809,#44810,#44811,#44812,#44813,#44814,#44815,#44816,#44817,
#44818,#44819,#44820,#44821,#44822,#44823,#44824,#44825,#44826,#44827,#44828,
#44829,#44830,#44831,#44832,#44833,#44834,#44835,#44836,#44837,#44838,#44839,
#44840,#44841,#44842,#44843,#44844,#44845,#44846,#44847,#44848,#44849,#44850,
#44851,#44852,#44853,#44854,#44855,#44856,#44857,#44858,#44859,#44860,#44861,
#44862,#44863,#44864,#44865,#44866,#44867,#44868,#44869,#44870,#44871,#44872,
#44873,#44874,#44875,#44876,#44877,#44878,#44879,#44880,#44881,#44882,#44883,
#44884,#44885,#44886,#44887,#44888,#44889,#44890,#44891,#44892,#44893,#44894,
#44895,#44896,#44897,#44898,#44899),.UNSPECIFIED.,.F.,.F.,(4,2,2,2,2,2,
2,2,2,2,2,2,2,2,2,2,2,2,2,2,2,2,2,2,2,2,2,2,2,2,2,2,2,2,2,2,2,2,2,2,2,2,
2,2,2,2,2,2,2,2,2,2,2,2,2,2,2,2,2,2,2,2,2,2,2,2,2,2,2,2,2,2,2,2,2,2,2,2,
2,2,2,2,2,2,2,2,2,2,2,2,2,2,4),(-0.946940986422606,-0.945273129429978,-0.942160311314846,
-0.938984453190988,-0.934175772564391,-0.918248594807293,-0.897127199870089,
-0.887835764106582,-0.885077458287909,-0.883295787308269,-0.881444785116189,
-0.878358208390088,-0.864596914267385,-0.843204236032207,-0.835314447087802,
-0.829125524487421,-0.825671593094014,-0.822657541866112,-0.818862318905677,
-0.810826146230518,-0.78335051547628,-0.774650674287677,-0.769052473036572,
-0.766733531961685,-0.765038182655621,-0.763005133583983,-0.759156303535479,
-0.742523950964127,-0.716361306456947,-0.71081108452574,-0.707485634065531,
-0.704446417435343,-0.70042128422846,-0.690936090814075,-0.676208217414093,
-0.653835422583673,-0.65026833950149,-0.648295193675655,-0.646570733017929,
-0.644136839121935,-0.637751084756656,-0.627117411670784,-0.599182957370083,
-0.593362861750196,-0.589951202174112,-0.586931213099849,-0.583069957631787,
-0.574638569714413,-0.562395052833682,-0.53613807859232,-0.532507612759943,
-0.530520765212932,-0.528799765121625,-0.526391624163697,-0.520191088440316,
-0.510035419802304,-0.484044541654161,-0.476546816441148,-0.472845431415462,
-0.469837085995646,-0.46631252417331,-0.459763982547263,-0.44175462194786,
-0.418645314570392,-0.414830573686059,-0.412804561520743,-0.411263783971376,
-0.409032986596193,-0.403981540457007,-0.396492341688873,-0.367777930730709,
-0.359248162891342,-0.355370748663632,-0.352348935800174,-0.348946461336781,
-0.343016513313748,-0.335568494788288,-0.316665470627747,-0.300913413829313,
-0.297055588947873,-0.295020588922136,-0.293325397822012,-0.291009091073461,
-0.285428307338621,-0.276769629828269,-0.249570163727085,-0.241320447274573,
-0.237489117061739,-0.234471782714412,-0.231041172390308,-0.224970569268392,
-0.217283494883199,-0.204898626771331),.UNSPECIFIED.);
#600=B_SPLINE_CURVE_WITH_KNOTS('',3,(#44904,#44905,#44906,#44907,#44908,
#44909,#44910,#44911,#44912,#44913,#44914,#44915,#44916,#44917,#44918,#44919,
#44920,#44921,#44922,#44923,#44924,#44925,#44926,#44927,#44928,#44929,#44930,
#44931,#44932,#44933,#44934,#44935,#44936,#44937,#44938,#44939,#44940,#44941,
#44942,#44943,#44944,#44945,#44946,#44947,#44948,#44949,#44950,#44951,#44952,
#44953,#44954,#44955,#44956,#44957,#44958,#44959,#44960,#44961,#44962,#44963,
#44964,#44965,#44966,#44967,#44968,#44969,#44970,#44971,#44972,#44973,#44974,
#44975,#44976,#44977,#44978,#44979,#44980,#44981,#44982,#44983,#44984,#44985,
#44986,#44987,#44988,#44989,#44990,#44991,#44992,#44993,#44994,#44995,#44996,
#44997,#44998,#44999,#45000,#45001,#45002,#45003,#45004,#45005,#45006,#45007,
#45008,#45009,#45010,#45011,#45012,#45013,#45014,#45015,#45016,#45017,#45018,
#45019,#45020,#45021,#45022,#45023,#45024,#45025,#45026,#45027,#45028,#45029,
#45030,#45031,#45032,#45033,#45034,#45035,#45036,#45037,#45038,#45039,#45040,
#45041,#45042,#45043,#45044,#45045,#45046,#45047,#45048,#45049,#45050,#45051,
#45052,#45053,#45054,#45055,#45056,#45057,#45058,#45059,#45060,#45061,#45062,
#45063,#45064,#45065,#45066,#45067,#45068,#45069,#45070,#45071,#45072,#45073,
#45074,#45075,#45076,#45077,#45078,#45079,#45080,#45081),.UNSPECIFIED.,
 .F.,.F.,(4,2,2,2,2,2,2,2,2,2,2,2,2,2,2,2,2,2,2,2,2,2,2,2,2,2,2,2,2,2,2,
2,2,2,2,2,2,2,2,2,2,2,2,2,2,2,2,2,2,2,2,2,2,2,2,2,2,2,2,2,2,2,2,2,2,2,2,
2,2,2,2,2,2,2,2,2,2,2,2,2,2,2,2,2,2,2,2,2,4),(-1.27993629200949,-1.25838528934253,
-1.24046364626388,-1.23714001774422,-1.23523842844544,-1.23350717076722,
-1.23134194145366,-1.22570290877557,-1.20443469292664,-1.19109793829111,
-1.18218348531449,-1.17824477603145,-1.17521611578875,-1.17184751934819,
-1.16608598933105,-1.13689143543466,-1.12691592614631,-1.12078703885223,
-1.11838894770219,-1.11666911667411,-1.11467618616052,-1.11101845011242,
-1.09003583687508,-1.07452246129919,-1.06780472055512,-1.06231488789013,
-1.05900103536451,-1.05595695983437,-1.05197226829816,-1.0431911546825,
-1.01685093444682,-1.00831211758722,-1.00278388854634,-1.00047540770876,
-0.998765398195904,-0.996716971036565,-0.992672705825595,-0.969777975801975,
-0.955862542643372,-0.946704510215881,-0.942727833543562,-0.939694163111128,
-0.93634408901286,-0.930675744374352,-0.905625657612196,-0.887022359456591,
-0.883738917736678,-0.881845619516375,-0.880109790718354,-0.877502229657632,
-0.870321639209526,-0.850312656505014,-0.831035632592875,-0.82614456984875,
-0.8229516795489,-0.819884988601071,-0.816189006419218,-0.806962714754732,
-0.779555801492472,-0.772049316339871,-0.766989871910192,-0.764757372632763,
-0.763216078827397,-0.761190190844976,-0.757377645968129,-0.742551582456069,
-0.713866195979949,-0.70865222442012,-0.705394378095877,-0.702328759868338,
-0.698130193527889,-0.687397720548324,-0.669151973577296,-0.652464714678316,
-0.648614527989473,-0.646580810570882,-0.644884865664761,-0.642565013702663,
-0.636963594497172,-0.628257948666415,-0.600719074393753,-0.59274849249036,
-0.588963763656592,-0.585949614305228,-0.582486369257423,-0.576254132829627,
-0.568289060658438,-0.546441838554268,-0.537894309400619),.UNSPECIFIED.);
#601=B_SPLINE_CURVE_WITH_KNOTS('',3,(#45083,#45084,#45085,#45086,#45087,
#45088,#45089,#45090,#45091,#45092,#45093,#45094,#45095,#45096,#45097,#45098,
#45099,#45100,#45101,#45102,#45103,#45104,#45105,#45106,#45107,#45108,#45109,
#45110,#45111,#45112,#45113,#45114,#45115,#45116,#45117,#45118,#45119,#45120,
#45121,#45122,#45123,#45124,#45125,#45126,#45127,#45128,#45129,#45130,#45131,
#45132,#45133,#45134,#45135,#45136),.UNSPECIFIED.,.F.,.F.,(4,2,2,2,2,2,
2,2,2,2,2,2,2,2,2,2,2,2,2,2,2,2,2,2,2,2,4),(-0.204898626771331,-0.198446153233599,
-0.183080360398766,-0.17924463951519,-0.177214273588691,-0.175518362895264,
-0.173195011964068,-0.16756861108729,-0.158804659985722,-0.130843744826638,
-0.123210654704607,-0.119485237308615,-0.116475728362113,-0.112970479982118,
-0.106521256637508,-0.0833930600211793,-0.065258886004377,-0.0614304673950918,
-0.0594016131898563,-0.05770542227049,-0.0553796452063263,-0.049737640895587,
-0.040937586280751,-0.0142283439117813,-0.00595310739962801,-0.00265801665500284,
-0.000347696305143031),.UNSPECIFIED.);
#602=B_SPLINE_CURVE_WITH_KNOTS('',3,(#45137,#45138,#45139,#45140,#45141,
#45142,#45143,#45144,#45145,#45146,#45147,#45148,#45149,#45150,#45151,#45152,
#45153,#45154,#45155,#45156,#45157,#45158,#45159,#45160,#45161,#45162,#45163,
#45164,#45165,#45166,#45167,#45168,#45169,#45170,#45171,#45172,#45173,#45174,
#45175,#45176,#45177,#45178,#45179,#45180,#45181,#45182,#45183,#45184,#45185,
#45186,#45187,#45188,#45189,#45190,#45191,#45192,#45193,#45194,#45195,#45196,
#45197,#45198,#45199,#45200,#45201,#45202,#45203,#45204,#45205,#45206,#45207,
#45208,#45209,#45210,#45211,#45212,#45213,#45214,#45215,#45216,#45217,#45218,
#45219,#45220,#45221,#45222,#45223,#45224,#45225,#45226,#45227,#45228,#45229,
#45230,#45231,#45232,#45233,#45234,#45235,#45236,#45237,#45238,#45239,#45240,
#45241,#45242,#45243,#45244,#45245,#45246,#45247,#45248,#45249,#45250,#45251,
#45252,#45253,#45254,#45255,#45256,#45257,#45258,#45259,#45260),
 .UNSPECIFIED.,.F.,.F.,(4,3,3,3,3,3,3,3,3,3,3,3,3,3,3,3,3,3,3,3,3,3,3,3,
3,3,3,3,3,3,3,3,3,3,3,3,3,3,3,3,3,4),(65.9734457253857,66.0990314776703,
66.2241716615538,66.3499801980389,66.4757887345241,66.6004702094946,66.719981694683,
66.8393732042342,66.95869761317,67.078007680618,67.1974393886703,67.3169434209799,
67.4366659695107,67.4732405342882,67.5979220092587,67.7174335580785,67.8368251306602,
67.9561496019118,68.0754597308459,68.1948914987132,68.3143955899358,68.4341181954617,
68.4706923340523,68.5953738090228,68.7148854589353,68.8342771334435,68.9536017072489,
69.0729119391582,69.1923438098461,69.3118480039161,69.4315707112718,69.4681441338164,
69.5928256087869,69.7123367977167,69.8317280117834,69.951052126569,70.070361901761,
70.18979332251,70.3092970700651,70.4290193404745,70.4655959335804,70.525019783164),
 .UNSPECIFIED.);
#603=B_SPLINE_CURVE_WITH_KNOTS('',3,(#45266,#45267,#45268,#45269,#45270,
#45271,#45272,#45273,#45274,#45275,#45276,#45277,#45278,#45279,#45280,#45281,
#45282,#45283,#45284,#45285,#45286,#45287,#45288,#45289,#45290,#45291,#45292,
#45293,#45294,#45295,#45296,#45297,#45298,#45299,#45300,#45301,#45302,#45303,
#45304,#45305,#45306,#45307,#45308,#45309,#45310,#45311,#45312,#45313,#45314,
#45315,#45316,#45317,#45318,#45319,#45320,#45321,#45322,#45323,#45324,#45325,
#45326,#45327,#45328,#45329,#45330,#45331,#45332,#45333,#45334,#45335,#45336,
#45337,#45338,#45339,#45340,#45341,#45342,#45343,#45344,#45345,#45346,#45347,
#45348,#45349,#45350,#45351,#45352,#45353,#45354,#45355,#45356,#45357,#45358,
#45359,#45360,#45361,#45362,#45363,#45364,#45365,#45366,#45367,#45368,#45369,
#45370,#45371,#45372,#45373,#45374,#45375,#45376,#45377,#45378,#45379,#45380,
#45381,#45382,#45383,#45384,#45385,#45386,#45387,#45388,#45389),
 .UNSPECIFIED.,.F.,.F.,(4,3,3,3,3,3,3,3,3,3,3,3,3,3,3,3,3,3,3,3,3,3,3,3,
3,3,3,3,3,3,3,3,3,3,3,3,3,3,3,3,3,4),(72.2566310330981,72.3746000738282,
72.4924200944505,72.6101467448915,72.7278354973385,72.8456247185995,72.9634700790888,
73.0815331296642,73.1364031389728,73.2610846139433,73.3806207054347,73.5000366324537,
73.6193852251617,73.7387191975766,73.858174224532,73.977701261838,74.0974461224598,
74.1338549387369,74.2585364137074,74.3780718711446,74.497487656099,74.616836592913,
74.7361713904628,74.8556279384821,74.9751569026416,75.0949042603196,75.131306738501,
75.2559882134715,75.3753544000741,75.4946006959659,75.6137802495987,75.7329460935138,
75.8522355715341,75.9715983635803,76.0911825638886,76.128758538265,76.2486946695722,
76.3684426008254,76.4880621388945,76.6076039822474,76.7271699042361,76.8075006878804),
 .UNSPECIFIED.);
#604=B_SPLINE_CURVE_WITH_KNOTS('',3,(#45390,#45391,#45392,#45393,#45394,
#45395,#45396,#45397,#45398,#45399,#45400,#45401,#45402,#45403,#45404,#45405,
#45406,#45407,#45408,#45409,#45410,#45411,#45412,#45413,#45414,#45415,#45416,
#45417,#45418,#45419,#45420,#45421,#45422,#45423,#45424,#45425,#45426,#45427,
#45428,#45429,#45430,#45431,#45432,#45433,#45434,#45435,#45436,#45437,#45438,
#45439,#45440,#45441,#45442,#45443,#45444,#45445,#45446,#45447),
 .UNSPECIFIED.,.F.,.F.,(4,2,2,2,2,2,2,2,2,2,2,2,2,2,2,2,2,2,2,2,2,2,2,2,
2,2,2,2,4),(-1.48433766817237,-1.47563063748376,-1.47332014712585,-1.47161845788704,
-1.46993229781918,-1.46790905738358,-1.46410793341904,-1.44500910995515,
-1.4287553840491,-1.41830408844958,-1.41414242371745,-1.4110823356441,-1.40781066287085,
-1.4025296177577,-1.37431356910048,-1.36311234463794,-1.35651410134926,
-1.35405056104863,-1.35232111084505,-1.35036111278482,-1.34685611593369,
-1.32392877667923,-1.30951371641234,-1.30015284979804,-1.29614588730459,
-1.29310863275993,-1.28977378438033,-1.28417923565751,-1.27993629200949),
 .UNSPECIFIED.);
#605=B_SPLINE_CURVE_WITH_KNOTS('',3,(#45449,#45450,#45451,#45452,#45453,
#45454,#45455,#45456,#45457,#45458,#45459,#45460,#45461,#45462,#45463,#45464,
#45465,#45466,#45467,#45468,#45469,#45470,#45471,#45472,#45473,#45474,#45475,
#45476,#45477,#45478,#45479,#45480,#45481,#45482,#45483,#45484,#45485,#45486,
#45487,#45488,#45489,#45490,#45491,#45492,#45493,#45494),.UNSPECIFIED.,
 .F.,.F.,(4,3,3,3,3,3,3,3,3,3,3,3,3,3,3,4),(70.525019783164,70.6446193576465,
70.7640700377342,70.8834247914381,71.0027364317802,71.1221489412945,71.2416079535534,
71.3613062955418,71.4630477333445,71.5810393630235,71.6988537785785,71.8165468469208,
71.9342244217906,72.05188624816,72.1696834755421,72.2566308475935),
 .UNSPECIFIED.);
#606=B_SPLINE_CURVE_WITH_KNOTS('',3,(#45495,#45496,#45497,#45498,#45499,
#45500,#45501,#45502,#45503),.UNSPECIFIED.,.F.,.F.,(4,1,1,1,1,1,4),(72.2566310325653,
72.4604995331086,73.4579513328726,74.4554031326367,75.4528549324008,76.4503067321649,
76.8085816652527),.UNSPECIFIED.);
#607=B_SPLINE_CURVE_WITH_KNOTS('',3,(#45509,#45510,#45511,#45512,#45513,
#45514,#45515,#45516,#45517,#45518,#45519,#45520,#45521,#45522,#45523,#45524,
#45525,#45526,#45527,#45528,#45529,#45530,#45531,#45532,#45533,#45534,#45535,
#45536,#45537,#45538,#45539,#45540,#45541,#45542,#45543,#45544,#45545,#45546,
#45547,#45548,#45549,#45550,#45551,#45552,#45553,#45554,#45555,#45556,#45557,
#45558,#45559,#45560,#45561,#45562,#45563,#45564,#45565,#45566),
 .UNSPECIFIED.,.F.,.F.,(4,3,3,3,3,3,3,3,3,3,3,3,3,3,3,3,3,3,3,4),(-4.09202352044871,
-3.98980719905628,-3.87618720905945,-3.76277252994605,-3.64947230427638,
-3.53624194244134,-3.42303695779458,-3.3097318571573,-3.19637810523371,
-3.08281265733122,-2.99235539929221,-2.87748405249459,-2.76546218494948,
-2.65354723694333,-2.54169248379193,-2.42461551907177,-2.31267073081522,
-2.20066051905403,-2.08847033816625,-2.07338462491128),.UNSPECIFIED.);
#608=B_SPLINE_CURVE_WITH_KNOTS('',3,(#45569,#45570,#45571,#45572,#45573),
 .UNSPECIFIED.,.F.,.F.,(4,1,4),(0.,0.997451799764071,1.12274180646108),
 .UNSPECIFIED.);
#609=B_SPLINE_CURVE_WITH_KNOTS('',3,(#45578,#45579,#45580,#45581,#45582,
#45583,#45584,#45585,#45586,#45587,#45588,#45589,#45590,#45591,#45592,#45593,
#45594,#45595,#45596,#45597,#45598,#45599,#45600,#45601,#45602,#45603,#45604,
#45605,#45606,#45607,#45608,#45609,#45610,#45611,#45612,#45613,#45614,#45615,
#45616,#45617,#45618,#45619,#45620,#45621,#45622,#45623,#45624,#45625,#45626,
#45627,#45628,#45629,#45630,#45631,#45632,#45633,#45634,#45635,#45636,#45637,
#45638,#45639,#45640,#45641,#45642,#45643,#45644,#45645,#45646,#45647,#45648,
#45649,#45650,#45651,#45652,#45653,#45654,#45655,#45656,#45657,#45658,#45659,
#45660,#45661,#45662,#45663,#45664,#45665,#45666,#45667,#45668,#45669,#45670,
#45671,#45672,#45673,#45674,#45675,#45676,#45677,#45678,#45679,#45680,#45681,
#45682,#45683,#45684,#45685,#45686,#45687,#45688,#45689,#45690,#45691,#45692,
#45693,#45694,#45695,#45696,#45697,#45698,#45699,#45700,#45701,#45702,#45703,
#45704,#45705,#45706,#45707,#45708,#45709,#45710,#45711,#45712,#45713,#45714,
#45715,#45716,#45717,#45718,#45719,#45720,#45721,#45722,#45723,#45724,#45725,
#45726,#45727,#45728,#45729,#45730,#45731,#45732,#45733,#45734,#45735,#45736,
#45737,#45738,#45739,#45740,#45741,#45742,#45743,#45744,#45745,#45746,#45747,
#45748,#45749),.UNSPECIFIED.,.F.,.F.,(4,3,3,3,3,3,3,3,3,3,3,3,3,3,3,3,3,
3,3,3,3,3,3,3,3,3,3,3,3,3,3,3,3,3,3,3,3,3,3,3,3,3,3,3,3,3,3,3,3,3,3,3,3,
3,3,3,3,4),(-10.3752083948442,-10.2503833026325,-10.1250731934845,-9.99915640520669,
-9.97451799764071,-9.86110404478188,-9.7478938926556,-9.63479711949915,
-9.5217687878178,-9.40876406182607,-9.29565488796158,-9.18249497057902,
-9.06911746887118,-8.97706619787663,-8.86365051339009,-8.7504385362878,
-8.63733988266257,-8.52430961893586,-8.41130291316752,-8.29819170237126,
-8.1850297132015,-8.07165010949183,-7.97961439811257,-7.866221606749,-7.75303258758301,
-7.6399569151839,-7.52694961616527,-7.41396581883048,-7.30087724665411,
-7.1877377834431,-7.07438023313187,-6.9821625983485,-6.86872768090052,-6.7554967577242,
-6.64237934606444,-6.52933054251218,-6.416305545515,-6.30317657085608,-6.18999708090129,
-6.07660062945385,-5.98471079858443,-5.87127727316595,-5.75804701760528,
-5.64492983239768,-5.53188081910232,-5.41885518058614,-5.30572490890431,
-5.19254375753916,-5.07914507247754,-4.98725899882036,-4.87535456408063,
-4.76370217495604,-4.65215993920821,-4.54068066613504,-4.42851637982691,
-4.31695888287723,-4.20449120188987,-4.09202352090251),.UNSPECIFIED.);
#610=B_SPLINE_CURVE_WITH_KNOTS('',3,(#45750,#45751,#45752,#45753,#45754,
#45755,#45756,#45757,#45758,#45759,#45760,#45761,#45762,#45763,#45764,#45765,
#45766,#45767,#45768,#45769,#45770,#45771,#45772,#45773,#45774,#45775,#45776,
#45777,#45778,#45779,#45780,#45781,#45782,#45783,#45784,#45785,#45786,#45787,
#45788,#45789,#45790,#45791,#45792,#45793,#45794,#45795,#45796,#45797,#45798,
#45799,#45800,#45801,#45802,#45803,#45804,#45805,#45806,#45807,#45808,#45809,
#45810,#45811,#45812,#45813,#45814,#45815,#45816,#45817,#45818,#45819,#45820,
#45821,#45822,#45823,#45824,#45825,#45826,#45827,#45828,#45829,#45830,#45831,
#45832,#45833,#45834,#45835,#45836,#45837,#45838,#45839,#45840,#45841,#45842,
#45843,#45844,#45845,#45846,#45847,#45848,#45849,#45850,#45851,#45852,#45853,
#45854,#45855,#45856,#45857,#45858,#45859,#45860,#45861,#45862,#45863,#45864,
#45865,#45866,#45867,#45868,#45869,#45870,#45871,#45872,#45873,#45874,#45875,
#45876,#45877,#45878,#45879,#45880,#45881,#45882,#45883,#45884,#45885,#45886,
#45887,#45888,#45889,#45890,#45891,#45892,#45893,#45894,#45895,#45896,#45897,
#45898,#45899,#45900,#45901,#45902,#45903,#45904,#45905,#45906,#45907,#45908,
#45909,#45910,#45911,#45912,#45913,#45914,#45915,#45916,#45917,#45918,#45919,
#45920,#45921),.UNSPECIFIED.,.F.,.F.,(4,3,3,3,3,3,3,3,3,3,3,3,3,3,3,3,3,
3,3,3,3,3,3,3,3,3,3,3,3,3,3,3,3,3,3,3,3,3,3,3,3,3,3,3,3,3,3,3,3,3,3,3,3,
3,3,3,3,4),(1.12274180646108,1.23349876035573,1.34411485397831,1.45463835255786,
1.56511733193191,1.67568120756514,1.78628277695729,1.89709830417144,1.99490359952814,
2.10843227033142,2.22175603103796,2.33496564339142,2.4481058330173,2.5612212229477,
2.67443827120793,2.78770468900851,2.90118502291775,2.99235539929221,3.10595521961689,
3.21935723981433,3.33264940080441,3.44587627945317,3.55908235530706,3.67239561566932,
3.78576145357676,3.89934529158946,3.98980719905628,4.10308827144724,4.21616283373811,
4.32912245662456,4.442012318588,4.55487749425247,4.66784654485166,4.78086579292607,
4.8941035087682,4.98725899882035,5.1006938369561,5.21392493052826,5.32704266355744,
5.44009193523297,5.55311754307617,5.66624733656245,5.77942776152503,5.89282532003093,
5.98471079858443,6.09814320678973,6.21137255611537,6.32448896567656,6.43753733727379,
6.55056247156036,6.66369246422572,6.77687346077531,6.89027220554026,6.98216259834849,
7.10604783685458,7.22955918790001,7.35249446618955,7.4059271132892),
 .UNSPECIFIED.);
#611=B_SPLINE_CURVE_WITH_KNOTS('',3,(#45926,#45927,#45928,#45929,#45930,
#45931,#45932,#45933,#45934,#45935),.UNSPECIFIED.,.F.,.F.,(4,1,1,1,1,1,
1,4),(-16.6583941348078,-15.9592287962251,-14.9617769964611,-13.964325196697,
-12.9668733969329,-11.9694215971689,-10.9719697974048,-10.3752088276283),
 .UNSPECIFIED.);
#612=B_SPLINE_CURVE_WITH_KNOTS('',3,(#45936,#45937,#45938,#45939,#45940,
#45941,#45942,#45943,#45944,#45945,#45946,#45947,#45948,#45949,#45950,#45951,
#45952,#45953,#45954,#45955,#45956,#45957,#45958,#45959,#45960,#45961,#45962,
#45963,#45964,#45965,#45966,#45967,#45968,#45969,#45970,#45971,#45972,#45973,
#45974,#45975,#45976,#45977,#45978,#45979,#45980,#45981,#45982,#45983,#45984,
#45985,#45986,#45987,#45988,#45989,#45990,#45991,#45992,#45993,#45994,#45995,
#45996,#45997,#45998,#45999,#46000,#46001,#46002,#46003,#46004,#46005,#46006,
#46007,#46008,#46009,#46010,#46011,#46012,#46013,#46014,#46015,#46016,#46017,
#46018,#46019,#46020,#46021,#46022,#46023,#46024,#46025,#46026,#46027,#46028,
#46029,#46030,#46031,#46032,#46033,#46034,#46035,#46036,#46037,#46038,#46039,
#46040,#46041,#46042,#46043,#46044,#46045,#46046,#46047,#46048,#46049,#46050,
#46051,#46052,#46053,#46054,#46055,#46056,#46057,#46058,#46059,#46060,#46061,
#46062,#46063,#46064,#46065,#46066,#46067,#46068,#46069,#46070,#46071,#46072,
#46073,#46074,#46075,#46076,#46077,#46078,#46079,#46080,#46081,#46082,#46083,
#46084,#46085,#46086,#46087,#46088,#46089,#46090,#46091,#46092,#46093,#46094,
#46095,#46096,#46097,#46098,#46099,#46100,#46101,#46102,#46103,#46104,#46105,
#46106,#46107),.UNSPECIFIED.,.F.,.F.,(4,3,3,3,3,3,3,3,3,3,3,3,3,3,3,3,3,
3,3,3,3,3,3,3,3,3,3,3,3,3,3,3,3,3,3,3,3,3,3,3,3,3,3,3,3,3,3,3,3,3,3,3,3,
3,3,3,3,4),(7.40592711364064,7.52121005042001,7.63668183552839,7.75224539306113,
7.86809182454605,7.97961439811257,8.09303015678759,8.20624218300847,8.31934087042466,
8.43237115264579,8.54537786162435,8.6584890519252,8.77165100746136,8.8850305562887,
8.97706619787664,9.09047984077282,9.20368979858075,9.31678644809962,9.42981472662471,
9.54281946982981,9.65592876979487,9.76908887367652,9.88246665916506,9.97451799764071,
10.0879271238153,10.2011324266134,10.3142243399969,10.4272478097423,10.5402476798992,
10.653352045565,10.7665071733445,10.8798799765599,10.9719697974048,11.0853819666047,
11.1985903765148,11.3116854339006,11.4247120789009,11.5377151499773,11.6508227308402,
11.7639810868815,11.8773570988817,11.9694215971689,12.0828332562848,12.1960411565483,
12.3091357049343,12.422161842498,12.5351644086174,12.6482714925108,12.7614293552009,
12.8748048862075,12.9668733969329,13.0792407947244,13.1914409444974,13.303520564868,
13.4155510689317,13.5275526454623,13.6396214903294,13.6891124208202),
 .UNSPECIFIED.);
#613=B_SPLINE_CURVE_WITH_KNOTS('',3,(#46112,#46113,#46114,#46115,#46116,
#46117,#46118,#46119,#46120,#46121,#46122,#46123,#46124,#46125,#46126,#46127,
#46128,#46129,#46130,#46131,#46132,#46133,#46134,#46135,#46136,#46137,#46138,
#46139,#46140,#46141,#46142,#46143,#46144,#46145,#46146,#46147,#46148,#46149,
#46150,#46151,#46152,#46153,#46154,#46155,#46156,#46157,#46158,#46159,#46160,
#46161,#46162,#46163,#46164,#46165,#46166,#46167,#46168,#46169,#46170,#46171,
#46172,#46173,#46174,#46175,#46176,#46177,#46178,#46179,#46180,#46181,#46182,
#46183,#46184,#46185,#46186,#46187,#46188,#46189,#46190,#46191,#46192,#46193,
#46194,#46195,#46196,#46197,#46198,#46199,#46200,#46201,#46202,#46203,#46204,
#46205,#46206,#46207,#46208,#46209,#46210,#46211,#46212,#46213,#46214,#46215,
#46216,#46217,#46218,#46219,#46220,#46221,#46222,#46223,#46224,#46225,#46226,
#46227,#46228,#46229,#46230,#46231,#46232,#46233,#46234,#46235,#46236,#46237,
#46238,#46239,#46240,#46241,#46242,#46243,#46244,#46245,#46246,#46247,#46248,
#46249,#46250,#46251,#46252,#46253,#46254,#46255,#46256,#46257,#46258,#46259,
#46260,#46261,#46262,#46263,#46264,#46265,#46266,#46267,#46268,#46269,#46270,
#46271,#46272,#46273,#46274,#46275,#46276,#46277,#46278,#46279,#46280,#46281,
#46282,#46283),.UNSPECIFIED.,.F.,.F.,(4,3,3,3,3,3,3,3,3,3,3,3,3,3,3,3,3,
3,3,3,3,3,3,3,3,3,3,3,3,3,3,3,3,3,3,3,3,3,3,3,3,3,3,3,3,3,3,3,3,3,3,3,3,
3,3,3,3,4),(-22.9415794419855,-22.8281641120224,-22.7149525583976,-22.6018543727819,
-22.4888246206922,-22.375818469337,-22.2627078130779,-22.1495464168245,
-22.0361672912024,-21.9439395948096,-21.8305281426948,-21.7173204588114,
-21.6042261323817,-21.4912002219535,-21.3781978877594,-21.265091041421,
-21.1519334197811,-21.0385581325795,-20.9464877950455,-20.8330763403247,
-20.7198686538157,-20.60677432475,-20.4937484116803,-20.3807460748438,-20.267639225883,
-20.1544816016273,-20.0411063118546,-19.9490359952814,-19.8356245481252,
-19.722416869167,-19.6093225476384,-19.4962966420793,-19.3832943127141,
-19.2701874711044,-19.1570298541452,-19.0436545714864,-18.9515841955173,
-18.8381727422958,-18.724965057378,-18.6118707299584,-18.4988448185861,
-18.385842483495,-18.2727356363388,-18.1595780139235,-18.0462027260256,
-17.9541323957533,-17.8407209262676,-17.7275132249132,-17.6144188809639,
-17.5013929529983,-17.3883906012796,-17.2752837375772,-17.1621260986338,
-17.0487507944498,-16.9566805959892,-16.81839297033,-16.6820945023375,-16.658394483377),
 .UNSPECIFIED.);
#614=B_SPLINE_CURVE_WITH_KNOTS('',3,(#46284,#46285,#46286,#46287,#46288,
#46289,#46290,#46291,#46292,#46293,#46294,#46295,#46296,#46297,#46298,#46299,
#46300,#46301,#46302,#46303,#46304,#46305,#46306,#46307,#46308,#46309,#46310,
#46311,#46312,#46313,#46314,#46315,#46316,#46317,#46318,#46319,#46320,#46321,
#46322,#46323,#46324,#46325,#46326,#46327,#46328,#46329,#46330,#46331,#46332,
#46333,#46334,#46335,#46336,#46337,#46338,#46339,#46340,#46341,#46342,#46343,
#46344,#46345,#46346,#46347,#46348,#46349,#46350,#46351,#46352,#46353,#46354,
#46355,#46356,#46357,#46358,#46359,#46360,#46361,#46362,#46363,#46364,#46365,
#46366,#46367,#46368,#46369,#46370,#46371,#46372,#46373,#46374,#46375,#46376,
#46377,#46378,#46379,#46380,#46381,#46382,#46383,#46384,#46385,#46386,#46387,
#46388,#46389,#46390,#46391,#46392,#46393,#46394,#46395,#46396,#46397,#46398,
#46399,#46400,#46401,#46402,#46403,#46404,#46405,#46406,#46407,#46408,#46409,
#46410,#46411,#46412,#46413,#46414,#46415,#46416,#46417,#46418,#46419,#46420,
#46421,#46422,#46423,#46424,#46425,#46426,#46427,#46428,#46429,#46430,#46431,
#46432,#46433,#46434,#46435,#46436,#46437,#46438,#46439,#46440,#46441,#46442,
#46443,#46444,#46445,#46446,#46447,#46448,#46449,#46450,#46451,#46452,#46453,
#46454,#46455),.UNSPECIFIED.,.F.,.F.,(4,3,3,3,3,3,3,3,3,3,3,3,3,3,3,3,3,
3,3,3,3,3,3,3,3,3,3,3,3,3,3,3,3,3,3,3,3,3,3,3,3,3,3,3,3,3,3,3,3,3,3,3,3,
3,3,3,3,4),(13.6891124212831,13.830426267103,13.964325196697,14.0777367610392,
14.1909445588691,14.304039000212,14.4170650263139,14.5300674767369,14.6431744392318,
14.7563321771748,14.869707579436,14.9617769964611,15.075188464516,15.1883961653478,
15.3014905093303,15.4145164378841,15.5275187907461,15.6406256564511,15.7537832978754,
15.8671586053055,15.9592287962251,16.0726402106002,16.1858478557609,16.2989421428955,
16.4119680135264,16.5249703074907,16.6380771132471,16.7512346940451,16.8646099404927,
16.9566805959892,17.0700920649716,17.1832997660237,17.2963941097936,17.4094200377023,
17.5224223894861,17.6355292534425,17.7486868927446,17.8620621974556,17.9541323957533,
18.067543848488,18.1807515330992,18.2938458603223,18.406871771608,18.5198741067224,
18.6329809540715,18.746138576774,18.8595138651107,18.9515841955174,19.064995643072,
19.1782033222769,19.2912976439594,19.40432354958,19.5173258789145,19.6304327203509,
19.7435903370575,19.8569656193363,19.9490359952814,19.9722977279999),
 .UNSPECIFIED.);
#615=B_SPLINE_CURVE_WITH_KNOTS('',3,(#46460,#46461,#46462,#46463,#46464,
#46465,#46466,#46467,#46468,#46469,#46470,#46471,#46472,#46473,#46474,#46475,
#46476,#46477,#46478,#46479,#46480,#46481,#46482,#46483,#46484,#46485,#46486,
#46487,#46488,#46489,#46490,#46491,#46492,#46493,#46494,#46495,#46496,#46497,
#46498,#46499,#46500,#46501,#46502,#46503,#46504,#46505,#46506,#46507,#46508,
#46509,#46510,#46511,#46512,#46513,#46514,#46515,#46516,#46517,#46518,#46519,
#46520,#46521,#46522,#46523,#46524,#46525,#46526,#46527,#46528,#46529,#46530,
#46531,#46532,#46533,#46534,#46535,#46536,#46537,#46538,#46539,#46540,#46541,
#46542,#46543,#46544,#46545,#46546,#46547,#46548,#46549,#46550,#46551,#46552,
#46553,#46554,#46555,#46556,#46557,#46558,#46559,#46560,#46561,#46562,#46563,
#46564,#46565,#46566,#46567,#46568,#46569,#46570,#46571,#46572,#46573,#46574,
#46575,#46576,#46577,#46578,#46579,#46580,#46581,#46582,#46583,#46584,#46585,
#46586,#46587,#46588,#46589,#46590,#46591,#46592,#46593,#46594,#46595,#46596,
#46597,#46598,#46599,#46600,#46601,#46602,#46603,#46604,#46605,#46606,#46607,
#46608,#46609,#46610,#46611,#46612,#46613,#46614,#46615,#46616,#46617,#46618,
#46619,#46620,#46621,#46622,#46623,#46624,#46625,#46626,#46627,#46628,#46629,
#46630,#46631),.UNSPECIFIED.,.F.,.F.,(4,3,3,3,3,3,3,3,3,3,3,3,3,3,3,3,3,
3,3,3,3,3,3,3,3,3,3,3,3,3,3,3,3,3,3,3,3,3,3,3,3,3,3,3,3,3,3,3,3,3,3,3,3,
3,3,3,3,4),(-29.2247643991025,-29.0886098418601,-28.9504612883211,-28.9261021931581,
-28.8126907409659,-28.6994830569944,-28.5863887304699,-28.4733628199404,
-28.360360485639,-28.2472536391849,-28.1340960174244,-28.0207207300958,
-27.928650393394,-27.815238941203,-27.7020312572328,-27.5889369307099,-27.4759110201822,
-27.3629086858827,-27.2498018394306,-27.1366442176723,-27.0232689303461,
-26.9311985936299,-26.8177871413807,-26.7045794573521,-26.5914851307706,
-26.4784592201845,-26.3654568858265,-26.2523500393167,-26.1391924175008,
-26.0258171301183,-25.9337467938658,-25.8203353417363,-25.7071276578268,
-25.5940333313641,-25.4810074208961,-25.3680050866555,-25.254898240261,
-25.1417406185593,-25.0283653312878,-24.9362949941018,-24.8228835419418,
-24.7096758580039,-24.5965815315139,-24.4835556210198,-24.3705532867545,
-24.2574464403373,-24.1442888186141,-24.0309135313233,-23.9388431943377,
-23.8254356156578,-23.7122317969665,-23.5991413251002,-23.486119251654,
-23.3731207299011,-23.2600176887708,-23.1468638370261,-23.0334923835988,
-22.9415794423358),.UNSPECIFIED.);
#616=B_SPLINE_CURVE_WITH_KNOTS('',3,(#46632,#46633,#46634,#46635,#46636,
#46637,#46638,#46639,#46640,#46641,#46642,#46643,#46644,#46645,#46646,#46647,
#46648,#46649,#46650,#46651,#46652,#46653,#46654,#46655,#46656,#46657,#46658,
#46659,#46660,#46661,#46662,#46663,#46664,#46665,#46666,#46667,#46668,#46669,
#46670,#46671,#46672,#46673,#46674,#46675,#46676,#46677,#46678,#46679,#46680,
#46681,#46682,#46683,#46684,#46685,#46686,#46687,#46688,#46689,#46690,#46691,
#46692,#46693,#46694,#46695,#46696,#46697,#46698,#46699,#46700,#46701,#46702,
#46703,#46704,#46705,#46706,#46707,#46708,#46709,#46710,#46711,#46712,#46713,
#46714,#46715,#46716,#46717,#46718,#46719,#46720,#46721,#46722,#46723,#46724,
#46725,#46726,#46727,#46728,#46729,#46730,#46731,#46732,#46733,#46734,#46735,
#46736,#46737,#46738,#46739,#46740,#46741,#46742,#46743,#46744,#46745,#46746,
#46747,#46748,#46749,#46750,#46751,#46752,#46753,#46754,#46755,#46756,#46757,
#46758,#46759,#46760,#46761,#46762,#46763,#46764,#46765,#46766,#46767,#46768,
#46769,#46770,#46771,#46772,#46773,#46774,#46775,#46776,#46777,#46778,#46779,
#46780,#46781,#46782,#46783,#46784,#46785,#46786,#46787,#46788,#46789,#46790,
#46791,#46792,#46793,#46794,#46795,#46796,#46797,#46798,#46799,#46800,#46801,
#46802,#46803),.UNSPECIFIED.,.F.,.F.,(4,3,3,3,3,3,3,3,3,3,3,3,3,3,3,3,3,
3,3,3,3,3,3,3,3,3,3,3,3,3,3,3,3,3,3,3,3,3,3,3,3,3,3,3,3,3,3,3,3,3,3,3,3,
3,3,3,3,4),(19.9722977286751,20.0852614447579,20.1980240325097,20.3106755095438,
20.4232615627257,20.5358277786643,20.6484999916156,20.7612277552495,20.8741653780159,
20.9464877950455,21.0598992471089,21.1731069309596,21.2862012573683,21.3992271677869,
21.5122295019828,21.6253363483408,21.7384939700102,21.8518692572571,21.9439395948096,
22.0573510464558,22.170558729865,22.2836530558175,22.3966789657663,22.5096812994795,
22.6227881453382,22.7359457664985,22.8493210532263,22.9413913945736,23.0548028471147,
23.1680105314422,23.2811048583265,23.394130769219,23.5071331038862,23.6202399507073,
23.7333975728362,23.8467728605304,23.9388431943377,24.0522546464927,24.1654623304275,
24.2785566569154,24.3915825674085,24.5045849016738,24.6176917480928,24.7308493698188,
24.8442246571138,24.9362949941018,25.049706446238,25.1629141301516,25.276008456617,
25.389034367086,25.502036701326,25.6151435477177,25.728301169415,25.84167645668,
25.9337467938658,26.0684010631508,26.2015071711322,26.2554830347735),
 .UNSPECIFIED.);
#617=B_SPLINE_CURVE_WITH_KNOTS('',3,(#46808,#46809,#46810,#46811,#46812,
#46813,#46814,#46815,#46816,#46817),.UNSPECIFIED.,.F.,.F.,(4,1,1,1,1,1,
1,4),(-35.5079500563466,-34.9108129917425,-33.9133611919784,-32.9159093922143,
-31.9184575924503,-30.9210057926862,-29.9235539929221,-29.2247647491671),
 .UNSPECIFIED.);
#618=B_SPLINE_CURVE_WITH_KNOTS('',3,(#46818,#46819,#46820,#46821,#46822,
#46823,#46824,#46825,#46826,#46827,#46828,#46829,#46830,#46831,#46832,#46833,
#46834,#46835,#46836,#46837,#46838,#46839,#46840,#46841,#46842,#46843,#46844,
#46845,#46846,#46847,#46848,#46849,#46850,#46851,#46852,#46853,#46854,#46855,
#46856,#46857,#46858,#46859,#46860,#46861,#46862,#46863,#46864,#46865,#46866,
#46867,#46868,#46869,#46870,#46871,#46872,#46873,#46874,#46875,#46876,#46877,
#46878,#46879,#46880,#46881,#46882,#46883,#46884,#46885,#46886,#46887,#46888,
#46889,#46890,#46891,#46892,#46893,#46894,#46895,#46896,#46897,#46898,#46899,
#46900,#46901,#46902,#46903,#46904,#46905,#46906,#46907,#46908,#46909,#46910,
#46911,#46912,#46913,#46914,#46915,#46916,#46917,#46918,#46919,#46920,#46921,
#46922,#46923,#46924,#46925,#46926,#46927,#46928,#46929,#46930,#46931,#46932,
#46933,#46934,#46935,#46936,#46937,#46938,#46939,#46940,#46941,#46942,#46943,
#46944,#46945,#46946,#46947,#46948,#46949,#46950,#46951,#46952,#46953,#46954,
#46955,#46956,#46957,#46958,#46959,#46960,#46961,#46962,#46963,#46964,#46965,
#46966,#46967,#46968,#46969,#46970,#46971,#46972,#46973,#46974,#46975,#46976,
#46977,#46978,#46979,#46980,#46981,#46982,#46983,#46984,#46985,#46986,#46987,
#46988,#46989),.UNSPECIFIED.,.F.,.F.,(4,3,3,3,3,3,3,3,3,3,3,3,3,3,3,3,3,
3,3,3,3,3,3,3,3,3,3,3,3,3,3,3,3,3,3,3,3,3,3,3,3,3,3,3,3,3,3,3,3,3,3,3,3,
3,3,3,3,4),(26.2554830351794,26.3682243124585,26.4809384286302,26.5937592235565,
26.7066280453205,26.8197294891619,26.9311985936299,27.0446100458205,27.1578177297904,
27.2709120563132,27.3839379668408,27.4969403011404,27.6100471475925,27.723204769351,
27.8365800566775,27.928650393394,28.0420618455871,28.1552695295592,28.268363856084,
28.3813897666136,28.4943921009147,28.6074989473684,28.7206565691285,28.8340318564562,
28.9261021931581,29.0395136453643,29.1527213293499,29.2658156558886,29.3788415664321,
29.4918439007475,29.6049507472155,29.71810836899,29.8314836563322,29.9235539929221,
30.0369654451204,30.1501731290981,30.2632674556285,30.3762933661638,30.4892957004709,
30.6024025469306,30.7155601686967,30.8289354560306,30.9210057926862,31.0344172448853,
31.1476249288639,31.2607192553953,31.3737451659315,31.4867475002398,31.5998543467004,
31.7130119684676,31.8263872558023,31.9184575924503,32.0328851634577,32.1471215288982,
32.2611933998447,32.375169438642,32.489104873967,32.538668342359),
 .UNSPECIFIED.);
#619=B_SPLINE_CURVE_WITH_KNOTS('',3,(#46994,#46995,#46996,#46997,#46998,
#46999,#47000,#47001,#47002,#47003,#47004,#47005,#47006,#47007,#47008,#47009,
#47010,#47011,#47012,#47013,#47014,#47015,#47016,#47017,#47018,#47019,#47020,
#47021,#47022,#47023,#47024,#47025,#47026,#47027,#47028,#47029,#47030,#47031,
#47032,#47033,#47034,#47035,#47036,#47037,#47038,#47039,#47040,#47041,#47042,
#47043,#47044,#47045,#47046,#47047,#47048,#47049,#47050,#47051,#47052,#47053,
#47054,#47055,#47056,#47057,#47058,#47059,#47060,#47061,#47062,#47063,#47064,
#47065,#47066,#47067,#47068,#47069,#47070,#47071,#47072,#47073,#47074,#47075,
#47076,#47077,#47078,#47079,#47080,#47081,#47082,#47083,#47084,#47085,#47086,
#47087,#47088,#47089,#47090,#47091,#47092,#47093,#47094,#47095,#47096,#47097,
#47098,#47099,#47100,#47101,#47102,#47103,#47104,#47105,#47106,#47107,#47108,
#47109,#47110,#47111,#47112,#47113,#47114,#47115,#47116,#47117,#47118,#47119,
#47120,#47121,#47122,#47123,#47124,#47125,#47126,#47127,#47128,#47129,#47130,
#47131,#47132,#47133,#47134,#47135,#47136,#47137,#47138,#47139,#47140,#47141,
#47142,#47143,#47144,#47145,#47146,#47147,#47148,#47149,#47150,#47151,#47152,
#47153,#47154,#47155,#47156,#47157,#47158,#47159,#47160,#47161,#47162,#47163,
#47164,#47165),.UNSPECIFIED.,.F.,.F.,(4,3,3,3,3,3,3,3,3,3,3,3,3,3,3,3,3,
3,3,3,3,3,3,3,3,3,3,3,3,3,3,3,3,3,3,3,3,3,3,3,3,3,3,3,3,3,3,3,3,3,3,3,3,
3,3,3,3,4),(-41.7911353630763,-41.6791839164827,-41.5674467917417,-41.4558025914072,
-41.3442043092205,-41.2320341794971,-41.1203170881086,-41.0079204392178,
-40.8955237903269,-40.7821123381277,-40.6689046541491,-40.5558103276177,
-40.4427844170814,-40.3297820827733,-40.2166752363126,-40.1035176145455,
-39.9901423272108,-39.8980719905628,-39.7846605383621,-39.671452854382,
-39.558358527849,-39.4453326173112,-39.3323302830015,-39.2192234365393,
-39.1060658147706,-38.9926905274342,-38.9006201907988,-38.7872087385991,
-38.67400105462,-38.560906728088,-38.4478808175513,-38.3348784832428,-38.2217716367815,
-38.108614015014,-37.9952387276787,-37.9031683910347,-37.7897569388349,
-37.6765492548556,-37.5634549283234,-37.4504290177865,-37.3374266834777,
-37.2243198370163,-37.1111622152485,-36.997786927913,-36.9057165912706,
-36.7923051390707,-36.6790974550913,-36.5660031285592,-36.4529772180219,
-36.3399748837131,-36.2268680372516,-36.1137104154836,-36.000335128148,
-35.9082647915066,-35.7824128954135,-35.657006136482,-35.5322949997494,
-35.507950489932),.UNSPECIFIED.);
#620=B_SPLINE_CURVE_WITH_KNOTS('',3,(#47166,#47167,#47168,#47169,#47170,
#47171,#47172,#47173,#47174,#47175),.UNSPECIFIED.,.F.,.F.,(4,1,1,1,1,1,
1,4),(32.5386754793687,32.9159093922144,33.9133611919784,34.9108129917425,
35.9082647915066,36.9057165912706,37.9031683910347,38.8218455523264),
 .UNSPECIFIED.);
#621=B_SPLINE_CURVE_WITH_KNOTS('',3,(#47180,#47181,#47182,#47183,#47184,
#47185,#47186,#47187,#47188,#47189,#47190,#47191,#47192,#47193,#47194,#47195,
#47196,#47197,#47198,#47199,#47200,#47201,#47202,#47203,#47204,#47205,#47206,
#47207,#47208,#47209,#47210,#47211,#47212,#47213,#47214,#47215,#47216,#47217,
#47218,#47219,#47220,#47221,#47222,#47223,#47224,#47225,#47226,#47227,#47228,
#47229,#47230,#47231,#47232,#47233,#47234,#47235,#47236,#47237,#47238,#47239,
#47240,#47241,#47242,#47243,#47244,#47245,#47246,#47247,#47248,#47249,#47250,
#47251,#47252,#47253,#47254,#47255,#47256,#47257,#47258,#47259,#47260,#47261,
#47262,#47263,#47264,#47265,#47266,#47267,#47268,#47269,#47270,#47271,#47272,
#47273,#47274,#47275,#47276,#47277,#47278,#47279,#47280,#47281,#47282,#47283,
#47284,#47285,#47286,#47287,#47288,#47289,#47290,#47291,#47292,#47293,#47294,
#47295,#47296,#47297,#47298,#47299,#47300,#47301,#47302,#47303,#47304,#47305,
#47306,#47307,#47308,#47309,#47310,#47311,#47312,#47313,#47314,#47315,#47316,
#47317,#47318,#47319,#47320,#47321,#47322,#47323,#47324,#47325,#47326,#47327,
#47328,#47329,#47330,#47331,#47332,#47333,#47334,#47335,#47336,#47337,#47338,
#47339,#47340,#47341,#47342,#47343,#47344,#47345,#47346,#47347,#47348,#47349,
#47350,#47351),.UNSPECIFIED.,.F.,.F.,(4,3,3,3,3,3,3,3,3,3,3,3,3,3,3,3,3,
3,3,3,3,3,3,3,3,3,3,3,3,3,3,3,3,3,3,3,3,3,3,3,3,3,3,3,3,3,3,3,3,3,3,3,3,
3,3,3,3,4),(-48.0743206707058,-47.9107513804871,-47.8776863886754,-47.7642749365203,
-47.6510672525854,-47.5379729260974,-47.4249470156042,-47.3119446813386,
-47.1988378349195,-47.0856802131936,-46.9723049258985,-46.8802345889113,
-46.7668231367748,-46.653615452861,-46.5405211263955,-46.4274952159263,
-46.3144928816861,-46.2013860352943,-46.0882284135968,-45.9748531263316,
-45.8827827891473,-45.7693713369007,-45.6561636528737,-45.5430693262933,
-45.4300434157076,-45.3170410813495,-45.2039342348387,-45.0907766130212,
-44.9774013256363,-44.8853309893832,-44.7719195371926,-44.6587118532226,
-44.5456175266998,-44.4325916161722,-44.3195892818726,-44.2064824354204,
-44.0933248136618,-43.9799495263352,-43.8878791896191,-43.7744677374261,
-43.661260053454,-43.5481657269291,-43.4351398163996,-43.3221374820982,
-43.2090306356445,-43.0958730138844,-42.9824977265567,-42.890427389855,
-42.7770159376488,-42.6638082536632,-42.5507139271245,-42.437688016581,
-42.3246856822654,-42.2115788357974,-42.0984212140229,-41.9850459266807,
-41.892975590091,-41.7911353635262),.UNSPECIFIED.);
#622=B_SPLINE_CURVE_WITH_KNOTS('',3,(#47352,#47353,#47354,#47355,#47356,
#47357,#47358,#47359,#47360,#47361,#47362,#47363,#47364,#47365,#47366,#47367,
#47368,#47369,#47370,#47371,#47372,#47373,#47374,#47375,#47376,#47377,#47378,
#47379,#47380,#47381,#47382,#47383,#47384,#47385,#47386,#47387,#47388,#47389,
#47390,#47391,#47392,#47393,#47394,#47395,#47396,#47397,#47398,#47399,#47400,
#47401,#47402,#47403,#47404,#47405,#47406,#47407,#47408,#47409,#47410,#47411,
#47412,#47413,#47414,#47415,#47416,#47417,#47418,#47419,#47420,#47421,#47422,
#47423,#47424,#47425,#47426,#47427,#47428,#47429,#47430,#47431,#47432,#47433,
#47434,#47435,#47436,#47437,#47438,#47439,#47440,#47441,#47442,#47443,#47444,
#47445,#47446,#47447,#47448,#47449,#47450,#47451,#47452,#47453,#47454,#47455,
#47456,#47457,#47458,#47459,#47460,#47461,#47462,#47463,#47464,#47465,#47466,
#47467,#47468,#47469,#47470,#47471,#47472,#47473,#47474,#47475,#47476,#47477,
#47478,#47479,#47480,#47481,#47482,#47483,#47484,#47485,#47486,#47487,#47488,
#47489,#47490,#47491,#47492,#47493,#47494,#47495,#47496,#47497,#47498,#47499,
#47500,#47501,#47502,#47503,#47504,#47505,#47506,#47507,#47508,#47509,#47510,
#47511,#47512,#47513,#47514,#47515,#47516,#47517,#47518,#47519,#47520,#47521,
#47522,#47523),.UNSPECIFIED.,.F.,.F.,(4,3,3,3,3,3,3,3,3,3,3,3,3,3,3,3,3,
3,3,3,3,3,3,3,3,3,3,3,3,3,3,3,3,3,3,3,3,3,3,3,3,3,3,3,3,3,3,3,3,3,3,3,3,
3,3,3,3,4),(38.8218536495386,38.9006201907988,39.0140316429996,39.1272393269797,
39.2403336535128,39.3533595640506,39.4663618983604,39.5794687448226,39.6926263665913,
39.8060016539276,39.8980719905628,40.0114834427619,40.1246911267404,40.2377854532718,
40.350811363808,40.4638136981161,40.5769205445768,40.6900781663439,40.8034534536787,
40.8955237903269,41.0089352425252,41.1221429265028,41.2352372530334,41.3482631635687,
41.4612654978759,41.5743723443357,41.6875299661018,41.8009052534357,41.892975590091,
42.0063870422976,42.1195947262836,42.2326890528224,42.345714963366,42.4587172976816,
42.5718241441495,42.6849817659238,42.7983570532657,42.8904273898551,43.0038388420472,
43.1170465260187,43.2301408525431,43.3431667630725,43.4561690973737,43.5692759438278,
43.6824335655883,43.7958088529168,43.8878791896191,44.0012906418101,44.1144983257803,
44.2275926523032,44.3406185628308,44.4536208971304,44.5667277435824,44.6798853653407,
44.7932606526669,44.8853309893832,45.0403742212961,45.1050389567181),
 .UNSPECIFIED.);
#623=B_SPLINE_CURVE_WITH_KNOTS('',3,(#47528,#47529,#47530,#47531,#47532,
#47533,#47534,#47535,#47536,#47537),.UNSPECIFIED.,.F.,.F.,(4,1,1,1,1,1,
1,4),(-54.3575057011833,-53.8623971872598,-52.8649453874958,-51.8674935877317,
-50.8700417879676,-49.8725899882035,-48.8751381884395,-48.0743241720579),
 .UNSPECIFIED.);
#624=B_SPLINE_CURVE_WITH_KNOTS('',3,(#47538,#47539,#47540,#47541,#47542,
#47543,#47544,#47545,#47546,#47547,#47548,#47549,#47550,#47551,#47552,#47553,
#47554,#47555,#47556,#47557,#47558,#47559,#47560,#47561,#47562,#47563,#47564,
#47565,#47566,#47567,#47568,#47569,#47570,#47571,#47572,#47573,#47574,#47575,
#47576,#47577,#47578,#47579,#47580,#47581,#47582,#47583,#47584,#47585,#47586,
#47587,#47588,#47589,#47590,#47591,#47592,#47593,#47594,#47595,#47596,#47597,
#47598,#47599,#47600,#47601,#47602,#47603,#47604,#47605,#47606,#47607,#47608,
#47609,#47610,#47611,#47612,#47613,#47614,#47615,#47616,#47617,#47618,#47619,
#47620,#47621,#47622,#47623,#47624,#47625,#47626,#47627,#47628,#47629,#47630,
#47631,#47632,#47633,#47634,#47635,#47636,#47637,#47638,#47639,#47640,#47641,
#47642,#47643,#47644,#47645,#47646,#47647,#47648,#47649,#47650,#47651,#47652,
#47653,#47654,#47655,#47656,#47657,#47658,#47659,#47660,#47661,#47662,#47663,
#47664,#47665,#47666,#47667,#47668,#47669,#47670,#47671,#47672,#47673,#47674,
#47675,#47676,#47677,#47678,#47679,#47680,#47681,#47682,#47683,#47684,#47685,
#47686,#47687,#47688,#47689,#47690,#47691,#47692,#47693,#47694,#47695,#47696,
#47697,#47698,#47699,#47700,#47701,#47702,#47703,#47704,#47705,#47706,#47707,
#47708,#47709),.UNSPECIFIED.,.F.,.F.,(4,3,3,3,3,3,3,3,3,3,3,3,3,3,3,3,3,
3,3,3,3,3,3,3,3,3,3,3,3,3,3,3,3,3,3,3,3,3,3,3,3,3,3,3,3,3,3,3,3,3,3,3,3,
3,3,3,3,4),(45.1050389572695,45.2166679109873,45.3282052498347,45.4396980981619,
45.5512757199758,45.662889531836,45.7747203023662,45.8827827891473,45.9961942412766,
46.1094019251858,46.2224962516483,46.3355221621161,46.4485244963565,46.5616313427509,
46.6747889644524,46.7881642517237,46.8802345889113,46.9936460410712,47.1068537250089,
47.2199480514988,47.3329739619927,47.4459762962578,47.5590831426749,47.6722407643979,
47.7856160516885,47.8776863886754,47.9910978412332,48.1043055255711,48.2173998524622,
48.3304257633577,48.443428098024,48.5565349448385,48.6696925669575,48.7830678546367,
48.8751381884395,48.9885496400318,49.1017573234071,49.214851649338,49.3278775592774,
49.4408798929934,49.5539867388737,49.6671443600661,49.7805196468428,49.8725899882036,
49.9860014403177,50.0992091242004,50.2123034506294,50.3253293610571,50.4383316952503,
50.551438541588,50.6645961632272,50.777971450428,50.8700417879676,50.9882858012164,
51.1061966176998,51.2239066097079,51.3413928306475,51.3882242638978),
 .UNSPECIFIED.);
#625=B_SPLINE_CURVE_WITH_KNOTS('',3,(#47714,#47715,#47716,#47717,#47718,
#47719,#47720,#47721,#47722,#47723,#47724,#47725,#47726,#47727,#47728,#47729,
#47730,#47731,#47732,#47733,#47734,#47735,#47736,#47737,#47738,#47739,#47740,
#47741,#47742,#47743,#47744,#47745,#47746,#47747,#47748,#47749,#47750,#47751,
#47752,#47753,#47754,#47755,#47756,#47757,#47758,#47759,#47760,#47761,#47762,
#47763,#47764,#47765,#47766,#47767,#47768,#47769,#47770,#47771,#47772,#47773,
#47774,#47775,#47776,#47777,#47778,#47779,#47780,#47781,#47782,#47783,#47784,
#47785,#47786,#47787,#47788,#47789,#47790,#47791,#47792,#47793,#47794,#47795,
#47796,#47797,#47798,#47799,#47800,#47801,#47802,#47803,#47804,#47805,#47806,
#47807,#47808,#47809,#47810,#47811,#47812,#47813,#47814,#47815,#47816,#47817,
#47818,#47819,#47820,#47821,#47822,#47823,#47824,#47825,#47826,#47827,#47828,
#47829,#47830,#47831,#47832,#47833,#47834,#47835,#47836,#47837,#47838,#47839,
#47840,#47841,#47842,#47843,#47844,#47845,#47846,#47847,#47848,#47849,#47850,
#47851,#47852,#47853,#47854,#47855,#47856,#47857,#47858,#47859,#47860,#47861,
#47862,#47863,#47864,#47865,#47866,#47867,#47868,#47869,#47870,#47871,#47872,
#47873,#47874,#47875,#47876,#47877,#47878,#47879,#47880,#47881,#47882,#47883,
#47884,#47885),.UNSPECIFIED.,.F.,.F.,(4,3,3,3,3,3,3,3,3,3,3,3,3,3,3,3,3,
3,3,3,3,3,3,3,3,3,3,3,3,3,3,3,3,3,3,3,3,3,3,3,3,3,3,3,3,3,3,3,3,3,3,3,3,
3,3,3,3,4),(-60.6406912844698,-60.5291209741293,-60.417650226069,-60.3062318016793,
-60.1914508477206,-60.0799232699748,-59.9635156279096,-59.8471079858443,
-59.7336963268614,-59.6204884267402,-59.5073938785023,-59.3943677410919,
-59.2813651751309,-59.1682580914026,-59.0551002288817,-58.9417246980488,
-58.8496561860802,-58.7362450335743,-58.6230376567668,-58.5099436417519,
-58.3969180465193,-58.2839160307492,-58.1708095053147,-58.0576522064656,
-57.9442772410778,-57.8522043863161,-57.7387928221874,-57.6255850245746,
-57.5124905834508,-57.3994645575697,-57.2864621073685,-57.1733551450959,
-57.0601974073755,-56.9468220053348,-56.854752586552,-56.7413411185027,
-56.6281334176777,-56.5150390737027,-56.4020131451571,-56.289010792304,
-56.1759039266089,-56.0627462851953,-55.9493709777767,-55.857300786788,
-55.7438893723472,-55.6306817271192,-55.5175874399162,-55.404561569216,
-55.2915592751816,-55.1784524693545,-55.0652948884853,-54.9519196419665,
-54.8598489870239,-54.7408090857764,-54.622127699113,-54.503666173285,-54.3854603615985,
-54.3575059778853),.UNSPECIFIED.);
#626=B_SPLINE_CURVE_WITH_KNOTS('',3,(#47886,#47887,#47888,#47889,#47890,
#47891,#47892,#47893,#47894,#47895,#47896,#47897,#47898,#47899,#47900,#47901,
#47902,#47903,#47904,#47905,#47906,#47907,#47908,#47909,#47910,#47911,#47912,
#47913,#47914,#47915,#47916,#47917,#47918,#47919,#47920,#47921,#47922,#47923,
#47924,#47925,#47926,#47927,#47928,#47929,#47930,#47931,#47932,#47933,#47934,
#47935,#47936,#47937,#47938,#47939,#47940,#47941,#47942,#47943,#47944,#47945,
#47946,#47947,#47948,#47949,#47950,#47951,#47952,#47953,#47954,#47955,#47956,
#47957,#47958,#47959,#47960,#47961,#47962,#47963,#47964,#47965,#47966,#47967,
#47968,#47969,#47970,#47971,#47972,#47973,#47974,#47975,#47976,#47977,#47978,
#47979,#47980,#47981,#47982,#47983,#47984,#47985,#47986,#47987,#47988,#47989,
#47990,#47991,#47992,#47993,#47994,#47995,#47996,#47997,#47998,#47999,#48000,
#48001,#48002,#48003,#48004,#48005,#48006,#48007,#48008,#48009,#48010,#48011,
#48012,#48013,#48014,#48015,#48016,#48017,#48018,#48019,#48020,#48021,#48022,
#48023,#48024,#48025,#48026,#48027,#48028,#48029,#48030,#48031,#48032,#48033,
#48034,#48035,#48036,#48037,#48038,#48039,#48040,#48041,#48042,#48043,#48044,
#48045,#48046,#48047,#48048,#48049,#48050,#48051,#48052,#48053,#48054,#48055,
#48056,#48057),.UNSPECIFIED.,.F.,.F.,(4,3,3,3,3,3,3,3,3,3,3,3,3,3,3,3,3,
3,3,3,3,3,3,3,3,3,3,3,3,3,3,3,3,3,3,3,3,3,3,3,3,3,3,3,3,3,3,3,3,3,3,3,3,
3,3,3,3,4),(51.388224264309,51.5080415951646,51.6277999255016,51.747986711116,
51.8674935877317,51.9809050348777,52.0941127138258,52.2072070353442,52.3202329408932,
52.4332352702484,52.5463421118483,52.6594997287978,52.7728750114472,52.8649453874958,
52.9783568407164,53.091564525633,53.2046588530513,53.3176847644222,53.430687099512,
53.5437939466665,53.6569515690802,53.7703268569763,53.8623971872599,53.9758086567831,
54.0890163581752,54.2021107021622,54.3151366301656,54.428138981922,54.5412458456617,
54.6544034846422,54.7677787888627,54.8598489870239,54.9732603983721,55.0864680416299,
55.1995623275488,55.3125881976491,55.4255904917669,55.5386972987355,55.6518548813328,
55.7652301305258,55.857300786788,55.9707122592066,56.0839199627815,56.1970143085166,
56.3100402378354,56.4230425904762,56.5361494544338,56.6493070932641,56.7626823967366,
56.8547525865521,56.96644110335,57.0779705555368,57.1893884864546,57.3007422449335,
57.4121297263007,57.5235379612258,57.6350798901998,57.6714095705593),
 .UNSPECIFIED.);
#627=B_SPLINE_CURVE_WITH_KNOTS('',3,(#48062,#48063,#48064,#48065,#48066,
#48067,#48068,#48069,#48070,#48071,#48072,#48073,#48074,#48075,#48076,#48077,
#48078,#48079,#48080,#48081,#48082,#48083,#48084,#48085,#48086,#48087,#48088,
#48089,#48090,#48091,#48092,#48093,#48094,#48095,#48096,#48097,#48098,#48099,
#48100,#48101,#48102,#48103,#48104,#48105,#48106,#48107,#48108,#48109,#48110,
#48111,#48112,#48113,#48114,#48115,#48116,#48117,#48118,#48119,#48120,#48121,
#48122,#48123,#48124,#48125,#48126,#48127,#48128,#48129,#48130,#48131,#48132,
#48133,#48134,#48135,#48136,#48137,#48138,#48139,#48140,#48141,#48142,#48143,
#48144,#48145,#48146,#48147,#48148,#48149,#48150,#48151,#48152,#48153,#48154,
#48155,#48156,#48157,#48158,#48159,#48160,#48161,#48162,#48163,#48164,#48165,
#48166,#48167,#48168,#48169,#48170,#48171,#48172,#48173,#48174,#48175,#48176,
#48177,#48178,#48179,#48180,#48181,#48182,#48183,#48184,#48185,#48186,#48187,
#48188,#48189,#48190,#48191,#48192,#48193,#48194,#48195,#48196,#48197,#48198,
#48199,#48200,#48201,#48202,#48203,#48204,#48205,#48206,#48207,#48208,#48209,
#48210,#48211,#48212,#48213,#48214,#48215,#48216,#48217,#48218,#48219,#48220,
#48221,#48222,#48223,#48224,#48225,#48226,#48227,#48228,#48229,#48230,#48231,
#48232,#48233),.UNSPECIFIED.,.F.,.F.,(4,3,3,3,3,3,3,3,3,3,3,3,3,3,3,3,3,
3,3,3,3,3,3,3,3,3,3,3,3,3,3,3,3,3,3,3,3,3,3,3,3,3,3,3,3,3,3,3,3,3,3,3,3,
3,3,3,3,4),(-66.9238765922446,-66.8292705841928,-66.7158357794347,-66.6026047197083,
-66.4894870207858,-66.3764377834166,-66.2634122100187,-66.150282450917,
-66.0371020603601,-65.9237045358565,-65.8318187844287,-65.7183863844429,
-65.6051570436917,-65.4920406429159,-65.3789922802997,-65.2659671551746,
-65.1528371718813,-65.0396561848354,-64.9262574496734,-64.8343669846646,
-64.7209731386006,-64.6077834563938,-64.4947073603155,-64.3816998763103,
-64.2687161323106,-64.155627982331,-64.0424891458818,-63.9291325519897,
-63.8369151849005,-63.7234994326658,-63.6102874129762,-63.4971887321421,
-63.384158456542,-63.2711517542119,-63.1580405705486,-63.0448786216547,
-62.9314990793927,-62.8394633851365,-62.726049743495,-62.6128397870048,
-62.4997431388413,-62.386714861707,-62.2737101199256,-62.1606008214247,
-62.0474407190319,-61.9340629350545,-61.8420115853724,-61.7286024564631,
-61.615397150865,-61.5023052346435,-61.3892817620273,-61.2762818889718,
-61.1631775203868,-61.0500223896721,-60.9366495835322,-60.8445597856083,
-60.683912590964,-60.640691285065),.UNSPECIFIED.);
#628=B_SPLINE_CURVE_WITH_KNOTS('',3,(#48234,#48235,#48236,#48237,#48238,
#48239,#48240,#48241,#48242,#48243,#48244,#48245,#48246,#48247,#48248,#48249,
#48250,#48251,#48252,#48253,#48254,#48255,#48256,#48257,#48258,#48259,#48260,
#48261,#48262,#48263,#48264,#48265,#48266,#48267,#48268,#48269,#48270,#48271,
#48272,#48273,#48274,#48275,#48276,#48277,#48278,#48279,#48280,#48281,#48282,
#48283,#48284,#48285,#48286,#48287,#48288,#48289,#48290,#48291,#48292,#48293,
#48294,#48295,#48296,#48297,#48298,#48299,#48300,#48301,#48302,#48303,#48304,
#48305,#48306,#48307,#48308,#48309,#48310,#48311,#48312,#48313,#48314,#48315,
#48316,#48317,#48318,#48319,#48320,#48321,#48322,#48323,#48324,#48325,#48326,
#48327,#48328,#48329,#48330,#48331,#48332,#48333,#48334,#48335,#48336,#48337,
#48338,#48339,#48340,#48341,#48342,#48343,#48344,#48345,#48346,#48347,#48348,
#48349,#48350,#48351,#48352,#48353,#48354,#48355,#48356,#48357,#48358,#48359,
#48360,#48361,#48362,#48363,#48364,#48365,#48366,#48367,#48368,#48369,#48370,
#48371,#48372,#48373,#48374,#48375,#48376,#48377,#48378,#48379,#48380,#48381,
#48382,#48383,#48384,#48385,#48386,#48387,#48388,#48389,#48390,#48391,#48392,
#48393,#48394,#48395,#48396,#48397,#48398,#48399,#48400,#48401,#48402,#48403,
#48404,#48405),.UNSPECIFIED.,.F.,.F.,(4,3,3,3,3,3,3,3,3,3,3,3,3,3,3,3,3,
3,3,3,3,3,3,3,3,3,3,3,3,3,3,3,3,3,3,3,3,3,3,3,3,3,3,3,3,3,3,3,3,3,3,3,3,
3,3,3,3,4),(57.6714095710774,57.8424716034082,57.8522043863161,57.96561551648,
58.0788228790694,58.1919168848318,58.3049424757643,58.4179444921801,58.5310510259175,
58.644208337316,58.7575833221,58.8496561860802,58.9630678826949,59.0762758065309,
59.1893703699776,59.3023965141141,59.4153990783317,59.5285061472084,59.6416639876074,
59.7550394846039,59.8471079858443,59.9605201596495,60.0737285724546,60.1868236316899,
60.2998502774975,60.4128533483403,60.5259609273589,60.6391192806626,60.752495288486,
60.8445597856084,60.9579687573358,61.0711739630446,61.1842658143953,61.2972892570663,
61.410289135053,61.5233935625653,61.6365487821517,61.7499217254423,61.8420115853724,
61.9554255397486,62.0686356933578,62.1817324679752,62.2947608010934,62.4077655284956,
62.5208747037191,62.6340346224343,62.7474121254151,62.8394633851365,62.9528790761637,
63.0660910598602,63.1791897201077,63.2922199904731,63.4052267028848,63.5183379202786,
63.6314999160311,63.7448795262153,63.8369151849006,63.9545948782569),
 .UNSPECIFIED.);
#629=B_SPLINE_CURVE_WITH_KNOTS('',3,(#48408,#48409,#48410,#48411,#48412,
#48413,#48414,#48415,#48416,#48417,#48418,#48419,#48420,#48421,#48422,#48423,
#48424,#48425,#48426,#48427,#48428,#48429,#48430,#48431,#48432,#48433,#48434,
#48435,#48436,#48437,#48438,#48439,#48440,#48441,#48442,#48443,#48444,#48445,
#48446,#48447,#48448,#48449,#48450,#48451,#48452,#48453,#48454,#48455,#48456,
#48457,#48458,#48459,#48460,#48461,#48462,#48463,#48464,#48465,#48466,#48467,
#48468,#48469,#48470,#48471,#48472,#48473,#48474,#48475,#48476,#48477,#48478,
#48479,#48480,#48481,#48482,#48483,#48484,#48485,#48486,#48487,#48488,#48489,
#48490,#48491,#48492,#48493,#48494,#48495,#48496,#48497,#48498,#48499,#48500,
#48501,#48502,#48503,#48504,#48505,#48506,#48507,#48508,#48509,#48510,#48511,
#48512,#48513,#48514,#48515,#48516,#48517,#48518,#48519,#48520,#48521,#48522,
#48523,#48524,#48525,#48526,#48527,#48528,#48529,#48530,#48531,#48532,#48533,
#48534,#48535,#48536,#48537,#48538,#48539,#48540,#48541,#48542,#48543,#48544,
#48545,#48546,#48547,#48548,#48549,#48550,#48551,#48552,#48553,#48554,#48555,
#48556,#48557,#48558,#48559,#48560,#48561,#48562,#48563,#48564,#48565,#48566,
#48567),.UNSPECIFIED.,.F.,.F.,(4,3,3,3,3,3,3,3,3,3,3,3,3,3,3,3,3,3,3,3,
3,3,3,3,3,3,3,3,3,3,3,3,3,3,3,3,3,3,3,3,3,3,3,3,3,3,3,3,3,3,3,3,3,4),(63.9545948787019,
64.0663283121786,64.1779267459133,64.2894374686781,64.4009076217729,64.5124655336905,
64.624063195758,64.7358746481165,64.8343669846646,64.9478019117417,65.0610328443785,
65.1741502653896,65.2871990781696,65.4002240842566,65.5133530677227,65.6265325663426,
65.7399290261141,65.8318187844287,65.9452523437199,66.0584826334375,66.1715998529507,
66.2846489006395,66.3976745735762,66.5108048794446,66.6239860649216,66.7373847835369,
66.8292705841928,66.9425447390915,67.0556149512323,67.1685717922222,67.2814604361248,
67.3943259551164,67.5072977677325,67.6203211180831,67.7335651001906,67.8267223839568,
67.9403424102071,68.0537571248511,68.1670573855848,68.2802877819635,68.3934928005795,
68.5067979340436,68.6201517182112,68.7337171970108,68.8241741837209,68.9390720244675,
69.0510940384473,69.16300915207,69.2748640897515,69.391987294737,69.5039323893411,
69.6159429374358,69.7281336005457,69.7433569096934),.UNSPECIFIED.);
#630=B_SPLINE_CURVE_WITH_KNOTS('',3,(#48570,#48571,#48572,#48573,#48574,
#48575,#48576,#48577),.UNSPECIFIED.,.F.,.F.,(4,1,1,1,1,4),(-71.8165295830131,
-70.819077783249,-69.821625983485,-68.8241741837209,-67.8267223839568,-66.9238856394982),
 .UNSPECIFIED.);
#631=B_SPLINE_CURVE_WITH_KNOTS('',3,(#48580,#48581,#48582,#48583,#48584,
#48585),.UNSPECIFIED.,.F.,.F.,(4,1,1,4),(76.8085816652527,77.4477585319289,
78.445210331693,78.5398163397448),.UNSPECIFIED.);
#632=B_SPLINE_CURVE_WITH_KNOTS('',3,(#48587,#48588,#48589,#48590,#48591,
#48592,#48593,#48594,#48595,#48596,#48597,#48598,#48599,#48600,#48601,#48602,
#48603,#48604,#48605,#48606,#48607,#48608,#48609,#48610,#48611,#48612,#48613,
#48614,#48615,#48616,#48617,#48618,#48619,#48620,#48621,#48622,#48623,#48624,
#48625,#48626,#48627,#48628,#48629,#48630,#48631,#48632,#48633,#48634,#48635,
#48636,#48637,#48638,#48639,#48640,#48641,#48642,#48643,#48644,#48645,#48646,
#48647,#48648,#48649,#48650,#48651,#48652,#48653,#48654,#48655,#48656,#48657,
#48658,#48659,#48660,#48661,#48662),.UNSPECIFIED.,.F.,.F.,(4,3,3,3,3,3,
3,3,3,3,3,3,3,3,3,3,3,3,3,3,3,3,3,3,3,4),(78.5398169174564,78.6578581631678,
78.7757424064956,78.8935252569696,79.0112621341111,79.1290951210731,79.2469767917089,
79.3650860989278,79.4426621314571,79.5673436064276,79.6870738654733,79.8066827764956,
79.9262228004682,80.0457462805851,80.165386573184,80.2850966099796,80.4050192989118,
80.4401139312211,80.5585544019957,80.6768236178663,80.7949767675224,80.9130688341455,
81.0312371578687,81.1494402209803,81.2678606949208,81.359267928529),
 .UNSPECIFIED.);
#633=B_SPLINE_CURVE_WITH_KNOTS('',3,(#48666,#48667,#48668,#48669,#48670,
#48671,#48672,#48673,#48674,#48675,#48676,#48677,#48678,#48679,#48680,#48681,
#48682,#48683,#48684,#48685,#48686,#48687,#48688,#48689,#48690,#48691,#48692,
#48693,#48694,#48695,#48696,#48697,#48698,#48699,#48700,#48701,#48702,#48703,
#48704,#48705),.UNSPECIFIED.,.F.,.F.,(4,3,3,3,3,3,3,3,3,3,3,3,3,4),(78.5398163397448,
78.659636125144,78.7796502246197,78.8997625732989,79.020191251719,79.1211139375573,
79.2457954125278,79.368520780898,79.4910833479872,79.6135264861919,79.7397862989743,
79.8621555193481,79.9903606283347,80.1185657373213),.UNSPECIFIED.);
#634=B_SPLINE_CURVE_WITH_KNOTS('',3,(#48706,#48707,#48708,#48709,#48710,
#48711,#48712,#48713,#48714,#48715,#48716,#48717,#48718,#48719,#48720,#48721,
#48722,#48723,#48724,#48725,#48726,#48727,#48728,#48729,#48730,#48731,#48732,
#48733,#48734,#48735,#48736,#48737,#48738,#48739,#48740,#48741,#48742,#48743,
#48744,#48745,#48746,#48747,#48748,#48749,#48750,#48751,#48752,#48753,#48754),
 .UNSPECIFIED.,.F.,.F.,(4,3,3,3,3,3,3,3,3,3,3,3,3,3,3,3,4),(76.8075006878804,
76.9271796581132,77.0470845181732,77.1262103380291,77.2508918129996,77.3705174501154,
77.4900255177582,77.6094686275862,77.7288992786733,77.8484533949029,77.9680810296881,
78.0879276324046,78.1236621377932,78.254454988324,78.3847951958607,78.5144734410687,
78.5398163389325),.UNSPECIFIED.);
#635=B_SPLINE_CURVE_WITH_KNOTS('',3,(#48759,#48760,#48761,#48762,#48763,
#48764,#48765,#48766,#48767,#48768,#48769,#48770,#48771,#48772,#48773,#48774,
#48775,#48776,#48777,#48778,#48779,#48780,#48781,#48782,#48783,#48784,#48785,
#48786,#48787,#48788,#48789,#48790,#48791,#48792,#48793,#48794,#48795,#48796,
#48797,#48798,#48799,#48800,#48801,#48802,#48803,#48804,#48805,#48806,#48807,
#48808,#48809,#48810,#48811,#48812,#48813,#48814,#48815,#48816,#48817,#48818,
#48819,#48820,#48821,#48822,#48823,#48824,#48825,#48826,#48827,#48828,#48829,
#48830,#48831,#48832,#48833,#48834,#48835,#48836,#48837),.UNSPECIFIED.,
 .F.,.F.,(4,3,3,3,3,3,3,3,3,3,3,3,3,3,3,3,3,3,3,3,3,3,3,3,3,3,4),(-0.272733684723234,
-0.263933091050529,-0.246609025869403,-0.237097850216621,-0.231283116386945,
-0.214097972171501,-0.199459807385004,-0.196214597656375,-0.179475273061678,
-0.163134910222118,-0.153693408780706,-0.149077859260717,-0.145944972824637,
-0.130068097350725,-0.12534056960152,-0.109094409153109,-0.101071207557617,
-0.0956993686354407,-0.0926136204289078,-0.0768607618484406,-0.0612146360061542,
-0.0532966001767691,-0.0475071880028156,-0.0447088814465312,-0.0296023839094069,
-0.0148011919547035,0.),.UNSPECIFIED.);
#636=B_SPLINE_CURVE_WITH_KNOTS('',3,(#48838,#48839,#48840,#48841,#48842,
#48843,#48844,#48845,#48846,#48847,#48848,#48849,#48850,#48851,#48852,#48853,
#48854,#48855,#48856,#48857,#48858,#48859,#48860,#48861,#48862,#48863,#48864,
#48865,#48866,#48867,#48868,#48869,#48870,#48871,#48872,#48873,#48874,#48875,
#48876,#48877,#48878,#48879,#48880,#48881,#48882,#48883,#48884,#48885,#48886,
#48887,#48888,#48889,#48890,#48891,#48892,#48893,#48894,#48895,#48896,#48897,
#48898,#48899,#48900,#48901,#48902,#48903,#48904,#48905,#48906,#48907,#48908,
#48909,#48910,#48911,#48912,#48913,#48914,#48915,#48916,#48917,#48918,#48919,
#48920,#48921,#48922),.UNSPECIFIED.,.F.,.F.,(4,3,3,3,3,3,3,3,3,3,3,3,3,
3,3,3,3,3,3,3,3,3,3,3,3,3,3,3,4),(-0.276631791712734,-0.267261996455995,
-0.252638662205674,-0.246312363040928,-0.242068560323364,-0.226785633742753,
-0.215996016587511,-0.212143694358535,-0.209338885277652,-0.193398609351846,
-0.177535603971384,-0.168251432662936,-0.162618668425473,-0.159671082387916,
-0.143143715898125,-0.140398918737591,-0.124353701295378,-0.116139469058262,
-0.111126710163082,-0.108002044299551,-0.0915419859739776,-0.0746030552852902,
-0.0650265681318801,-0.0590759629246126,-0.0560748708216743,-0.0528975941021778,
-0.0354276289851714,-0.0177138144925857,0.),.UNSPECIFIED.);
#637=B_SPLINE_CURVE_WITH_KNOTS('',3,(#49224,#49225,#49226,#49227),
 .UNSPECIFIED.,.F.,.F.,(4,4),(-0.026145581273058,0.),.UNSPECIFIED.);
#638=B_SPLINE_CURVE_WITH_KNOTS('',3,(#49228,#49229,#49230,#49231,#49232,
#49233,#49234,#49235,#49236,#49237,#49238,#49239,#49240,#49241,#49242,#49243,
#49244,#49245,#49246,#49247,#49248,#49249,#49250,#49251,#49252,#49253,#49254,
#49255,#49256,#49257,#49258,#49259,#49260,#49261,#49262,#49263,#49264,#49265,
#49266,#49267,#49268,#49269,#49270,#49271,#49272,#49273,#49274,#49275,#49276,
#49277,#49278,#49279,#49280,#49281,#49282,#49283,#49284,#49285,#49286,#49287,
#49288,#49289,#49290,#49291,#49292,#49293,#49294,#49295,#49296,#49297,#49298,
#49299,#49300,#49301,#49302,#49303,#49304,#49305,#49306,#49307,#49308,#49309),
 .UNSPECIFIED.,.F.,.F.,(4,3,3,3,3,3,3,3,3,3,3,3,3,3,3,3,3,3,3,3,3,3,3,3,
3,3,3,4),(-0.276631791712739,-0.267261996456003,-0.252555963292598,-0.246312378453633,
-0.242068565443008,-0.226785642088753,-0.21599602390543,-0.212143486540232,
-0.209338645876512,-0.193538398420259,-0.177483821941212,-0.168251250557197,
-0.162618632421756,-0.159671067091488,-0.143143700304065,-0.140398918737599,
-0.124285864682194,-0.111126709917846,-0.108002044065338,-0.0915419879252078,
-0.0746030592382071,-0.0650265697785082,-0.0590759664797879,-0.0560748754887655,
-0.0528975949305316,-0.035427631110524,-0.017713815555262,0.),
 .UNSPECIFIED.);
#639=B_SPLINE_CURVE_WITH_KNOTS('',3,(#49314,#49315,#49316,#49317,#49318,
#49319,#49320,#49321,#49322,#49323,#49324,#49325,#49326,#49327,#49328,#49329,
#49330,#49331,#49332,#49333,#49334,#49335,#49336,#49337,#49338,#49339,#49340,
#49341,#49342,#49343,#49344,#49345,#49346,#49347,#49348,#49349,#49350,#49351,
#49352,#49353,#49354,#49355,#49356,#49357,#49358,#49359,#49360,#49361,#49362,
#49363,#49364,#49365,#49366,#49367,#49368,#49369,#49370,#49371,#49372,#49373,
#49374,#49375,#49376,#49377,#49378,#49379,#49380,#49381,#49382,#49383,#49384,
#49385,#49386,#49387,#49388,#49389,#49390,#49391,#49392,#49393,#49394,#49395),
 .UNSPECIFIED.,.F.,.F.,(4,3,3,3,3,3,3,3,3,3,3,3,3,3,3,3,3,3,3,3,3,3,3,3,
3,3,3,4),(-0.272733710415022,-0.26393309105054,-0.246451516153048,-0.23709784863092,
-0.233168130330458,-0.215966889594249,-0.204638177861954,-0.1994597979912,
-0.196214581144175,-0.179475255804651,-0.163134888932547,-0.153693392769608,
-0.149077802760023,-0.145944936327465,-0.130068057058006,-0.125340569601517,
-0.108707156583976,-0.101071231081186,-0.095699368520472,-0.0926136207771124,
-0.0768306446800761,-0.0611558835737404,-0.0532966012025288,-0.0475071908126714,
-0.0447088840235041,-0.0296023913127002,-0.0148011956563501,0.),
 .UNSPECIFIED.);
#640=B_SPLINE_CURVE_WITH_KNOTS('',3,(#49697,#49698,#49699,#49700),
 .UNSPECIFIED.,.F.,.F.,(4,4),(-0.0264538357708102,0.),.UNSPECIFIED.);
#897=B_SPLINE_SURFACE_WITH_KNOTS('',3,3,((#48924,#48925,#48926,#48927,#48928,
#48929,#48930,#48931,#48932,#48933,#48934,#48935,#48936,#48937,#48938,#48939,
#48940,#48941,#48942,#48943,#48944,#48945,#48946,#48947,#48948,#48949,#48950,
#48951,#48952,#48953,#48954,#48955,#48956,#48957,#48958,#48959,#48960,#48961,
#48962,#48963,#48964,#48965,#48966,#48967,#48968,#48969,#48970,#48971,#48972,
#48973,#48974,#48975,#48976,#48977,#48978,#48979,#48980,#48981,#48982,#48983,
#48984,#48985,#48986,#48987,#48988,#48989,#48990,#48991,#48992,#48993,#48994,
#48995,#48996,#48997,#48998),(#48999,#49000,#49001,#49002,#49003,#49004,
#49005,#49006,#49007,#49008,#49009,#49010,#49011,#49012,#49013,#49014,#49015,
#49016,#49017,#49018,#49019,#49020,#49021,#49022,#49023,#49024,#49025,#49026,
#49027,#49028,#49029,#49030,#49031,#49032,#49033,#49034,#49035,#49036,#49037,
#49038,#49039,#49040,#49041,#49042,#49043,#49044,#49045,#49046,#49047,#49048,
#49049,#49050,#49051,#49052,#49053,#49054,#49055,#49056,#49057,#49058,#49059,
#49060,#49061,#49062,#49063,#49064,#49065,#49066,#49067,#49068,#49069,#49070,
#49071,#49072,#49073),(#49074,#49075,#49076,#49077,#49078,#49079,#49080,
#49081,#49082,#49083,#49084,#49085,#49086,#49087,#49088,#49089,#49090,#49091,
#49092,#49093,#49094,#49095,#49096,#49097,#49098,#49099,#49100,#49101,#49102,
#49103,#49104,#49105,#49106,#49107,#49108,#49109,#49110,#49111,#49112,#49113,
#49114,#49115,#49116,#49117,#49118,#49119,#49120,#49121,#49122,#49123,#49124,
#49125,#49126,#49127,#49128,#49129,#49130,#49131,#49132,#49133,#49134,#49135,
#49136,#49137,#49138,#49139,#49140,#49141,#49142,#49143,#49144,#49145,#49146,
#49147,#49148),(#49149,#49150,#49151,#49152,#49153,#49154,#49155,#49156,
#49157,#49158,#49159,#49160,#49161,#49162,#49163,#49164,#49165,#49166,#49167,
#49168,#49169,#49170,#49171,#49172,#49173,#49174,#49175,#49176,#49177,#49178,
#49179,#49180,#49181,#49182,#49183,#49184,#49185,#49186,#49187,#49188,#49189,
#49190,#49191,#49192,#49193,#49194,#49195,#49196,#49197,#49198,#49199,#49200,
#49201,#49202,#49203,#49204,#49205,#49206,#49207,#49208,#49209,#49210,#49211,
#49212,#49213,#49214,#49215,#49216,#49217,#49218,#49219,#49220,#49221,#49222,
#49223)),.UNSPECIFIED.,.F.,.F.,.F.,(4,4),(4,1,1,1,1,1,1,1,1,1,1,1,1,1,1,
1,1,1,1,1,1,1,1,1,1,1,1,1,1,1,1,1,1,1,1,1,1,1,1,1,1,1,1,1,1,1,1,1,1,1,1,
1,1,1,1,1,1,1,1,1,1,1,1,1,1,1,1,1,1,1,1,1,4),(-0.000245115248125111,0.0332154979215098),
(8.30203615430821,9.29948795407228,10.2969397538364,11.2943915536004,12.2918433533645,
13.2892951531286,14.2867469528926,15.2841987526567,16.2816505524208,17.2791023521849,
18.2765541519489,19.274005951713,20.2714577514771,21.2689095512411,22.2663613510052,
23.2638131507693,24.2612649505334,25.2587167502974,26.2561685500615,27.2536203498256,
28.2510721495896,29.2485239493537,30.2459757491178,31.2434275488818,32.2408793486459,
33.23833114841,34.2357829481741,35.2332347479381,36.2306865477022,37.2281383474663,
38.2255901472303,39.2230419469944,40.2204937467585,41.2179455465226,42.2153973462866,
43.2128491460507,44.2103009458148,45.2077527455788,46.2052045453429,47.202656345107,
48.2001081448711,49.1975599446351,50.1950117443992,51.1924635441633,52.1899153439273,
53.1873671436914,54.1848189434555,55.1822707432196,56.1797225429836,57.1771743427477,
58.1746261425118,59.1720779422758,60.1695297420399,61.166981541804,62.1644333415681,
63.1618851413321,64.1593369410962,65.1567887408603,66.1542405406243,67.1516923403884,
68.1491441401525,69.1465959399166,70.1440477396806,71.1414995394447,72.1389513392088,
73.1364031389728,74.1338549387369,75.131306738501,76.128758538265,77.1262103380291,
78.1236621377932,79.1211139375573,80.1188108525694),.UNSPECIFIED.);
#898=B_SPLINE_SURFACE_WITH_KNOTS('',3,3,((#49397,#49398,#49399,#49400,#49401,
#49402,#49403,#49404,#49405,#49406,#49407,#49408,#49409,#49410,#49411,#49412,
#49413,#49414,#49415,#49416,#49417,#49418,#49419,#49420,#49421,#49422,#49423,
#49424,#49425,#49426,#49427,#49428,#49429,#49430,#49431,#49432,#49433,#49434,
#49435,#49436,#49437,#49438,#49439,#49440,#49441,#49442,#49443,#49444,#49445,
#49446,#49447,#49448,#49449,#49450,#49451,#49452,#49453,#49454,#49455,#49456,
#49457,#49458,#49459,#49460,#49461,#49462,#49463,#49464,#49465,#49466,#49467,
#49468,#49469,#49470,#49471),(#49472,#49473,#49474,#49475,#49476,#49477,
#49478,#49479,#49480,#49481,#49482,#49483,#49484,#49485,#49486,#49487,#49488,
#49489,#49490,#49491,#49492,#49493,#49494,#49495,#49496,#49497,#49498,#49499,
#49500,#49501,#49502,#49503,#49504,#49505,#49506,#49507,#49508,#49509,#49510,
#49511,#49512,#49513,#49514,#49515,#49516,#49517,#49518,#49519,#49520,#49521,
#49522,#49523,#49524,#49525,#49526,#49527,#49528,#49529,#49530,#49531,#49532,
#49533,#49534,#49535,#49536,#49537,#49538,#49539,#49540,#49541,#49542,#49543,
#49544,#49545,#49546),(#49547,#49548,#49549,#49550,#49551,#49552,#49553,
#49554,#49555,#49556,#49557,#49558,#49559,#49560,#49561,#49562,#49563,#49564,
#49565,#49566,#49567,#49568,#49569,#49570,#49571,#49572,#49573,#49574,#49575,
#49576,#49577,#49578,#49579,#49580,#49581,#49582,#49583,#49584,#49585,#49586,
#49587,#49588,#49589,#49590,#49591,#49592,#49593,#49594,#49595,#49596,#49597,
#49598,#49599,#49600,#49601,#49602,#49603,#49604,#49605,#49606,#49607,#49608,
#49609,#49610,#49611,#49612,#49613,#49614,#49615,#49616,#49617,#49618,#49619,
#49620,#49621),(#49622,#49623,#49624,#49625,#49626,#49627,#49628,#49629,
#49630,#49631,#49632,#49633,#49634,#49635,#49636,#49637,#49638,#49639,#49640,
#49641,#49642,#49643,#49644,#49645,#49646,#49647,#49648,#49649,#49650,#49651,
#49652,#49653,#49654,#49655,#49656,#49657,#49658,#49659,#49660,#49661,#49662,
#49663,#49664,#49665,#49666,#49667,#49668,#49669,#49670,#49671,#49672,#49673,
#49674,#49675,#49676,#49677,#49678,#49679,#49680,#49681,#49682,#49683,#49684,
#49685,#49686,#49687,#49688,#49689,#49690,#49691,#49692,#49693,#49694,#49695,
#49696)),.UNSPECIFIED.,.F.,.F.,.F.,(4,4),(4,1,1,1,1,1,1,1,1,1,1,1,1,1,1,
1,1,1,1,1,1,1,1,1,1,1,1,1,1,1,1,1,1,1,1,1,1,1,1,1,1,1,1,1,1,1,1,1,1,1,1,
1,1,1,1,1,1,1,1,1,1,1,1,1,1,1,1,1,1,1,1,1,4),(-0.000210453224954951,0.0332406947647496),
(11.6156946206196,12.6133915472643,13.6108433470284,14.6082951467925,15.6057469465565,
16.6031987463206,17.6006505460847,18.5981023458487,19.5955541456128,20.5930059453769,
21.590457745141,22.587909544905,23.5853613446691,24.5828131444332,25.5802649441972,
26.5777167439613,27.5751685437254,28.5726203434894,29.5700721432535,30.5675239430176,
31.5649757427817,32.5624275425457,33.5598793423098,34.5573311420739,35.5547829418379,
36.552234741602,37.5496865413661,38.5471383411302,39.5445901408942,40.5420419406583,
41.5394937404224,42.5369455401864,43.5343973399505,44.5318491397146,45.5293009394787,
46.5267527392427,47.5242045390068,48.5216563387709,49.5191081385349,50.516559938299,
51.5140117380631,52.5114635378272,53.5089153375912,54.5063671373553,55.5038189371194,
56.5012707368834,57.4987225366475,58.4961743364116,59.4936261361756,60.4910779359397,
61.4885297357038,62.4859815354679,63.4834333352319,64.480885134996,65.4783369347601,
66.4757887345241,67.4732405342882,68.4706923340523,69.4681441338164,70.4655959335804,
71.4630477333445,72.4604995331086,73.4579513328726,74.4554031326367,75.4528549324008,
76.4503067321649,77.4477585319289,78.445210331693,79.4426621314571,80.4401139312211,
81.4375657309852,82.4350175307493,83.4324693305134),.UNSPECIFIED.);
#909=SHAPE_REPRESENTATION_RELATIONSHIP('SRR','None',#83304,#923);
#923=ADVANCED_BREP_SHAPE_REPRESENTATION('',(#951),#83209);
#937=STYLED_ITEM('',(#83383),#951);
#951=MANIFOLD_SOLID_BREP('Body1',#26933);
#1017=FACE_BOUND('',#4136,.T.);
#1018=FACE_BOUND('',#4251,.T.);
#1284=PLANE('',#27624);
#1285=PLANE('',#27627);
#1286=PLANE('',#27633);
#1287=PLANE('',#27637);
#1288=PLANE('',#27638);
#1289=PLANE('',#27639);
#1290=PLANE('',#27641);
#1291=PLANE('',#27717);
#1292=PLANE('',#27718);
#1293=PLANE('',#27719);
#1294=PLANE('',#27720);
#1295=PLANE('',#27721);
#1296=PLANE('',#27722);
#1297=PLANE('',#27723);
#1298=PLANE('',#27724);
#1299=PLANE('',#27725);
#1300=PLANE('',#27726);
#1301=PLANE('',#27727);
#1302=PLANE('',#27728);
#1303=PLANE('',#27729);
#1304=PLANE('',#27730);
#1305=PLANE('',#27731);
#1306=PLANE('',#27732);
#1307=PLANE('',#27733);
#1308=PLANE('',#27734);
#1309=PLANE('',#27735);
#1310=PLANE('',#27736);
#1311=PLANE('',#27737);
#1312=PLANE('',#27738);
#1313=PLANE('',#27739);
#1314=PLANE('',#27740);
#1315=PLANE('',#27741);
#1316=PLANE('',#27742);
#1317=PLANE('',#27743);
#1318=PLANE('',#27744);
#1319=PLANE('',#27745);
#1320=PLANE('',#27746);
#1321=PLANE('',#27747);
#1322=PLANE('',#27748);
#1323=PLANE('',#27749);
#1324=PLANE('',#27750);
#1325=PLANE('',#27751);
#1326=PLANE('',#27752);
#1327=PLANE('',#27753);
#1328=PLANE('',#27754);
#1329=PLANE('',#27755);
#1330=PLANE('',#27756);
#1331=PLANE('',#27757);
#1332=PLANE('',#27758);
#1333=PLANE('',#27759);
#1334=PLANE('',#27760);
#1335=PLANE('',#27761);
#1336=PLANE('',#27762);
#1337=PLANE('',#27763);
#1338=PLANE('',#27764);
#1339=PLANE('',#27765);
#1340=PLANE('',#27766);
#1341=PLANE('',#27767);
#1342=PLANE('',#27768);
#1343=PLANE('',#27769);
#1344=PLANE('',#27770);
#1345=PLANE('',#27771);
#1346=PLANE('',#27772);
#1347=PLANE('',#27773);
#1348=PLANE('',#27774);
#1349=PLANE('',#27775);
#1350=PLANE('',#27776);
#1351=PLANE('',#27777);
#1352=PLANE('',#27778);
#1353=PLANE('',#27779);
#1354=PLANE('',#27780);
#1355=PLANE('',#27781);
#1356=PLANE('',#27782);
#1357=PLANE('',#27783);
#1358=PLANE('',#27784);
#1359=PLANE('',#27785);
#1360=PLANE('',#27786);
#1361=PLANE('',#27787);
#1362=PLANE('',#27788);
#1363=PLANE('',#27789);
#1364=PLANE('',#27790);
#1365=PLANE('',#27791);
#1366=PLANE('',#27792);
#1367=PLANE('',#27793);
#1368=PLANE('',#27794);
#1369=PLANE('',#27795);
#1370=PLANE('',#27796);
#1371=PLANE('',#27797);
#1372=PLANE('',#27798);
#1373=PLANE('',#27799);
#1374=PLANE('',#27800);
#1375=PLANE('',#27801);
#1376=PLANE('',#27802);
#1377=PLANE('',#27803);
#1378=PLANE('',#27804);
#1379=PLANE('',#27805);
#1380=PLANE('',#27806);
#1381=PLANE('',#27807);
#1382=PLANE('',#27808);
#1383=PLANE('',#27809);
#1384=PLANE('',#27810);
#1385=PLANE('',#27811);
#1386=PLANE('',#27812);
#1387=PLANE('',#27813);
#1388=PLANE('',#27814);
#1389=PLANE('',#27815);
#1390=PLANE('',#27816);
#1391=PLANE('',#27817);
#1392=PLANE('',#27818);
#1393=PLANE('',#27819);
#1394=PLANE('',#27820);
#1395=PLANE('',#27821);
#1396=PLANE('',#27826);
#1397=PLANE('',#27847);
#1398=PLANE('',#27848);
#1399=PLANE('',#27849);
#1400=PLANE('',#27850);
#1401=PLANE('',#27851);
#1402=PLANE('',#27852);
#1403=PLANE('',#27853);
#1404=PLANE('',#27854);
#1405=PLANE('',#27855);
#1406=PLANE('',#27856);
#1407=PLANE('',#27858);
#1408=PLANE('',#27860);
#1409=PLANE('',#27862);
#1410=PLANE('',#27864);
#1411=PLANE('',#27866);
#1412=PLANE('',#27869);
#1413=PLANE('',#27870);
#1414=PLANE('',#27871);
#2228=CYLINDRICAL_SURFACE('',#27596,1.17775);
#2229=CYLINDRICAL_SURFACE('',#27598,1.17775);
#2230=CYLINDRICAL_SURFACE('',#27599,1.17775);
#2231=CYLINDRICAL_SURFACE('',#27600,1.17775);
#2232=CYLINDRICAL_SURFACE('',#27601,1.17775);
#2233=CYLINDRICAL_SURFACE('',#27602,1.17775);
#2234=CYLINDRICAL_SURFACE('',#27603,1.17775);
#2235=CYLINDRICAL_SURFACE('',#27604,1.17775);
#2236=CYLINDRICAL_SURFACE('',#27605,1.17775);
#2237=CYLINDRICAL_SURFACE('',#27606,1.17775);
#2238=CYLINDRICAL_SURFACE('',#27607,1.17775);
#2239=CYLINDRICAL_SURFACE('',#27608,1.4635);
#2240=CYLINDRICAL_SURFACE('',#27610,1.4635);
#2241=CYLINDRICAL_SURFACE('',#27611,1.4635);
#2242=CYLINDRICAL_SURFACE('',#27612,1.4635);
#2243=CYLINDRICAL_SURFACE('',#27613,1.4635);
#2244=CYLINDRICAL_SURFACE('',#27614,1.4635);
#2245=CYLINDRICAL_SURFACE('',#27615,1.4635);
#2246=CYLINDRICAL_SURFACE('',#27616,1.4635);
#2247=CYLINDRICAL_SURFACE('',#27617,1.4635);
#2248=CYLINDRICAL_SURFACE('',#27618,1.4635);
#2249=CYLINDRICAL_SURFACE('',#27619,1.4635);
#2250=CYLINDRICAL_SURFACE('',#27620,1.4635);
#2251=CYLINDRICAL_SURFACE('',#27622,1.17775);
#2252=CYLINDRICAL_SURFACE('',#27642,2.75);
#2253=CYLINDRICAL_SURFACE('',#27835,1.39337567297406);
#2254=CYLINDRICAL_SURFACE('',#27837,1.39337567297406);
#2255=CYLINDRICAL_SURFACE('',#27839,1.39337567297406);
#2256=CYLINDRICAL_SURFACE('',#27841,1.39337567297406);
#2257=CYLINDRICAL_SURFACE('',#27843,1.39337567297406);
#2258=CYLINDRICAL_SURFACE('',#27845,1.39337567297406);
#2671=FACE_OUTER_BOUND('',#4106,.T.);
#2672=FACE_OUTER_BOUND('',#4107,.T.);
#2673=FACE_OUTER_BOUND('',#4108,.T.);
#2674=FACE_OUTER_BOUND('',#4109,.T.);
#2675=FACE_OUTER_BOUND('',#4110,.T.);
#2676=FACE_OUTER_BOUND('',#4111,.T.);
#2677=FACE_OUTER_BOUND('',#4112,.T.);
#2678=FACE_OUTER_BOUND('',#4113,.T.);
#2679=FACE_OUTER_BOUND('',#4114,.T.);
#2680=FACE_OUTER_BOUND('',#4115,.T.);
#2681=FACE_OUTER_BOUND('',#4116,.T.);
#2682=FACE_OUTER_BOUND('',#4117,.T.);
#2683=FACE_OUTER_BOUND('',#4118,.T.);
#2684=FACE_OUTER_BOUND('',#4119,.T.);
#2685=FACE_OUTER_BOUND('',#4120,.T.);
#2686=FACE_OUTER_BOUND('',#4121,.T.);
#2687=FACE_OUTER_BOUND('',#4122,.T.);
#2688=FACE_OUTER_BOUND('',#4123,.T.);
#2689=FACE_OUTER_BOUND('',#4124,.T.);
#2690=FACE_OUTER_BOUND('',#4125,.T.);
#2691=FACE_OUTER_BOUND('',#4126,.T.);
#2692=FACE_OUTER_BOUND('',#4127,.T.);
#2693=FACE_OUTER_BOUND('',#4128,.T.);
#2694=FACE_OUTER_BOUND('',#4129,.T.);
#2695=FACE_OUTER_BOUND('',#4130,.T.);
#2696=FACE_OUTER_BOUND('',#4131,.T.);
#2697=FACE_OUTER_BOUND('',#4132,.T.);
#2698=FACE_OUTER_BOUND('',#4133,.T.);
#2699=FACE_OUTER_BOUND('',#4134,.T.);
#2700=FACE_OUTER_BOUND('',#4135,.T.);
#2701=FACE_OUTER_BOUND('',#4137,.T.);
#2702=FACE_OUTER_BOUND('',#4138,.T.);
#2703=FACE_OUTER_BOUND('',#4139,.T.);
#2704=FACE_OUTER_BOUND('',#4140,.T.);
#2705=FACE_OUTER_BOUND('',#4141,.T.);
#2706=FACE_OUTER_BOUND('',#4142,.T.);
#2707=FACE_OUTER_BOUND('',#4143,.T.);
#2708=FACE_OUTER_BOUND('',#4144,.T.);
#2709=FACE_OUTER_BOUND('',#4145,.T.);
#2710=FACE_OUTER_BOUND('',#4146,.T.);
#2711=FACE_OUTER_BOUND('',#4147,.T.);
#2712=FACE_OUTER_BOUND('',#4148,.T.);
#2713=FACE_OUTER_BOUND('',#4149,.T.);
#2714=FACE_OUTER_BOUND('',#4150,.T.);
#2715=FACE_OUTER_BOUND('',#4151,.T.);
#2716=FACE_OUTER_BOUND('',#4152,.T.);
#2717=FACE_OUTER_BOUND('',#4153,.T.);
#2718=FACE_OUTER_BOUND('',#4154,.T.);
#2719=FACE_OUTER_BOUND('',#4155,.T.);
#2720=FACE_OUTER_BOUND('',#4156,.T.);
#2721=FACE_OUTER_BOUND('',#4157,.T.);
#2722=FACE_OUTER_BOUND('',#4158,.T.);
#2723=FACE_OUTER_BOUND('',#4159,.T.);
#2724=FACE_OUTER_BOUND('',#4160,.T.);
#2725=FACE_OUTER_BOUND('',#4161,.T.);
#2726=FACE_OUTER_BOUND('',#4162,.T.);
#2727=FACE_OUTER_BOUND('',#4163,.T.);
#2728=FACE_OUTER_BOUND('',#4164,.T.);
#2729=FACE_OUTER_BOUND('',#4165,.T.);
#2730=FACE_OUTER_BOUND('',#4166,.T.);
#2731=FACE_OUTER_BOUND('',#4167,.T.);
#2732=FACE_OUTER_BOUND('',#4168,.T.);
#2733=FACE_OUTER_BOUND('',#4169,.T.);
#2734=FACE_OUTER_BOUND('',#4170,.T.);
#2735=FACE_OUTER_BOUND('',#4171,.T.);
#2736=FACE_OUTER_BOUND('',#4172,.T.);
#2737=FACE_OUTER_BOUND('',#4173,.T.);
#2738=FACE_OUTER_BOUND('',#4174,.T.);
#2739=FACE_OUTER_BOUND('',#4175,.T.);
#2740=FACE_OUTER_BOUND('',#4176,.T.);
#2741=FACE_OUTER_BOUND('',#4177,.T.);
#2742=FACE_OUTER_BOUND('',#4178,.T.);
#2743=FACE_OUTER_BOUND('',#4179,.T.);
#2744=FACE_OUTER_BOUND('',#4180,.T.);
#2745=FACE_OUTER_BOUND('',#4181,.T.);
#2746=FACE_OUTER_BOUND('',#4182,.T.);
#2747=FACE_OUTER_BOUND('',#4183,.T.);
#2748=FACE_OUTER_BOUND('',#4184,.T.);
#2749=FACE_OUTER_BOUND('',#4185,.T.);
#2750=FACE_OUTER_BOUND('',#4186,.T.);
#2751=FACE_OUTER_BOUND('',#4187,.T.);
#2752=FACE_OUTER_BOUND('',#4188,.T.);
#2753=FACE_OUTER_BOUND('',#4189,.T.);
#2754=FACE_OUTER_BOUND('',#4190,.T.);
#2755=FACE_OUTER_BOUND('',#4191,.T.);
#2756=FACE_OUTER_BOUND('',#4192,.T.);
#2757=FACE_OUTER_BOUND('',#4193,.T.);
#2758=FACE_OUTER_BOUND('',#4194,.T.);
#2759=FACE_OUTER_BOUND('',#4195,.T.);
#2760=FACE_OUTER_BOUND('',#4196,.T.);
#2761=FACE_OUTER_BOUND('',#4197,.T.);
#2762=FACE_OUTER_BOUND('',#4198,.T.);
#2763=FACE_OUTER_BOUND('',#4199,.T.);
#2764=FACE_OUTER_BOUND('',#4200,.T.);
#2765=FACE_OUTER_BOUND('',#4201,.T.);
#2766=FACE_OUTER_BOUND('',#4202,.T.);
#2767=FACE_OUTER_BOUND('',#4203,.T.);
#2768=FACE_OUTER_BOUND('',#4204,.T.);
#2769=FACE_OUTER_BOUND('',#4205,.T.);
#2770=FACE_OUTER_BOUND('',#4206,.T.);
#2771=FACE_OUTER_BOUND('',#4207,.T.);
#2772=FACE_OUTER_BOUND('',#4208,.T.);
#2773=FACE_OUTER_BOUND('',#4209,.T.);
#2774=FACE_OUTER_BOUND('',#4210,.T.);
#2775=FACE_OUTER_BOUND('',#4211,.T.);
#2776=FACE_OUTER_BOUND('',#4212,.T.);
#2777=FACE_OUTER_BOUND('',#4213,.T.);
#2778=FACE_OUTER_BOUND('',#4214,.T.);
#2779=FACE_OUTER_BOUND('',#4215,.T.);
#2780=FACE_OUTER_BOUND('',#4216,.T.);
#2781=FACE_OUTER_BOUND('',#4217,.T.);
#2782=FACE_OUTER_BOUND('',#4218,.T.);
#2783=FACE_OUTER_BOUND('',#4219,.T.);
#2784=FACE_OUTER_BOUND('',#4220,.T.);
#2785=FACE_OUTER_BOUND('',#4221,.T.);
#2786=FACE_OUTER_BOUND('',#4222,.T.);
#2787=FACE_OUTER_BOUND('',#4223,.T.);
#2788=FACE_OUTER_BOUND('',#4224,.T.);
#2789=FACE_OUTER_BOUND('',#4225,.T.);
#2790=FACE_OUTER_BOUND('',#4226,.T.);
#2791=FACE_OUTER_BOUND('',#4227,.T.);
#2792=FACE_OUTER_BOUND('',#4228,.T.);
#2793=FACE_OUTER_BOUND('',#4229,.T.);
#2794=FACE_OUTER_BOUND('',#4230,.T.);
#2795=FACE_OUTER_BOUND('',#4231,.T.);
#2796=FACE_OUTER_BOUND('',#4232,.T.);
#2797=FACE_OUTER_BOUND('',#4233,.T.);
#2798=FACE_OUTER_BOUND('',#4234,.T.);
#2799=FACE_OUTER_BOUND('',#4235,.T.);
#2800=FACE_OUTER_BOUND('',#4236,.T.);
#2801=FACE_OUTER_BOUND('',#4237,.T.);
#2802=FACE_OUTER_BOUND('',#4238,.T.);
#2803=FACE_OUTER_BOUND('',#4239,.T.);
#2804=FACE_OUTER_BOUND('',#4240,.T.);
#2805=FACE_OUTER_BOUND('',#4241,.T.);
#2806=FACE_OUTER_BOUND('',#4242,.T.);
#2807=FACE_OUTER_BOUND('',#4243,.T.);
#2808=FACE_OUTER_BOUND('',#4244,.T.);
#2809=FACE_OUTER_BOUND('',#4245,.T.);
#2810=FACE_OUTER_BOUND('',#4246,.T.);
#2811=FACE_OUTER_BOUND('',#4247,.T.);
#2812=FACE_OUTER_BOUND('',#4248,.T.);
#2813=FACE_OUTER_BOUND('',#4249,.T.);
#2814=FACE_OUTER_BOUND('',#4250,.T.);
#2815=FACE_OUTER_BOUND('',#4252,.T.);
#2816=FACE_OUTER_BOUND('',#4253,.T.);
#2817=FACE_OUTER_BOUND('',#4254,.T.);
#2818=FACE_OUTER_BOUND('',#4255,.T.);
#2819=FACE_OUTER_BOUND('',#4256,.T.);
#2820=FACE_OUTER_BOUND('',#4257,.T.);
#2821=FACE_OUTER_BOUND('',#4258,.T.);
#2822=FACE_OUTER_BOUND('',#4259,.T.);
#2823=FACE_OUTER_BOUND('',#4260,.T.);
#2824=FACE_OUTER_BOUND('',#4261,.T.);
#2825=FACE_OUTER_BOUND('',#4262,.T.);
#2826=FACE_OUTER_BOUND('',#4263,.T.);
#2827=FACE_OUTER_BOUND('',#4264,.T.);
#2828=FACE_OUTER_BOUND('',#4265,.T.);
#2829=FACE_OUTER_BOUND('',#4266,.T.);
#2830=FACE_OUTER_BOUND('',#4267,.T.);
#2831=FACE_OUTER_BOUND('',#4268,.T.);
#2832=FACE_OUTER_BOUND('',#4269,.T.);
#2833=FACE_OUTER_BOUND('',#4270,.T.);
#2834=FACE_OUTER_BOUND('',#4271,.T.);
#2835=FACE_OUTER_BOUND('',#4272,.T.);
#2836=FACE_OUTER_BOUND('',#4273,.T.);
#2837=FACE_OUTER_BOUND('',#4274,.T.);
#2838=FACE_OUTER_BOUND('',#4275,.T.);
#2839=FACE_OUTER_BOUND('',#4276,.T.);
#2840=FACE_OUTER_BOUND('',#4277,.T.);
#4106=EDGE_LOOP('',(#19212,#19213,#19214,#19215));
#4107=EDGE_LOOP('',(#19216,#19217,#19218,#19219,#19220,#19221));
#4108=EDGE_LOOP('',(#19222,#19223,#19224,#19225,#19226));
#4109=EDGE_LOOP('',(#19227,#19228,#19229,#19230,#19231,#19232));
#4110=EDGE_LOOP('',(#19233,#19234,#19235,#19236));
#4111=EDGE_LOOP('',(#19237,#19238,#19239,#19240,#19241,#19242));
#4112=EDGE_LOOP('',(#19243,#19244,#19245,#19246));
#4113=EDGE_LOOP('',(#19247,#19248,#19249,#19250,#19251,#19252));
#4114=EDGE_LOOP('',(#19253,#19254,#19255,#19256,#19257));
#4115=EDGE_LOOP('',(#19258,#19259,#19260,#19261,#19262));
#4116=EDGE_LOOP('',(#19263,#19264,#19265,#19266,#19267,#19268));
#4117=EDGE_LOOP('',(#19269,#19270,#19271,#19272));
#4118=EDGE_LOOP('',(#19273,#19274,#19275,#19276));
#4119=EDGE_LOOP('',(#19277,#19278,#19279,#19280));
#4120=EDGE_LOOP('',(#19281,#19282,#19283,#19284));
#4121=EDGE_LOOP('',(#19285,#19286,#19287,#19288));
#4122=EDGE_LOOP('',(#19289,#19290,#19291,#19292));
#4123=EDGE_LOOP('',(#19293,#19294,#19295,#19296));
#4124=EDGE_LOOP('',(#19297,#19298,#19299,#19300));
#4125=EDGE_LOOP('',(#19301,#19302,#19303,#19304));
#4126=EDGE_LOOP('',(#19305,#19306,#19307,#19308));
#4127=EDGE_LOOP('',(#19309,#19310,#19311,#19312));
#4128=EDGE_LOOP('',(#19313,#19314,#19315,#19316));
#4129=EDGE_LOOP('',(#19317,#19318,#19319,#19320,#19321,#19322));
#4130=EDGE_LOOP('',(#19323,#19324,#19325,#19326,#19327));
#4131=EDGE_LOOP('',(#19328,#19329,#19330,#19331,#19332,#19333,#19334,#19335,
#19336,#19337,#19338,#19339,#19340,#19341,#19342,#19343,#19344,#19345,#19346,
#19347,#19348,#19349,#19350,#19351,#19352,#19353,#19354,#19355,#19356,#19357,
#19358,#19359,#19360,#19361,#19362));
#4132=EDGE_LOOP('',(#19363,#19364,#19365,#19366,#19367));
#4133=EDGE_LOOP('',(#19368,#19369,#19370,#19371,#19372,#19373,#19374,#19375,
#19376,#19377,#19378,#19379,#19380,#19381,#19382,#19383,#19384,#19385,#19386,
#19387,#19388,#19389,#19390,#19391,#19392,#19393,#19394,#19395,#19396,#19397,
#19398,#19399,#19400,#19401));
#4134=EDGE_LOOP('',(#19402,#19403,#19404,#19405,#19406,#19407,#19408));
#4135=EDGE_LOOP('',(#19409));
#4136=EDGE_LOOP('',(#19410));
#4137=EDGE_LOOP('',(#19411,#19412,#19413,#19414,#19415,#19416,#19417));
#4138=EDGE_LOOP('',(#19418));
#4139=EDGE_LOOP('',(#19419,#19420,#19421,#19422));
#4140=EDGE_LOOP('',(#19423,#19424,#19425));
#4141=EDGE_LOOP('',(#19426,#19427,#19428,#19429));
#4142=EDGE_LOOP('',(#19430,#19431,#19432,#19433,#19434,#19435,#19436,#19437,
#19438,#19439,#19440,#19441,#19442,#19443,#19444,#19445,#19446,#19447,#19448,
#19449,#19450,#19451,#19452,#19453,#19454,#19455,#19456,#19457,#19458,#19459,
#19460,#19461,#19462,#19463,#19464,#19465,#19466,#19467,#19468,#19469,#19470,
#19471,#19472,#19473,#19474,#19475,#19476,#19477,#19478,#19479,#19480,#19481,
#19482,#19483,#19484,#19485,#19486,#19487,#19488,#19489,#19490,#19491,#19492,
#19493,#19494,#19495,#19496,#19497,#19498,#19499,#19500,#19501,#19502,#19503,
#19504,#19505,#19506,#19507,#19508,#19509,#19510,#19511,#19512,#19513,#19514,
#19515,#19516,#19517,#19518,#19519,#19520,#19521,#19522,#19523,#19524,#19525,
#19526,#19527,#19528,#19529,#19530,#19531,#19532,#19533,#19534,#19535,#19536,
#19537,#19538,#19539,#19540,#19541,#19542,#19543,#19544,#19545,#19546,#19547,
#19548,#19549,#19550,#19551,#19552,#19553,#19554,#19555,#19556,#19557,#19558,
#19559,#19560,#19561,#19562,#19563,#19564,#19565,#19566,#19567,#19568,#19569,
#19570,#19571,#19572,#19573,#19574,#19575,#19576,#19577,#19578));
#4143=EDGE_LOOP('',(#19579,#19580,#19581,#19582));
#4144=EDGE_LOOP('',(#19583,#19584,#19585));
#4145=EDGE_LOOP('',(#19586,#19587,#19588,#19589));
#4146=EDGE_LOOP('',(#19590,#19591,#19592,#19593));
#4147=EDGE_LOOP('',(#19594,#19595,#19596));
#4148=EDGE_LOOP('',(#19597,#19598,#19599,#19600));
#4149=EDGE_LOOP('',(#19601,#19602,#19603,#19604));
#4150=EDGE_LOOP('',(#19605,#19606,#19607));
#4151=EDGE_LOOP('',(#19608,#19609,#19610,#19611));
#4152=EDGE_LOOP('',(#19612,#19613,#19614,#19615));
#4153=EDGE_LOOP('',(#19616,#19617,#19618));
#4154=EDGE_LOOP('',(#19619,#19620,#19621,#19622));
#4155=EDGE_LOOP('',(#19623,#19624,#19625,#19626));
#4156=EDGE_LOOP('',(#19627,#19628,#19629));
#4157=EDGE_LOOP('',(#19630,#19631,#19632,#19633));
#4158=EDGE_LOOP('',(#19634,#19635,#19636,#19637));
#4159=EDGE_LOOP('',(#19638,#19639,#19640));
#4160=EDGE_LOOP('',(#19641,#19642,#19643,#19644));
#4161=EDGE_LOOP('',(#19645,#19646,#19647,#19648));
#4162=EDGE_LOOP('',(#19649,#19650,#19651));
#4163=EDGE_LOOP('',(#19652,#19653,#19654,#19655));
#4164=EDGE_LOOP('',(#19656,#19657,#19658,#19659));
#4165=EDGE_LOOP('',(#19660,#19661,#19662));
#4166=EDGE_LOOP('',(#19663,#19664,#19665,#19666));
#4167=EDGE_LOOP('',(#19667,#19668,#19669,#19670));
#4168=EDGE_LOOP('',(#19671,#19672,#19673));
#4169=EDGE_LOOP('',(#19674,#19675,#19676,#19677));
#4170=EDGE_LOOP('',(#19678,#19679,#19680,#19681));
#4171=EDGE_LOOP('',(#19682,#19683,#19684));
#4172=EDGE_LOOP('',(#19685,#19686,#19687,#19688));
#4173=EDGE_LOOP('',(#19689,#19690,#19691,#19692));
#4174=EDGE_LOOP('',(#19693,#19694,#19695));
#4175=EDGE_LOOP('',(#19696,#19697,#19698,#19699));
#4176=EDGE_LOOP('',(#19700,#19701,#19702,#19703));
#4177=EDGE_LOOP('',(#19704,#19705,#19706));
#4178=EDGE_LOOP('',(#19707,#19708,#19709,#19710));
#4179=EDGE_LOOP('',(#19711,#19712,#19713,#19714));
#4180=EDGE_LOOP('',(#19715,#19716,#19717));
#4181=EDGE_LOOP('',(#19718,#19719,#19720,#19721));
#4182=EDGE_LOOP('',(#19722,#19723,#19724,#19725));
#4183=EDGE_LOOP('',(#19726,#19727,#19728));
#4184=EDGE_LOOP('',(#19729,#19730,#19731,#19732));
#4185=EDGE_LOOP('',(#19733,#19734,#19735,#19736));
#4186=EDGE_LOOP('',(#19737,#19738,#19739));
#4187=EDGE_LOOP('',(#19740,#19741,#19742,#19743));
#4188=EDGE_LOOP('',(#19744,#19745,#19746,#19747));
#4189=EDGE_LOOP('',(#19748,#19749,#19750));
#4190=EDGE_LOOP('',(#19751,#19752,#19753,#19754));
#4191=EDGE_LOOP('',(#19755,#19756,#19757,#19758));
#4192=EDGE_LOOP('',(#19759,#19760,#19761,#19762));
#4193=EDGE_LOOP('',(#19763,#19764,#19765,#19766));
#4194=EDGE_LOOP('',(#19767,#19768,#19769,#19770));
#4195=EDGE_LOOP('',(#19771,#19772,#19773));
#4196=EDGE_LOOP('',(#19774,#19775,#19776,#19777));
#4197=EDGE_LOOP('',(#19778,#19779,#19780,#19781));
#4198=EDGE_LOOP('',(#19782,#19783,#19784));
#4199=EDGE_LOOP('',(#19785,#19786,#19787,#19788));
#4200=EDGE_LOOP('',(#19789,#19790,#19791,#19792));
#4201=EDGE_LOOP('',(#19793,#19794,#19795));
#4202=EDGE_LOOP('',(#19796,#19797,#19798,#19799));
#4203=EDGE_LOOP('',(#19800,#19801,#19802,#19803));
#4204=EDGE_LOOP('',(#19804,#19805,#19806));
#4205=EDGE_LOOP('',(#19807,#19808,#19809,#19810));
#4206=EDGE_LOOP('',(#19811,#19812,#19813,#19814));
#4207=EDGE_LOOP('',(#19815,#19816,#19817));
#4208=EDGE_LOOP('',(#19818,#19819,#19820,#19821));
#4209=EDGE_LOOP('',(#19822,#19823,#19824,#19825));
#4210=EDGE_LOOP('',(#19826,#19827,#19828));
#4211=EDGE_LOOP('',(#19829,#19830,#19831,#19832));
#4212=EDGE_LOOP('',(#19833,#19834,#19835,#19836));
#4213=EDGE_LOOP('',(#19837,#19838,#19839));
#4214=EDGE_LOOP('',(#19840,#19841,#19842,#19843));
#4215=EDGE_LOOP('',(#19844,#19845,#19846,#19847));
#4216=EDGE_LOOP('',(#19848,#19849,#19850));
#4217=EDGE_LOOP('',(#19851,#19852,#19853,#19854));
#4218=EDGE_LOOP('',(#19855,#19856,#19857,#19858));
#4219=EDGE_LOOP('',(#19859,#19860,#19861));
#4220=EDGE_LOOP('',(#19862,#19863,#19864,#19865));
#4221=EDGE_LOOP('',(#19866,#19867,#19868,#19869));
#4222=EDGE_LOOP('',(#19870,#19871,#19872));
#4223=EDGE_LOOP('',(#19873,#19874,#19875,#19876));
#4224=EDGE_LOOP('',(#19877,#19878,#19879,#19880));
#4225=EDGE_LOOP('',(#19881,#19882,#19883));
#4226=EDGE_LOOP('',(#19884,#19885,#19886,#19887));
#4227=EDGE_LOOP('',(#19888,#19889,#19890,#19891));
#4228=EDGE_LOOP('',(#19892,#19893,#19894));
#4229=EDGE_LOOP('',(#19895,#19896,#19897,#19898));
#4230=EDGE_LOOP('',(#19899,#19900,#19901,#19902));
#4231=EDGE_LOOP('',(#19903,#19904,#19905));
#4232=EDGE_LOOP('',(#19906,#19907,#19908,#19909));
#4233=EDGE_LOOP('',(#19910,#19911,#19912,#19913));
#4234=EDGE_LOOP('',(#19914,#19915,#19916));
#4235=EDGE_LOOP('',(#19917,#19918,#19919,#19920));
#4236=EDGE_LOOP('',(#19921,#19922,#19923,#19924));
#4237=EDGE_LOOP('',(#19925,#19926,#19927));
#4238=EDGE_LOOP('',(#19928,#19929,#19930,#19931));
#4239=EDGE_LOOP('',(#19932,#19933,#19934,#19935));
#4240=EDGE_LOOP('',(#19936,#19937,#19938));
#4241=EDGE_LOOP('',(#19939,#19940,#19941,#19942));
#4242=EDGE_LOOP('',(#19943,#19944,#19945,#19946));
#4243=EDGE_LOOP('',(#19947,#19948,#19949));
#4244=EDGE_LOOP('',(#19950,#19951,#19952,#19953));
#4245=EDGE_LOOP('',(#19954,#19955,#19956,#19957));
#4246=EDGE_LOOP('',(#19958,#19959,#19960));
#4247=EDGE_LOOP('',(#19961,#19962,#19963,#19964));
#4248=EDGE_LOOP('',(#19965,#19966,#19967,#19968,#19969));
#4249=EDGE_LOOP('',(#19970,#19971,#19972,#19973,#19974,#19975,#19976,#19977,
#19978,#19979,#19980,#19981,#19982,#19983,#19984,#19985,#19986,#19987,#19988,
#19989,#19990,#19991,#19992,#19993,#19994,#19995,#19996,#19997,#19998,#19999,
#20000,#20001,#20002,#20003,#20004,#20005,#20006,#20007,#20008,#20009,#20010,
#20011,#20012,#20013,#20014,#20015,#20016,#20017,#20018,#20019,#20020,#20021,
#20022,#20023,#20024,#20025,#20026,#20027,#20028,#20029,#20030,#20031,#20032,
#20033,#20034,#20035,#20036,#20037,#20038,#20039,#20040,#20041,#20042,#20043,
#20044,#20045,#20046,#20047,#20048,#20049,#20050,#20051,#20052,#20053,#20054,
#20055,#20056,#20057,#20058,#20059,#20060,#20061,#20062,#20063,#20064,#20065,
#20066,#20067,#20068,#20069,#20070,#20071,#20072,#20073,#20074,#20075,#20076,
#20077,#20078,#20079,#20080));
#4250=EDGE_LOOP('',(#20081));
#4251=EDGE_LOOP('',(#20082));
#4252=EDGE_LOOP('',(#20083,#20084,#20085,#20086,#20087,#20088,#20089,#20090,
#20091,#20092,#20093,#20094,#20095,#20096,#20097,#20098,#20099,#20100,#20101,
#20102,#20103));
#4253=EDGE_LOOP('',(#20104,#20105,#20106,#20107));
#4254=EDGE_LOOP('',(#20108,#20109,#20110,#20111));
#4255=EDGE_LOOP('',(#20112,#20113,#20114,#20115));
#4256=EDGE_LOOP('',(#20116,#20117,#20118,#20119));
#4257=EDGE_LOOP('',(#20120,#20121,#20122,#20123));
#4258=EDGE_LOOP('',(#20124,#20125,#20126,#20127));
#4259=EDGE_LOOP('',(#20128,#20129,#20130,#20131,#20132,#20133,#20134,#20135));
#4260=EDGE_LOOP('',(#20136,#20137,#20138,#20139,#20140,#20141,#20142,#20143));
#4261=EDGE_LOOP('',(#20144,#20145,#20146,#20147,#20148,#20149,#20150,#20151));
#4262=EDGE_LOOP('',(#20152,#20153));
#4263=EDGE_LOOP('',(#20154,#20155));
#4264=EDGE_LOOP('',(#20156,#20157));
#4265=EDGE_LOOP('',(#20158,#20159));
#4266=EDGE_LOOP('',(#20160,#20161));
#4267=EDGE_LOOP('',(#20162,#20163));
#4268=EDGE_LOOP('',(#20164,#20165));
#4269=EDGE_LOOP('',(#20166,#20167));
#4270=EDGE_LOOP('',(#20168,#20169));
#4271=EDGE_LOOP('',(#20170,#20171));
#4272=EDGE_LOOP('',(#20172,#20173));
#4273=EDGE_LOOP('',(#20174,#20175));
#4274=EDGE_LOOP('',(#20176,#20177,#20178,#20179,#20180,#20181,#20182,#20183));
#4275=EDGE_LOOP('',(#20184,#20185,#20186,#20187,#20188,#20189,#20190,#20191));
#4276=EDGE_LOOP('',(#20192,#20193,#20194,#20195,#20196,#20197,#20198,#20199));
#4277=EDGE_LOOP('',(#20200,#20201,#20202,#20203,#20204,#20205,#20206,#20207));
#5816=LINE('',#42117,#8327);
#5817=LINE('',#42282,#8328);
#5818=LINE('',#42526,#8329);
#5819=LINE('',#42839,#8330);
#5820=LINE('',#43222,#8331);
#5821=LINE('',#43578,#8332);
#5822=LINE('',#43954,#8333);
#5823=LINE('',#44326,#8334);
#5824=LINE('',#44574,#8335);
#5825=LINE('',#44903,#8336);
#5826=LINE('',#45264,#8337);
#5827=LINE('',#45507,#8338);
#5828=LINE('',#45577,#8339);
#5829=LINE('',#45925,#8340);
#5830=LINE('',#46111,#8341);
#5831=LINE('',#46459,#8342);
#5832=LINE('',#46807,#8343);
#5833=LINE('',#46993,#8344);
#5834=LINE('',#47179,#8345);
#5835=LINE('',#47527,#8346);
#5836=LINE('',#47713,#8347);
#5837=LINE('',#48061,#8348);
#5838=LINE('',#49710,#8349);
#5839=LINE('',#49720,#8350);
#5840=LINE('',#49722,#8351);
#5841=LINE('',#49723,#8352);
#5842=LINE('',#49727,#8353);
#5843=LINE('',#49733,#8354);
#5844=LINE('',#49739,#8355);
#5845=LINE('',#49746,#8356);
#5846=LINE('',#49750,#8357);
#5847=LINE('',#49754,#8358);
#5848=LINE('',#49758,#8359);
#5849=LINE('',#49762,#8360);
#5850=LINE('',#49766,#8361);
#5851=LINE('',#49770,#8362);
#5852=LINE('',#49774,#8363);
#5853=LINE('',#49778,#8364);
#5854=LINE('',#49782,#8365);
#5855=LINE('',#49786,#8366);
#5856=LINE('',#49790,#8367);
#5857=LINE('',#49794,#8368);
#5858=LINE('',#49798,#8369);
#5859=LINE('',#49802,#8370);
#5860=LINE('',#49806,#8371);
#5861=LINE('',#49810,#8372);
#5862=LINE('',#49814,#8373);
#5863=LINE('',#49818,#8374);
#5864=LINE('',#49822,#8375);
#5865=LINE('',#49826,#8376);
#5866=LINE('',#49830,#8377);
#5867=LINE('',#49834,#8378);
#5868=LINE('',#49838,#8379);
#5869=LINE('',#49842,#8380);
#5870=LINE('',#49846,#8381);
#5871=LINE('',#49850,#8382);
#5872=LINE('',#49854,#8383);
#5873=LINE('',#49858,#8384);
#5874=LINE('',#49862,#8385);
#5875=LINE('',#49866,#8386);
#5876=LINE('',#49870,#8387);
#5877=LINE('',#49874,#8388);
#5878=LINE('',#49879,#8389);
#5879=LINE('',#49883,#8390);
#5880=LINE('',#49887,#8391);
#5881=LINE('',#49891,#8392);
#5882=LINE('',#49895,#8393);
#5883=LINE('',#49899,#8394);
#5884=LINE('',#49903,#8395);
#5885=LINE('',#49907,#8396);
#5886=LINE('',#49911,#8397);
#5887=LINE('',#49915,#8398);
#5888=LINE('',#49919,#8399);
#5889=LINE('',#49923,#8400);
#5890=LINE('',#49927,#8401);
#5891=LINE('',#49931,#8402);
#5892=LINE('',#49935,#8403);
#5893=LINE('',#49939,#8404);
#5894=LINE('',#49943,#8405);
#5895=LINE('',#49947,#8406);
#5896=LINE('',#49951,#8407);
#5897=LINE('',#49955,#8408);
#5898=LINE('',#49959,#8409);
#5899=LINE('',#49963,#8410);
#5900=LINE('',#49967,#8411);
#5901=LINE('',#49971,#8412);
#5902=LINE('',#49975,#8413);
#5903=LINE('',#49979,#8414);
#5904=LINE('',#49983,#8415);
#5905=LINE('',#49987,#8416);
#5906=LINE('',#49991,#8417);
#5907=LINE('',#49995,#8418);
#5908=LINE('',#49999,#8419);
#5909=LINE('',#50003,#8420);
#5910=LINE('',#50007,#8421);
#5911=LINE('',#50011,#8422);
#5912=LINE('',#50015,#8423);
#5913=LINE('',#50019,#8424);
#5914=LINE('',#50022,#8425);
#5915=LINE('',#50029,#8426);
#5916=LINE('',#50030,#8427);
#5917=LINE('',#50032,#8428);
#5918=LINE('',#50043,#8429);
#5919=LINE('',#50044,#8430);
#5920=LINE('',#50046,#8431);
#5921=LINE('',#50057,#8432);
#5922=LINE('',#50058,#8433);
#5923=LINE('',#50060,#8434);
#5924=LINE('',#50071,#8435);
#5925=LINE('',#50072,#8436);
#5926=LINE('',#50074,#8437);
#5927=LINE('',#50085,#8438);
#5928=LINE('',#50086,#8439);
#5929=LINE('',#50088,#8440);
#5930=LINE('',#50099,#8441);
#5931=LINE('',#50100,#8442);
#5932=LINE('',#50102,#8443);
#5933=LINE('',#50113,#8444);
#5934=LINE('',#50114,#8445);
#5935=LINE('',#50116,#8446);
#5936=LINE('',#50127,#8447);
#5937=LINE('',#50128,#8448);
#5938=LINE('',#50130,#8449);
#5939=LINE('',#50141,#8450);
#5940=LINE('',#50142,#8451);
#5941=LINE('',#50144,#8452);
#5942=LINE('',#50155,#8453);
#5943=LINE('',#50156,#8454);
#5944=LINE('',#50158,#8455);
#5945=LINE('',#50169,#8456);
#5946=LINE('',#50170,#8457);
#5947=LINE('',#50172,#8458);
#5948=LINE('',#50183,#8459);
#5949=LINE('',#50184,#8460);
#5950=LINE('',#50186,#8461);
#5951=LINE('',#50197,#8462);
#5952=LINE('',#50198,#8463);
#5953=LINE('',#50200,#8464);
#5954=LINE('',#50211,#8465);
#5955=LINE('',#50212,#8466);
#5956=LINE('',#50214,#8467);
#5957=LINE('',#50225,#8468);
#5958=LINE('',#50226,#8469);
#5959=LINE('',#50228,#8470);
#5960=LINE('',#50239,#8471);
#5961=LINE('',#50240,#8472);
#5962=LINE('',#50242,#8473);
#5963=LINE('',#50253,#8474);
#5964=LINE('',#50254,#8475);
#5965=LINE('',#50256,#8476);
#5966=LINE('',#50267,#8477);
#5967=LINE('',#50268,#8478);
#5968=LINE('',#50270,#8479);
#5969=LINE('',#50281,#8480);
#5970=LINE('',#50282,#8481);
#5971=LINE('',#50284,#8482);
#5972=LINE('',#50295,#8483);
#5973=LINE('',#50296,#8484);
#5974=LINE('',#50298,#8485);
#5975=LINE('',#50309,#8486);
#5976=LINE('',#50310,#8487);
#5977=LINE('',#50312,#8488);
#5978=LINE('',#50323,#8489);
#5979=LINE('',#50324,#8490);
#5980=LINE('',#50326,#8491);
#5981=LINE('',#50337,#8492);
#5982=LINE('',#50338,#8493);
#5983=LINE('',#50340,#8494);
#5984=LINE('',#50351,#8495);
#5985=LINE('',#50352,#8496);
#5986=LINE('',#50354,#8497);
#5987=LINE('',#50365,#8498);
#5988=LINE('',#50366,#8499);
#5989=LINE('',#50368,#8500);
#5990=LINE('',#50379,#8501);
#5991=LINE('',#50380,#8502);
#5992=LINE('',#50382,#8503);
#5993=LINE('',#50393,#8504);
#5994=LINE('',#50394,#8505);
#5995=LINE('',#50396,#8506);
#5996=LINE('',#50407,#8507);
#5997=LINE('',#50408,#8508);
#5998=LINE('',#50410,#8509);
#5999=LINE('',#50421,#8510);
#6000=LINE('',#50422,#8511);
#6001=LINE('',#50424,#8512);
#6002=LINE('',#50435,#8513);
#6003=LINE('',#50436,#8514);
#6004=LINE('',#50438,#8515);
#6005=LINE('',#50449,#8516);
#6006=LINE('',#50450,#8517);
#6007=LINE('',#50452,#8518);
#6008=LINE('',#50463,#8519);
#6009=LINE('',#50464,#8520);
#6010=LINE('',#50466,#8521);
#6011=LINE('',#50477,#8522);
#6012=LINE('',#50478,#8523);
#6013=LINE('',#50480,#8524);
#6014=LINE('',#50491,#8525);
#6015=LINE('',#50492,#8526);
#6016=LINE('',#50494,#8527);
#6017=LINE('',#50505,#8528);
#6018=LINE('',#50506,#8529);
#6019=LINE('',#50508,#8530);
#6020=LINE('',#50517,#8531);
#6021=LINE('',#50583,#8532);
#6022=LINE('',#50586,#8533);
#6023=LINE('',#50588,#8534);
#6024=LINE('',#50592,#8535);
#6025=LINE('',#50594,#8536);
#6026=LINE('',#50598,#8537);
#6027=LINE('',#50601,#8538);
#6028=LINE('',#50604,#8539);
#6029=LINE('',#50606,#8540);
#6030=LINE('',#50610,#8541);
#6031=LINE('',#50613,#8542);
#6032=LINE('',#50616,#8543);
#6033=LINE('',#50619,#8544);
#6034=LINE('',#50621,#8545);
#6035=LINE('',#50623,#8546);
#6036=LINE('',#50625,#8547);
#6037=LINE('',#50626,#8548);
#6038=LINE('',#50628,#8549);
#6039=LINE('',#50630,#8550);
#6040=LINE('',#50631,#8551);
#6041=LINE('',#50633,#8552);
#6042=LINE('',#50635,#8553);
#6043=LINE('',#50636,#8554);
#6044=LINE('',#50640,#8555);
#6045=LINE('',#50643,#8556);
#6046=LINE('',#50645,#8557);
#6047=LINE('',#50648,#8558);
#6048=LINE('',#50658,#8559);
#6049=LINE('',#50661,#8560);
#6050=LINE('',#50665,#8561);
#6051=LINE('',#50667,#8562);
#6052=LINE('',#50669,#8563);
#8327=VECTOR('',#30792,1.17775);
#8328=VECTOR('',#30797,1.17775);
#8329=VECTOR('',#30800,1.17775);
#8330=VECTOR('',#30803,1.17775);
#8331=VECTOR('',#30806,1.17775);
#8332=VECTOR('',#30809,1.17775);
#8333=VECTOR('',#30812,1.17775);
#8334=VECTOR('',#30815,1.17775);
#8335=VECTOR('',#30818,1.17775);
#8336=VECTOR('',#30821,1.17775);
#8337=VECTOR('',#30824,1.17775);
#8338=VECTOR('',#30827,1.4635);
#8339=VECTOR('',#30832,1.4635);
#8340=VECTOR('',#30835,1.4635);
#8341=VECTOR('',#30838,1.4635);
#8342=VECTOR('',#30841,1.4635);
#8343=VECTOR('',#30844,1.4635);
#8344=VECTOR('',#30847,1.4635);
#8345=VECTOR('',#30850,1.4635);
#8346=VECTOR('',#30853,1.4635);
#8347=VECTOR('',#30856,1.4635);
#8348=VECTOR('',#30859,1.4635);
#8349=VECTOR('',#30892,1.2885);
#8350=VECTOR('',#30899,10.);
#8351=VECTOR('',#30900,10.);
#8352=VECTOR('',#30901,10.);
#8353=VECTOR('',#30906,10.);
#8354=VECTOR('',#30909,10.);
#8355=VECTOR('',#30914,2.75);
#8356=VECTOR('',#30921,10.);
#8357=VECTOR('',#30924,10.);
#8358=VECTOR('',#30927,10.);
#8359=VECTOR('',#30930,10.);
#8360=VECTOR('',#30933,10.);
#8361=VECTOR('',#30936,10.);
#8362=VECTOR('',#30939,10.);
#8363=VECTOR('',#30942,10.);
#8364=VECTOR('',#30945,10.);
#8365=VECTOR('',#30948,10.);
#8366=VECTOR('',#30951,10.);
#8367=VECTOR('',#30954,10.);
#8368=VECTOR('',#30957,10.);
#8369=VECTOR('',#30960,10.);
#8370=VECTOR('',#30963,10.);
#8371=VECTOR('',#30966,10.);
#8372=VECTOR('',#30969,10.);
#8373=VECTOR('',#30972,10.);
#8374=VECTOR('',#30975,10.);
#8375=VECTOR('',#30978,10.);
#8376=VECTOR('',#30981,10.);
#8377=VECTOR('',#30984,10.);
#8378=VECTOR('',#30987,10.);
#8379=VECTOR('',#30990,10.);
#8380=VECTOR('',#30993,10.);
#8381=VECTOR('',#30996,10.);
#8382=VECTOR('',#30999,10.);
#8383=VECTOR('',#31002,10.);
#8384=VECTOR('',#31005,10.);
#8385=VECTOR('',#31008,10.);
#8386=VECTOR('',#31011,10.);
#8387=VECTOR('',#31014,10.);
#8388=VECTOR('',#31017,10.);
#8389=VECTOR('',#31022,10.);
#8390=VECTOR('',#31025,10.);
#8391=VECTOR('',#31028,10.);
#8392=VECTOR('',#31031,10.);
#8393=VECTOR('',#31034,10.);
#8394=VECTOR('',#31037,10.);
#8395=VECTOR('',#31040,10.);
#8396=VECTOR('',#31043,10.);
#8397=VECTOR('',#31046,10.);
#8398=VECTOR('',#31049,10.);
#8399=VECTOR('',#31052,10.);
#8400=VECTOR('',#31055,10.);
#8401=VECTOR('',#31058,10.);
#8402=VECTOR('',#31061,10.);
#8403=VECTOR('',#31064,10.);
#8404=VECTOR('',#31067,10.);
#8405=VECTOR('',#31070,10.);
#8406=VECTOR('',#31073,10.);
#8407=VECTOR('',#31076,10.);
#8408=VECTOR('',#31079,10.);
#8409=VECTOR('',#31082,10.);
#8410=VECTOR('',#31085,10.);
#8411=VECTOR('',#31088,10.);
#8412=VECTOR('',#31091,10.);
#8413=VECTOR('',#31094,10.);
#8414=VECTOR('',#31097,10.);
#8415=VECTOR('',#31100,10.);
#8416=VECTOR('',#31103,10.);
#8417=VECTOR('',#31106,10.);
#8418=VECTOR('',#31109,10.);
#8419=VECTOR('',#31112,10.);
#8420=VECTOR('',#31115,10.);
#8421=VECTOR('',#31118,10.);
#8422=VECTOR('',#31121,10.);
#8423=VECTOR('',#31124,10.);
#8424=VECTOR('',#31127,10.);
#8425=VECTOR('',#31130,10.);
#8426=VECTOR('',#31133,10.);
#8427=VECTOR('',#31134,10.);
#8428=VECTOR('',#31137,10.);
#8429=VECTOR('',#31142,10.);
#8430=VECTOR('',#31143,10.);
#8431=VECTOR('',#31146,10.);
#8432=VECTOR('',#31151,10.);
#8433=VECTOR('',#31152,10.);
#8434=VECTOR('',#31155,10.);
#8435=VECTOR('',#31160,10.);
#8436=VECTOR('',#31161,10.);
#8437=VECTOR('',#31164,10.);
#8438=VECTOR('',#31169,10.);
#8439=VECTOR('',#31170,10.);
#8440=VECTOR('',#31173,10.);
#8441=VECTOR('',#31178,10.);
#8442=VECTOR('',#31179,10.);
#8443=VECTOR('',#31182,10.);
#8444=VECTOR('',#31187,10.);
#8445=VECTOR('',#31188,10.);
#8446=VECTOR('',#31191,10.);
#8447=VECTOR('',#31196,10.);
#8448=VECTOR('',#31197,10.);
#8449=VECTOR('',#31200,10.);
#8450=VECTOR('',#31205,10.);
#8451=VECTOR('',#31206,10.);
#8452=VECTOR('',#31209,10.);
#8453=VECTOR('',#31214,10.);
#8454=VECTOR('',#31215,10.);
#8455=VECTOR('',#31218,10.);
#8456=VECTOR('',#31223,10.);
#8457=VECTOR('',#31224,10.);
#8458=VECTOR('',#31227,10.);
#8459=VECTOR('',#31232,10.);
#8460=VECTOR('',#31233,10.);
#8461=VECTOR('',#31236,10.);
#8462=VECTOR('',#31241,10.);
#8463=VECTOR('',#31242,10.);
#8464=VECTOR('',#31245,10.);
#8465=VECTOR('',#31250,10.);
#8466=VECTOR('',#31251,10.);
#8467=VECTOR('',#31254,10.);
#8468=VECTOR('',#31259,10.);
#8469=VECTOR('',#31260,10.);
#8470=VECTOR('',#31263,10.);
#8471=VECTOR('',#31268,10.);
#8472=VECTOR('',#31269,10.);
#8473=VECTOR('',#31272,10.);
#8474=VECTOR('',#31277,10.);
#8475=VECTOR('',#31278,10.);
#8476=VECTOR('',#31281,10.);
#8477=VECTOR('',#31286,10.);
#8478=VECTOR('',#31287,10.);
#8479=VECTOR('',#31290,10.);
#8480=VECTOR('',#31295,10.);
#8481=VECTOR('',#31296,10.);
#8482=VECTOR('',#31299,10.);
#8483=VECTOR('',#31304,10.);
#8484=VECTOR('',#31305,10.);
#8485=VECTOR('',#31308,10.);
#8486=VECTOR('',#31313,10.);
#8487=VECTOR('',#31314,10.);
#8488=VECTOR('',#31317,10.);
#8489=VECTOR('',#31322,10.);
#8490=VECTOR('',#31323,10.);
#8491=VECTOR('',#31326,10.);
#8492=VECTOR('',#31331,10.);
#8493=VECTOR('',#31332,10.);
#8494=VECTOR('',#31335,10.);
#8495=VECTOR('',#31340,10.);
#8496=VECTOR('',#31341,10.);
#8497=VECTOR('',#31344,10.);
#8498=VECTOR('',#31349,10.);
#8499=VECTOR('',#31350,10.);
#8500=VECTOR('',#31353,10.);
#8501=VECTOR('',#31358,10.);
#8502=VECTOR('',#31359,10.);
#8503=VECTOR('',#31362,10.);
#8504=VECTOR('',#31367,10.);
#8505=VECTOR('',#31368,10.);
#8506=VECTOR('',#31371,10.);
#8507=VECTOR('',#31376,10.);
#8508=VECTOR('',#31377,10.);
#8509=VECTOR('',#31380,10.);
#8510=VECTOR('',#31385,10.);
#8511=VECTOR('',#31386,10.);
#8512=VECTOR('',#31389,10.);
#8513=VECTOR('',#31394,10.);
#8514=VECTOR('',#31395,10.);
#8515=VECTOR('',#31398,10.);
#8516=VECTOR('',#31403,10.);
#8517=VECTOR('',#31404,10.);
#8518=VECTOR('',#31407,10.);
#8519=VECTOR('',#31412,10.);
#8520=VECTOR('',#31413,10.);
#8521=VECTOR('',#31416,10.);
#8522=VECTOR('',#31421,10.);
#8523=VECTOR('',#31422,10.);
#8524=VECTOR('',#31425,10.);
#8525=VECTOR('',#31430,10.);
#8526=VECTOR('',#31431,10.);
#8527=VECTOR('',#31434,10.);
#8528=VECTOR('',#31439,10.);
#8529=VECTOR('',#31440,10.);
#8530=VECTOR('',#31443,10.);
#8531=VECTOR('',#31452,2.6);
#8532=VECTOR('',#31473,1.49337567297406);
#8533=VECTOR('',#31476,10.);
#8534=VECTOR('',#31477,10.);
#8535=VECTOR('',#31482,10.);
#8536=VECTOR('',#31483,10.);
#8537=VECTOR('',#31488,10.);
#8538=VECTOR('',#31491,10.);
#8539=VECTOR('',#31494,10.);
#8540=VECTOR('',#31495,10.);
#8541=VECTOR('',#31500,10.);
#8542=VECTOR('',#31503,10.);
#8543=VECTOR('',#31506,10.);
#8544=VECTOR('',#31509,10.);
#8545=VECTOR('',#31512,10.);
#8546=VECTOR('',#31513,10.);
#8547=VECTOR('',#31514,10.);
#8548=VECTOR('',#31515,10.);
#8549=VECTOR('',#31518,10.);
#8550=VECTOR('',#31519,10.);
#8551=VECTOR('',#31520,10.);
#8552=VECTOR('',#31523,10.);
#8553=VECTOR('',#31524,10.);
#8554=VECTOR('',#31525,10.);
#8555=VECTOR('',#31532,10.);
#8556=VECTOR('',#31537,9.99999999999999);
#8557=VECTOR('',#31540,10.);
#8558=VECTOR('',#31543,10.);
#8559=VECTOR('',#31560,10.);
#8560=VECTOR('',#31565,9.99999999999999);
#8561=VECTOR('',#31570,1.44337567297406);
#8562=VECTOR('',#31573,10.);
#8563=VECTOR('',#31576,10.);
#10509=CIRCLE('',#27597,1.17775);
#10510=CIRCLE('',#27609,1.4635);
#10511=CIRCLE('',#27621,1.4635);
#10512=CIRCLE('',#27623,1.17775);
#10513=CIRCLE('',#27625,1.4635);
#10514=CIRCLE('',#27626,1.4635);
#10515=CIRCLE('',#27628,1.4635);
#10516=CIRCLE('',#27629,1.4635);
#10517=CIRCLE('',#27631,1.5635);
#10518=CIRCLE('',#27632,0.1);
#10519=CIRCLE('',#27634,2.55);
#10520=CIRCLE('',#27636,1.1135);
#10521=CIRCLE('',#27640,2.75);
#10522=CIRCLE('',#27643,2.75);
#10523=CIRCLE('',#27644,2.75);
#10524=CIRCLE('',#27645,2.75);
#10525=CIRCLE('',#27646,2.75);
#10526=CIRCLE('',#27647,2.75);
#10527=CIRCLE('',#27648,2.75);
#10528=CIRCLE('',#27649,2.75);
#10529=CIRCLE('',#27650,2.75);
#10530=CIRCLE('',#27651,2.75);
#10531=CIRCLE('',#27652,2.75);
#10532=CIRCLE('',#27653,2.75);
#10533=CIRCLE('',#27654,2.75);
#10534=CIRCLE('',#27655,2.75);
#10535=CIRCLE('',#27656,2.75);
#10536=CIRCLE('',#27657,2.75);
#10537=CIRCLE('',#27658,2.75);
#10538=CIRCLE('',#27659,2.75);
#10539=CIRCLE('',#27660,2.75);
#10540=CIRCLE('',#27661,2.75);
#10541=CIRCLE('',#27662,2.75);
#10542=CIRCLE('',#27663,2.75);
#10543=CIRCLE('',#27664,2.75);
#10544=CIRCLE('',#27665,2.75);
#10545=CIRCLE('',#27666,2.75);
#10546=CIRCLE('',#27667,2.75);
#10547=CIRCLE('',#27668,2.75);
#10548=CIRCLE('',#27669,2.75);
#10549=CIRCLE('',#27670,2.75);
#10550=CIRCLE('',#27671,2.75);
#10551=CIRCLE('',#27672,2.75);
#10552=CIRCLE('',#27673,2.75);
#10553=CIRCLE('',#27674,2.75);
#10554=CIRCLE('',#27675,2.75);
#10555=CIRCLE('',#27676,2.75);
#10556=CIRCLE('',#27677,2.75);
#10557=CIRCLE('',#27678,2.75);
#10558=CIRCLE('',#27679,2.75);
#10559=CIRCLE('',#27680,2.75);
#10560=CIRCLE('',#27681,2.75);
#10561=CIRCLE('',#27682,2.75);
#10562=CIRCLE('',#27683,2.75);
#10563=CIRCLE('',#27684,2.75);
#10564=CIRCLE('',#27685,2.75);
#10565=CIRCLE('',#27686,2.75);
#10566=CIRCLE('',#27687,2.75);
#10567=CIRCLE('',#27688,2.75);
#10568=CIRCLE('',#27689,2.75);
#10569=CIRCLE('',#27690,2.75);
#10570=CIRCLE('',#27691,2.75);
#10571=CIRCLE('',#27692,2.75);
#10572=CIRCLE('',#27693,2.75);
#10573=CIRCLE('',#27694,2.75);
#10574=CIRCLE('',#27695,2.75);
#10575=CIRCLE('',#27696,2.75);
#10576=CIRCLE('',#27697,2.75);
#10577=CIRCLE('',#27698,2.75);
#10578=CIRCLE('',#27699,2.75);
#10579=CIRCLE('',#27700,2.75);
#10580=CIRCLE('',#27701,2.75);
#10581=CIRCLE('',#27702,2.75);
#10582=CIRCLE('',#27703,2.75);
#10583=CIRCLE('',#27704,2.75);
#10584=CIRCLE('',#27705,2.75);
#10585=CIRCLE('',#27706,2.75);
#10586=CIRCLE('',#27707,2.75);
#10587=CIRCLE('',#27708,2.75);
#10588=CIRCLE('',#27709,2.75);
#10589=CIRCLE('',#27710,2.75);
#10590=CIRCLE('',#27711,2.75);
#10591=CIRCLE('',#27712,2.75);
#10592=CIRCLE('',#27713,2.75);
#10593=CIRCLE('',#27714,2.75);
#10594=CIRCLE('',#27715,2.75);
#10595=CIRCLE('',#27716,2.75);
#10596=CIRCLE('',#27823,0.2);
#10597=CIRCLE('',#27825,2.45);
#10598=CIRCLE('',#27827,1.59337567297407);
#10599=CIRCLE('',#27829,1.39337567297406);
#10600=CIRCLE('',#27830,1.39337567297406);
#10601=CIRCLE('',#27831,1.39337567297406);
#10602=CIRCLE('',#27832,1.39337567297406);
#10603=CIRCLE('',#27833,1.39337567297406);
#10604=CIRCLE('',#27834,1.39337567297406);
#10605=CIRCLE('',#27836,1.39337567297406);
#10606=CIRCLE('',#27838,1.39337567297406);
#10607=CIRCLE('',#27840,1.39337567297406);
#10608=CIRCLE('',#27842,1.39337567297406);
#10609=CIRCLE('',#27844,1.39337567297406);
#10610=CIRCLE('',#27846,1.39337567297406);
#10611=CIRCLE('',#27857,1.44337567297406);
#10612=CIRCLE('',#27859,1.44337567297406);
#10613=CIRCLE('',#27861,1.44337567297406);
#10614=CIRCLE('',#27863,1.44337567297406);
#10615=CIRCLE('',#27865,1.44337567297406);
#10616=CIRCLE('',#27867,1.44337567297406);
#11568=VERTEX_POINT('',#42115);
#11569=VERTEX_POINT('',#42116);
#11570=VERTEX_POINT('',#42118);
#11571=VERTEX_POINT('',#42216);
#11572=VERTEX_POINT('',#42280);
#11573=VERTEX_POINT('',#42281);
#11574=VERTEX_POINT('',#42283);
#11575=VERTEX_POINT('',#42341);
#11576=VERTEX_POINT('',#42524);
#11577=VERTEX_POINT('',#42525);
#11578=VERTEX_POINT('',#42527);
#11579=VERTEX_POINT('',#42837);
#11580=VERTEX_POINT('',#42838);
#11581=VERTEX_POINT('',#42840);
#11582=VERTEX_POINT('',#43026);
#11583=VERTEX_POINT('',#43220);
#11584=VERTEX_POINT('',#43221);
#11585=VERTEX_POINT('',#43576);
#11586=VERTEX_POINT('',#43577);
#11587=VERTEX_POINT('',#43579);
#11588=VERTEX_POINT('',#43770);
#11589=VERTEX_POINT('',#43952);
#11590=VERTEX_POINT('',#43953);
#11591=VERTEX_POINT('',#44324);
#11592=VERTEX_POINT('',#44325);
#11593=VERTEX_POINT('',#44327);
#11594=VERTEX_POINT('',#44390);
#11595=VERTEX_POINT('',#44572);
#11596=VERTEX_POINT('',#44573);
#11597=VERTEX_POINT('',#44575);
#11598=VERTEX_POINT('',#44901);
#11599=VERTEX_POINT('',#44902);
#11600=VERTEX_POINT('',#45082);
#11601=VERTEX_POINT('',#45262);
#11602=VERTEX_POINT('',#45263);
#11603=VERTEX_POINT('',#45265);
#11604=VERTEX_POINT('',#45448);
#11605=VERTEX_POINT('',#45505);
#11606=VERTEX_POINT('',#45506);
#11607=VERTEX_POINT('',#45508);
#11608=VERTEX_POINT('',#45567);
#11609=VERTEX_POINT('',#45575);
#11610=VERTEX_POINT('',#45576);
#11611=VERTEX_POINT('',#45923);
#11612=VERTEX_POINT('',#45924);
#11613=VERTEX_POINT('',#46109);
#11614=VERTEX_POINT('',#46110);
#11615=VERTEX_POINT('',#46457);
#11616=VERTEX_POINT('',#46458);
#11617=VERTEX_POINT('',#46805);
#11618=VERTEX_POINT('',#46806);
#11619=VERTEX_POINT('',#46991);
#11620=VERTEX_POINT('',#46992);
#11621=VERTEX_POINT('',#47177);
#11622=VERTEX_POINT('',#47178);
#11623=VERTEX_POINT('',#47525);
#11624=VERTEX_POINT('',#47526);
#11625=VERTEX_POINT('',#47711);
#11626=VERTEX_POINT('',#47712);
#11627=VERTEX_POINT('',#48059);
#11628=VERTEX_POINT('',#48060);
#11629=VERTEX_POINT('',#48407);
#11630=VERTEX_POINT('',#48568);
#11631=VERTEX_POINT('',#48579);
#11632=VERTEX_POINT('',#48586);
#11633=VERTEX_POINT('',#48663);
#11634=VERTEX_POINT('',#48665);
#11635=VERTEX_POINT('',#48756);
#11636=VERTEX_POINT('',#48757);
#11637=VERTEX_POINT('',#49311);
#11638=VERTEX_POINT('',#49312);
#11639=VERTEX_POINT('',#49702);
#11640=VERTEX_POINT('',#49706);
#11641=VERTEX_POINT('',#49709);
#11642=VERTEX_POINT('',#49714);
#11643=VERTEX_POINT('',#49715);
#11644=VERTEX_POINT('',#49719);
#11645=VERTEX_POINT('',#49721);
#11646=VERTEX_POINT('',#49725);
#11647=VERTEX_POINT('',#49729);
#11648=VERTEX_POINT('',#49735);
#11649=VERTEX_POINT('',#49736);
#11650=VERTEX_POINT('',#49738);
#11651=VERTEX_POINT('',#49740);
#11652=VERTEX_POINT('',#49743);
#11653=VERTEX_POINT('',#49745);
#11654=VERTEX_POINT('',#49747);
#11655=VERTEX_POINT('',#49749);
#11656=VERTEX_POINT('',#49751);
#11657=VERTEX_POINT('',#49753);
#11658=VERTEX_POINT('',#49755);
#11659=VERTEX_POINT('',#49757);
#11660=VERTEX_POINT('',#49759);
#11661=VERTEX_POINT('',#49761);
#11662=VERTEX_POINT('',#49763);
#11663=VERTEX_POINT('',#49765);
#11664=VERTEX_POINT('',#49767);
#11665=VERTEX_POINT('',#49769);
#11666=VERTEX_POINT('',#49771);
#11667=VERTEX_POINT('',#49773);
#11668=VERTEX_POINT('',#49775);
#11669=VERTEX_POINT('',#49777);
#11670=VERTEX_POINT('',#49779);
#11671=VERTEX_POINT('',#49781);
#11672=VERTEX_POINT('',#49783);
#11673=VERTEX_POINT('',#49785);
#11674=VERTEX_POINT('',#49787);
#11675=VERTEX_POINT('',#49789);
#11676=VERTEX_POINT('',#49791);
#11677=VERTEX_POINT('',#49793);
#11678=VERTEX_POINT('',#49795);
#11679=VERTEX_POINT('',#49797);
#11680=VERTEX_POINT('',#49799);
#11681=VERTEX_POINT('',#49801);
#11682=VERTEX_POINT('',#49803);
#11683=VERTEX_POINT('',#49805);
#11684=VERTEX_POINT('',#49807);
#11685=VERTEX_POINT('',#49809);
#11686=VERTEX_POINT('',#49811);
#11687=VERTEX_POINT('',#49813);
#11688=VERTEX_POINT('',#49815);
#11689=VERTEX_POINT('',#49817);
#11690=VERTEX_POINT('',#49819);
#11691=VERTEX_POINT('',#49821);
#11692=VERTEX_POINT('',#49823);
#11693=VERTEX_POINT('',#49825);
#11694=VERTEX_POINT('',#49827);
#11695=VERTEX_POINT('',#49829);
#11696=VERTEX_POINT('',#49831);
#11697=VERTEX_POINT('',#49833);
#11698=VERTEX_POINT('',#49835);
#11699=VERTEX_POINT('',#49837);
#11700=VERTEX_POINT('',#49839);
#11701=VERTEX_POINT('',#49841);
#11702=VERTEX_POINT('',#49843);
#11703=VERTEX_POINT('',#49845);
#11704=VERTEX_POINT('',#49847);
#11705=VERTEX_POINT('',#49849);
#11706=VERTEX_POINT('',#49851);
#11707=VERTEX_POINT('',#49853);
#11708=VERTEX_POINT('',#49855);
#11709=VERTEX_POINT('',#49857);
#11710=VERTEX_POINT('',#49859);
#11711=VERTEX_POINT('',#49861);
#11712=VERTEX_POINT('',#49863);
#11713=VERTEX_POINT('',#49865);
#11714=VERTEX_POINT('',#49867);
#11715=VERTEX_POINT('',#49869);
#11716=VERTEX_POINT('',#49871);
#11717=VERTEX_POINT('',#49873);
#11718=VERTEX_POINT('',#49876);
#11719=VERTEX_POINT('',#49878);
#11720=VERTEX_POINT('',#49880);
#11721=VERTEX_POINT('',#49882);
#11722=VERTEX_POINT('',#49884);
#11723=VERTEX_POINT('',#49886);
#11724=VERTEX_POINT('',#49888);
#11725=VERTEX_POINT('',#49890);
#11726=VERTEX_POINT('',#49892);
#11727=VERTEX_POINT('',#49894);
#11728=VERTEX_POINT('',#49896);
#11729=VERTEX_POINT('',#49898);
#11730=VERTEX_POINT('',#49900);
#11731=VERTEX_POINT('',#49902);
#11732=VERTEX_POINT('',#49904);
#11733=VERTEX_POINT('',#49906);
#11734=VERTEX_POINT('',#49908);
#11735=VERTEX_POINT('',#49910);
#11736=VERTEX_POINT('',#49912);
#11737=VERTEX_POINT('',#49914);
#11738=VERTEX_POINT('',#49916);
#11739=VERTEX_POINT('',#49918);
#11740=VERTEX_POINT('',#49920);
#11741=VERTEX_POINT('',#49922);
#11742=VERTEX_POINT('',#49924);
#11743=VERTEX_POINT('',#49926);
#11744=VERTEX_POINT('',#49928);
#11745=VERTEX_POINT('',#49930);
#11746=VERTEX_POINT('',#49932);
#11747=VERTEX_POINT('',#49934);
#11748=VERTEX_POINT('',#49936);
#11749=VERTEX_POINT('',#49938);
#11750=VERTEX_POINT('',#49940);
#11751=VERTEX_POINT('',#49942);
#11752=VERTEX_POINT('',#49944);
#11753=VERTEX_POINT('',#49946);
#11754=VERTEX_POINT('',#49948);
#11755=VERTEX_POINT('',#49950);
#11756=VERTEX_POINT('',#49952);
#11757=VERTEX_POINT('',#49954);
#11758=VERTEX_POINT('',#49956);
#11759=VERTEX_POINT('',#49958);
#11760=VERTEX_POINT('',#49960);
#11761=VERTEX_POINT('',#49962);
#11762=VERTEX_POINT('',#49964);
#11763=VERTEX_POINT('',#49966);
#11764=VERTEX_POINT('',#49968);
#11765=VERTEX_POINT('',#49970);
#11766=VERTEX_POINT('',#49972);
#11767=VERTEX_POINT('',#49974);
#11768=VERTEX_POINT('',#49976);
#11769=VERTEX_POINT('',#49978);
#11770=VERTEX_POINT('',#49980);
#11771=VERTEX_POINT('',#49982);
#11772=VERTEX_POINT('',#49984);
#11773=VERTEX_POINT('',#49986);
#11774=VERTEX_POINT('',#49988);
#11775=VERTEX_POINT('',#49990);
#11776=VERTEX_POINT('',#49992);
#11777=VERTEX_POINT('',#49994);
#11778=VERTEX_POINT('',#49996);
#11779=VERTEX_POINT('',#49998);
#11780=VERTEX_POINT('',#50000);
#11781=VERTEX_POINT('',#50002);
#11782=VERTEX_POINT('',#50004);
#11783=VERTEX_POINT('',#50006);
#11784=VERTEX_POINT('',#50008);
#11785=VERTEX_POINT('',#50010);
#11786=VERTEX_POINT('',#50012);
#11787=VERTEX_POINT('',#50014);
#11788=VERTEX_POINT('',#50016);
#11789=VERTEX_POINT('',#50018);
#11790=VERTEX_POINT('',#50020);
#11791=VERTEX_POINT('',#50024);
#11792=VERTEX_POINT('',#50028);
#11793=VERTEX_POINT('',#50038);
#11794=VERTEX_POINT('',#50042);
#11795=VERTEX_POINT('',#50052);
#11796=VERTEX_POINT('',#50056);
#11797=VERTEX_POINT('',#50066);
#11798=VERTEX_POINT('',#50070);
#11799=VERTEX_POINT('',#50080);
#11800=VERTEX_POINT('',#50084);
#11801=VERTEX_POINT('',#50094);
#11802=VERTEX_POINT('',#50098);
#11803=VERTEX_POINT('',#50108);
#11804=VERTEX_POINT('',#50112);
#11805=VERTEX_POINT('',#50122);
#11806=VERTEX_POINT('',#50126);
#11807=VERTEX_POINT('',#50136);
#11808=VERTEX_POINT('',#50140);
#11809=VERTEX_POINT('',#50150);
#11810=VERTEX_POINT('',#50154);
#11811=VERTEX_POINT('',#50164);
#11812=VERTEX_POINT('',#50168);
#11813=VERTEX_POINT('',#50178);
#11814=VERTEX_POINT('',#50182);
#11815=VERTEX_POINT('',#50192);
#11816=VERTEX_POINT('',#50196);
#11817=VERTEX_POINT('',#50206);
#11818=VERTEX_POINT('',#50210);
#11819=VERTEX_POINT('',#50220);
#11820=VERTEX_POINT('',#50224);
#11821=VERTEX_POINT('',#50234);
#11822=VERTEX_POINT('',#50238);
#11823=VERTEX_POINT('',#50248);
#11824=VERTEX_POINT('',#50252);
#11825=VERTEX_POINT('',#50262);
#11826=VERTEX_POINT('',#50266);
#11827=VERTEX_POINT('',#50276);
#11828=VERTEX_POINT('',#50280);
#11829=VERTEX_POINT('',#50290);
#11830=VERTEX_POINT('',#50294);
#11831=VERTEX_POINT('',#50304);
#11832=VERTEX_POINT('',#50308);
#11833=VERTEX_POINT('',#50318);
#11834=VERTEX_POINT('',#50322);
#11835=VERTEX_POINT('',#50332);
#11836=VERTEX_POINT('',#50336);
#11837=VERTEX_POINT('',#50346);
#11838=VERTEX_POINT('',#50350);
#11839=VERTEX_POINT('',#50360);
#11840=VERTEX_POINT('',#50364);
#11841=VERTEX_POINT('',#50374);
#11842=VERTEX_POINT('',#50378);
#11843=VERTEX_POINT('',#50388);
#11844=VERTEX_POINT('',#50392);
#11845=VERTEX_POINT('',#50402);
#11846=VERTEX_POINT('',#50406);
#11847=VERTEX_POINT('',#50416);
#11848=VERTEX_POINT('',#50420);
#11849=VERTEX_POINT('',#50430);
#11850=VERTEX_POINT('',#50434);
#11851=VERTEX_POINT('',#50444);
#11852=VERTEX_POINT('',#50448);
#11853=VERTEX_POINT('',#50458);
#11854=VERTEX_POINT('',#50462);
#11855=VERTEX_POINT('',#50472);
#11856=VERTEX_POINT('',#50476);
#11857=VERTEX_POINT('',#50486);
#11858=VERTEX_POINT('',#50490);
#11859=VERTEX_POINT('',#50500);
#11860=VERTEX_POINT('',#50504);
#11861=VERTEX_POINT('',#50516);
#11862=VERTEX_POINT('',#50520);
#11863=VERTEX_POINT('',#50523);
#11864=VERTEX_POINT('',#50524);
#11865=VERTEX_POINT('',#50528);
#11866=VERTEX_POINT('',#50530);
#11867=VERTEX_POINT('',#50534);
#11868=VERTEX_POINT('',#50538);
#11869=VERTEX_POINT('',#50540);
#11870=VERTEX_POINT('',#50544);
#11871=VERTEX_POINT('',#50548);
#11872=VERTEX_POINT('',#50550);
#11873=VERTEX_POINT('',#50554);
#11874=VERTEX_POINT('',#50558);
#11875=VERTEX_POINT('',#50560);
#11876=VERTEX_POINT('',#50564);
#11877=VERTEX_POINT('',#50568);
#11878=VERTEX_POINT('',#50570);
#11879=VERTEX_POINT('',#50574);
#11880=VERTEX_POINT('',#50578);
#11881=VERTEX_POINT('',#50585);
#11882=VERTEX_POINT('',#50587);
#11883=VERTEX_POINT('',#50591);
#11884=VERTEX_POINT('',#50593);
#11885=VERTEX_POINT('',#50597);
#11886=VERTEX_POINT('',#50599);
#11887=VERTEX_POINT('',#50603);
#11888=VERTEX_POINT('',#50605);
#11889=VERTEX_POINT('',#50609);
#11890=VERTEX_POINT('',#50611);
#11891=VERTEX_POINT('',#50615);
#11892=VERTEX_POINT('',#50617);
#11893=VERTEX_POINT('',#50622);
#11894=VERTEX_POINT('',#50624);
#11895=VERTEX_POINT('',#50629);
#11896=VERTEX_POINT('',#50634);
#11897=VERTEX_POINT('',#50647);
#11898=VERTEX_POINT('',#50657);
#11899=VERTEX_POINT('',#50664);
#14467=EDGE_CURVE('',#11568,#11569,#5816,.T.);
#14468=EDGE_CURVE('',#11570,#11568,#572,.T.);
#14469=EDGE_CURVE('',#11571,#11570,#10509,.T.);
#14470=EDGE_CURVE('',#11571,#11569,#573,.T.);
#14471=EDGE_CURVE('',#11572,#11573,#5817,.T.);
#14472=EDGE_CURVE('',#11574,#11572,#574,.T.);
#14473=EDGE_CURVE('',#11568,#11574,#575,.T.);
#14474=EDGE_CURVE('',#11569,#11575,#576,.T.);
#14475=EDGE_CURVE('',#11575,#11573,#577,.T.);
#14476=EDGE_CURVE('',#11576,#11577,#5818,.T.);
#14477=EDGE_CURVE('',#11578,#11576,#578,.T.);
#14478=EDGE_CURVE('',#11572,#11578,#579,.T.);
#14479=EDGE_CURVE('',#11573,#11577,#580,.T.);
#14480=EDGE_CURVE('',#11579,#11580,#5819,.T.);
#14481=EDGE_CURVE('',#11581,#11579,#581,.F.);
#14482=EDGE_CURVE('',#11576,#11581,#582,.T.);
#14483=EDGE_CURVE('',#11577,#11582,#583,.T.);
#14484=EDGE_CURVE('',#11582,#11580,#584,.T.);
#14485=EDGE_CURVE('',#11583,#11584,#5820,.T.);
#14486=EDGE_CURVE('',#11579,#11583,#585,.F.);
#14487=EDGE_CURVE('',#11580,#11584,#586,.T.);
#14488=EDGE_CURVE('',#11585,#11586,#5821,.T.);
#14489=EDGE_CURVE('',#11587,#11585,#587,.F.);
#14490=EDGE_CURVE('',#11583,#11587,#588,.F.);
#14491=EDGE_CURVE('',#11584,#11588,#589,.T.);
#14492=EDGE_CURVE('',#11588,#11586,#590,.T.);
#14493=EDGE_CURVE('',#11589,#11590,#5822,.T.);
#14494=EDGE_CURVE('',#11585,#11589,#591,.F.);
#14495=EDGE_CURVE('',#11586,#11590,#592,.T.);
#14496=EDGE_CURVE('',#11591,#11592,#5823,.T.);
#14497=EDGE_CURVE('',#11593,#11591,#593,.T.);
#14498=EDGE_CURVE('',#11589,#11593,#594,.F.);
#14499=EDGE_CURVE('',#11590,#11594,#595,.T.);
#14500=EDGE_CURVE('',#11594,#11592,#596,.T.);
#14501=EDGE_CURVE('',#11595,#11596,#5824,.T.);
#14502=EDGE_CURVE('',#11597,#11595,#597,.F.);
#14503=EDGE_CURVE('',#11591,#11597,#598,.T.);
#14504=EDGE_CURVE('',#11592,#11596,#599,.T.);
#14505=EDGE_CURVE('',#11598,#11599,#5825,.T.);
#14506=EDGE_CURVE('',#11595,#11598,#600,.F.);
#14507=EDGE_CURVE('',#11596,#11600,#601,.T.);
#14508=EDGE_CURVE('',#11600,#11599,#602,.T.);
#14509=EDGE_CURVE('',#11601,#11602,#5826,.T.);
#14510=EDGE_CURVE('',#11603,#11601,#603,.T.);
#14511=EDGE_CURVE('',#11598,#11603,#604,.F.);
#14512=EDGE_CURVE('',#11599,#11604,#605,.T.);
#14513=EDGE_CURVE('',#11604,#11602,#606,.T.);
#14514=EDGE_CURVE('',#11605,#11606,#5827,.T.);
#14515=EDGE_CURVE('',#11605,#11607,#607,.T.);
#14516=EDGE_CURVE('',#11608,#11607,#10510,.T.);
#14517=EDGE_CURVE('',#11608,#11606,#608,.T.);
#14518=EDGE_CURVE('',#11609,#11610,#5828,.T.);
#14519=EDGE_CURVE('',#11609,#11605,#609,.T.);
#14520=EDGE_CURVE('',#11606,#11610,#610,.T.);
#14521=EDGE_CURVE('',#11611,#11612,#5829,.T.);
#14522=EDGE_CURVE('',#11611,#11609,#611,.T.);
#14523=EDGE_CURVE('',#11610,#11612,#612,.T.);
#14524=EDGE_CURVE('',#11613,#11614,#5830,.T.);
#14525=EDGE_CURVE('',#11613,#11611,#613,.T.);
#14526=EDGE_CURVE('',#11612,#11614,#614,.T.);
#14527=EDGE_CURVE('',#11615,#11616,#5831,.T.);
#14528=EDGE_CURVE('',#11615,#11613,#615,.T.);
#14529=EDGE_CURVE('',#11614,#11616,#616,.T.);
#14530=EDGE_CURVE('',#11617,#11618,#5832,.T.);
#14531=EDGE_CURVE('',#11617,#11615,#617,.T.);
#14532=EDGE_CURVE('',#11616,#11618,#618,.T.);
#14533=EDGE_CURVE('',#11619,#11620,#5833,.T.);
#14534=EDGE_CURVE('',#11619,#11617,#619,.T.);
#14535=EDGE_CURVE('',#11618,#11620,#620,.T.);
#14536=EDGE_CURVE('',#11621,#11622,#5834,.T.);
#14537=EDGE_CURVE('',#11621,#11619,#621,.T.);
#14538=EDGE_CURVE('',#11620,#11622,#622,.T.);
#14539=EDGE_CURVE('',#11623,#11624,#5835,.T.);
#14540=EDGE_CURVE('',#11623,#11621,#623,.T.);
#14541=EDGE_CURVE('',#11622,#11624,#624,.T.);
#14542=EDGE_CURVE('',#11625,#11626,#5836,.T.);
#14543=EDGE_CURVE('',#11625,#11623,#625,.T.);
#14544=EDGE_CURVE('',#11624,#11626,#626,.T.);
#14545=EDGE_CURVE('',#11627,#11628,#5837,.T.);
#14546=EDGE_CURVE('',#11627,#11625,#627,.T.);
#14547=EDGE_CURVE('',#11626,#11628,#628,.T.);
#14548=EDGE_CURVE('',#11628,#11629,#629,.T.);
#14549=EDGE_CURVE('',#11630,#11629,#10511,.T.);
#14550=EDGE_CURVE('',#11630,#11627,#630,.T.);
#14551=EDGE_CURVE('',#11602,#11631,#631,.T.);
#14552=EDGE_CURVE('',#11631,#11632,#632,.T.);
#14553=EDGE_CURVE('',#11633,#11632,#10512,.T.);
#14554=EDGE_CURVE('',#11634,#11633,#633,.T.);
#14555=EDGE_CURVE('',#11601,#11634,#634,.T.);
#14556=EDGE_CURVE('',#11635,#11636,#10513,.T.);
#14557=EDGE_CURVE('',#11635,#11633,#635,.T.);
#14558=EDGE_CURVE('',#11632,#11630,#636,.T.);
#14559=EDGE_CURVE('',#11636,#11630,#10514,.T.);
#14560=EDGE_CURVE('',#11629,#11635,#637,.T.);
#14561=EDGE_CURVE('',#11570,#11608,#638,.T.);
#14562=EDGE_CURVE('',#11637,#11638,#10515,.T.);
#14563=EDGE_CURVE('',#11637,#11571,#639,.T.);
#14564=EDGE_CURVE('',#11638,#11608,#10516,.T.);
#14565=EDGE_CURVE('',#11607,#11637,#640,.T.);
#14566=EDGE_CURVE('',#11639,#11639,#10517,.T.);
#14567=EDGE_CURVE('',#11639,#11638,#10518,.T.);
#14568=EDGE_CURVE('',#11640,#11640,#10519,.T.);
#14569=EDGE_CURVE('',#11636,#11641,#5838,.T.);
#14570=EDGE_CURVE('',#11641,#11641,#10520,.T.);
#14571=EDGE_CURVE('',#11642,#11643,#197,.T.);
#14572=EDGE_CURVE('',#11642,#11644,#5839,.T.);
#14573=EDGE_CURVE('',#11644,#11645,#5840,.T.);
#14574=EDGE_CURVE('',#11643,#11645,#5841,.T.);
#14575=EDGE_CURVE('',#11645,#11646,#10521,.T.);
#14576=EDGE_CURVE('',#11646,#11644,#5842,.T.);
#14577=EDGE_CURVE('',#11647,#11642,#198,.T.);
#14578=EDGE_CURVE('',#11646,#11647,#5843,.T.);
#14579=EDGE_CURVE('',#11648,#11649,#10522,.T.);
#14580=EDGE_CURVE('',#11649,#11650,#5844,.T.);
#14581=EDGE_CURVE('',#11651,#11650,#10523,.T.);
#14582=EDGE_CURVE('',#11650,#11651,#10524,.T.);
#14583=EDGE_CURVE('',#11649,#11652,#10525,.T.);
#14584=EDGE_CURVE('',#11652,#11653,#5845,.T.);
#14585=EDGE_CURVE('',#11654,#11653,#10526,.T.);
#14586=EDGE_CURVE('',#11654,#11655,#5846,.T.);
#14587=EDGE_CURVE('',#11655,#11656,#10527,.T.);
#14588=EDGE_CURVE('',#11656,#11657,#5847,.T.);
#14589=EDGE_CURVE('',#11658,#11657,#10528,.T.);
#14590=EDGE_CURVE('',#11658,#11659,#5848,.T.);
#14591=EDGE_CURVE('',#11659,#11660,#10529,.T.);
#14592=EDGE_CURVE('',#11660,#11661,#5849,.T.);
#14593=EDGE_CURVE('',#11662,#11661,#10530,.T.);
#14594=EDGE_CURVE('',#11662,#11663,#5850,.T.);
#14595=EDGE_CURVE('',#11663,#11664,#10531,.T.);
#14596=EDGE_CURVE('',#11664,#11665,#5851,.T.);
#14597=EDGE_CURVE('',#11666,#11665,#10532,.T.);
#14598=EDGE_CURVE('',#11666,#11667,#5852,.T.);
#14599=EDGE_CURVE('',#11667,#11668,#10533,.T.);
#14600=EDGE_CURVE('',#11668,#11669,#5853,.T.);
#14601=EDGE_CURVE('',#11670,#11669,#10534,.T.);
#14602=EDGE_CURVE('',#11670,#11671,#5854,.T.);
#14603=EDGE_CURVE('',#11671,#11672,#10535,.T.);
#14604=EDGE_CURVE('',#11672,#11673,#5855,.T.);
#14605=EDGE_CURVE('',#11674,#11673,#10536,.T.);
#14606=EDGE_CURVE('',#11674,#11675,#5856,.T.);
#14607=EDGE_CURVE('',#11675,#11676,#10537,.T.);
#14608=EDGE_CURVE('',#11676,#11677,#5857,.T.);
#14609=EDGE_CURVE('',#11678,#11677,#10538,.T.);
#14610=EDGE_CURVE('',#11678,#11679,#5858,.T.);
#14611=EDGE_CURVE('',#11679,#11680,#10539,.T.);
#14612=EDGE_CURVE('',#11680,#11681,#5859,.T.);
#14613=EDGE_CURVE('',#11682,#11681,#10540,.T.);
#14614=EDGE_CURVE('',#11682,#11683,#5860,.T.);
#14615=EDGE_CURVE('',#11683,#11684,#10541,.T.);
#14616=EDGE_CURVE('',#11684,#11685,#5861,.T.);
#14617=EDGE_CURVE('',#11686,#11685,#10542,.T.);
#14618=EDGE_CURVE('',#11686,#11687,#5862,.T.);
#14619=EDGE_CURVE('',#11687,#11688,#10543,.T.);
#14620=EDGE_CURVE('',#11688,#11689,#5863,.T.);
#14621=EDGE_CURVE('',#11690,#11689,#10544,.T.);
#14622=EDGE_CURVE('',#11690,#11691,#5864,.T.);
#14623=EDGE_CURVE('',#11691,#11692,#10545,.T.);
#14624=EDGE_CURVE('',#11692,#11693,#5865,.T.);
#14625=EDGE_CURVE('',#11694,#11693,#10546,.T.);
#14626=EDGE_CURVE('',#11694,#11695,#5866,.T.);
#14627=EDGE_CURVE('',#11695,#11696,#10547,.T.);
#14628=EDGE_CURVE('',#11696,#11697,#5867,.T.);
#14629=EDGE_CURVE('',#11698,#11697,#10548,.T.);
#14630=EDGE_CURVE('',#11698,#11699,#5868,.T.);
#14631=EDGE_CURVE('',#11699,#11700,#10549,.T.);
#14632=EDGE_CURVE('',#11700,#11701,#5869,.T.);
#14633=EDGE_CURVE('',#11702,#11701,#10550,.T.);
#14634=EDGE_CURVE('',#11702,#11703,#5870,.T.);
#14635=EDGE_CURVE('',#11703,#11704,#10551,.T.);
#14636=EDGE_CURVE('',#11704,#11705,#5871,.T.);
#14637=EDGE_CURVE('',#11706,#11705,#10552,.T.);
#14638=EDGE_CURVE('',#11706,#11707,#5872,.T.);
#14639=EDGE_CURVE('',#11707,#11708,#10553,.T.);
#14640=EDGE_CURVE('',#11708,#11709,#5873,.T.);
#14641=EDGE_CURVE('',#11710,#11709,#10554,.T.);
#14642=EDGE_CURVE('',#11710,#11711,#5874,.T.);
#14643=EDGE_CURVE('',#11711,#11712,#10555,.T.);
#14644=EDGE_CURVE('',#11712,#11713,#5875,.T.);
#14645=EDGE_CURVE('',#11714,#11713,#10556,.T.);
#14646=EDGE_CURVE('',#11714,#11715,#5876,.T.);
#14647=EDGE_CURVE('',#11715,#11716,#10557,.T.);
#14648=EDGE_CURVE('',#11716,#11717,#5877,.T.);
#14649=EDGE_CURVE('',#11643,#11717,#10558,.T.);
#14650=EDGE_CURVE('',#11718,#11647,#10559,.T.);
#14651=EDGE_CURVE('',#11718,#11719,#5878,.T.);
#14652=EDGE_CURVE('',#11719,#11720,#10560,.T.);
#14653=EDGE_CURVE('',#11720,#11721,#5879,.T.);
#14654=EDGE_CURVE('',#11722,#11721,#10561,.T.);
#14655=EDGE_CURVE('',#11722,#11723,#5880,.T.);
#14656=EDGE_CURVE('',#11723,#11724,#10562,.T.);
#14657=EDGE_CURVE('',#11724,#11725,#5881,.T.);
#14658=EDGE_CURVE('',#11726,#11725,#10563,.T.);
#14659=EDGE_CURVE('',#11726,#11727,#5882,.T.);
#14660=EDGE_CURVE('',#11727,#11728,#10564,.T.);
#14661=EDGE_CURVE('',#11728,#11729,#5883,.T.);
#14662=EDGE_CURVE('',#11730,#11729,#10565,.T.);
#14663=EDGE_CURVE('',#11730,#11731,#5884,.T.);
#14664=EDGE_CURVE('',#11731,#11732,#10566,.T.);
#14665=EDGE_CURVE('',#11732,#11733,#5885,.T.);
#14666=EDGE_CURVE('',#11734,#11733,#10567,.T.);
#14667=EDGE_CURVE('',#11734,#11735,#5886,.T.);
#14668=EDGE_CURVE('',#11735,#11736,#10568,.T.);
#14669=EDGE_CURVE('',#11736,#11737,#5887,.T.);
#14670=EDGE_CURVE('',#11738,#11737,#10569,.T.);
#14671=EDGE_CURVE('',#11738,#11739,#5888,.T.);
#14672=EDGE_CURVE('',#11739,#11740,#10570,.T.);
#14673=EDGE_CURVE('',#11740,#11741,#5889,.T.);
#14674=EDGE_CURVE('',#11742,#11741,#10571,.T.);
#14675=EDGE_CURVE('',#11742,#11743,#5890,.T.);
#14676=EDGE_CURVE('',#11743,#11744,#10572,.T.);
#14677=EDGE_CURVE('',#11744,#11745,#5891,.T.);
#14678=EDGE_CURVE('',#11746,#11745,#10573,.T.);
#14679=EDGE_CURVE('',#11746,#11747,#5892,.T.);
#14680=EDGE_CURVE('',#11747,#11748,#10574,.T.);
#14681=EDGE_CURVE('',#11748,#11749,#5893,.T.);
#14682=EDGE_CURVE('',#11750,#11749,#10575,.T.);
#14683=EDGE_CURVE('',#11750,#11751,#5894,.T.);
#14684=EDGE_CURVE('',#11751,#11752,#10576,.T.);
#14685=EDGE_CURVE('',#11752,#11753,#5895,.T.);
#14686=EDGE_CURVE('',#11754,#11753,#10577,.T.);
#14687=EDGE_CURVE('',#11754,#11755,#5896,.T.);
#14688=EDGE_CURVE('',#11755,#11756,#10578,.T.);
#14689=EDGE_CURVE('',#11756,#11757,#5897,.T.);
#14690=EDGE_CURVE('',#11758,#11757,#10579,.T.);
#14691=EDGE_CURVE('',#11758,#11759,#5898,.T.);
#14692=EDGE_CURVE('',#11759,#11760,#10580,.T.);
#14693=EDGE_CURVE('',#11760,#11761,#5899,.T.);
#14694=EDGE_CURVE('',#11762,#11761,#10581,.T.);
#14695=EDGE_CURVE('',#11762,#11763,#5900,.T.);
#14696=EDGE_CURVE('',#11763,#11764,#10582,.T.);
#14697=EDGE_CURVE('',#11764,#11765,#5901,.T.);
#14698=EDGE_CURVE('',#11766,#11765,#10583,.T.);
#14699=EDGE_CURVE('',#11766,#11767,#5902,.T.);
#14700=EDGE_CURVE('',#11767,#11768,#10584,.T.);
#14701=EDGE_CURVE('',#11768,#11769,#5903,.T.);
#14702=EDGE_CURVE('',#11770,#11769,#10585,.T.);
#14703=EDGE_CURVE('',#11770,#11771,#5904,.T.);
#14704=EDGE_CURVE('',#11771,#11772,#10586,.T.);
#14705=EDGE_CURVE('',#11772,#11773,#5905,.T.);
#14706=EDGE_CURVE('',#11774,#11773,#10587,.T.);
#14707=EDGE_CURVE('',#11774,#11775,#5906,.T.);
#14708=EDGE_CURVE('',#11775,#11776,#10588,.T.);
#14709=EDGE_CURVE('',#11776,#11777,#5907,.T.);
#14710=EDGE_CURVE('',#11778,#11777,#10589,.T.);
#14711=EDGE_CURVE('',#11778,#11779,#5908,.T.);
#14712=EDGE_CURVE('',#11779,#11780,#10590,.T.);
#14713=EDGE_CURVE('',#11780,#11781,#5909,.T.);
#14714=EDGE_CURVE('',#11782,#11781,#10591,.T.);
#14715=EDGE_CURVE('',#11782,#11783,#5910,.T.);
#14716=EDGE_CURVE('',#11783,#11784,#10592,.T.);
#14717=EDGE_CURVE('',#11784,#11785,#5911,.T.);
#14718=EDGE_CURVE('',#11786,#11785,#10593,.T.);
#14719=EDGE_CURVE('',#11786,#11787,#5912,.T.);
#14720=EDGE_CURVE('',#11787,#11788,#10594,.T.);
#14721=EDGE_CURVE('',#11788,#11789,#5913,.T.);
#14722=EDGE_CURVE('',#11790,#11789,#10595,.T.);
#14723=EDGE_CURVE('',#11790,#11648,#5914,.T.);
#14724=EDGE_CURVE('',#11791,#11714,#199,.T.);
#14725=EDGE_CURVE('',#11791,#11792,#5915,.T.);
#14726=EDGE_CURVE('',#11792,#11715,#5916,.T.);
#14727=EDGE_CURVE('',#11716,#11792,#5917,.T.);
#14728=EDGE_CURVE('',#11717,#11791,#200,.T.);
#14729=EDGE_CURVE('',#11793,#11710,#201,.T.);
#14730=EDGE_CURVE('',#11793,#11794,#5918,.T.);
#14731=EDGE_CURVE('',#11794,#11711,#5919,.T.);
#14732=EDGE_CURVE('',#11712,#11794,#5920,.T.);
#14733=EDGE_CURVE('',#11713,#11793,#202,.T.);
#14734=EDGE_CURVE('',#11795,#11706,#203,.T.);
#14735=EDGE_CURVE('',#11795,#11796,#5921,.T.);
#14736=EDGE_CURVE('',#11796,#11707,#5922,.T.);
#14737=EDGE_CURVE('',#11708,#11796,#5923,.T.);
#14738=EDGE_CURVE('',#11709,#11795,#204,.T.);
#14739=EDGE_CURVE('',#11797,#11702,#205,.T.);
#14740=EDGE_CURVE('',#11797,#11798,#5924,.T.);
#14741=EDGE_CURVE('',#11798,#11703,#5925,.T.);
#14742=EDGE_CURVE('',#11704,#11798,#5926,.T.);
#14743=EDGE_CURVE('',#11705,#11797,#206,.T.);
#14744=EDGE_CURVE('',#11799,#11698,#207,.T.);
#14745=EDGE_CURVE('',#11799,#11800,#5927,.T.);
#14746=EDGE_CURVE('',#11800,#11699,#5928,.T.);
#14747=EDGE_CURVE('',#11700,#11800,#5929,.T.);
#14748=EDGE_CURVE('',#11701,#11799,#208,.T.);
#14749=EDGE_CURVE('',#11801,#11694,#209,.T.);
#14750=EDGE_CURVE('',#11801,#11802,#5930,.T.);
#14751=EDGE_CURVE('',#11802,#11695,#5931,.T.);
#14752=EDGE_CURVE('',#11696,#11802,#5932,.T.);
#14753=EDGE_CURVE('',#11697,#11801,#210,.T.);
#14754=EDGE_CURVE('',#11803,#11690,#211,.T.);
#14755=EDGE_CURVE('',#11803,#11804,#5933,.T.);
#14756=EDGE_CURVE('',#11804,#11691,#5934,.T.);
#14757=EDGE_CURVE('',#11692,#11804,#5935,.T.);
#14758=EDGE_CURVE('',#11693,#11803,#212,.T.);
#14759=EDGE_CURVE('',#11805,#11686,#213,.T.);
#14760=EDGE_CURVE('',#11805,#11806,#5936,.T.);
#14761=EDGE_CURVE('',#11806,#11687,#5937,.T.);
#14762=EDGE_CURVE('',#11688,#11806,#5938,.T.);
#14763=EDGE_CURVE('',#11689,#11805,#214,.T.);
#14764=EDGE_CURVE('',#11807,#11682,#215,.T.);
#14765=EDGE_CURVE('',#11807,#11808,#5939,.T.);
#14766=EDGE_CURVE('',#11808,#11683,#5940,.T.);
#14767=EDGE_CURVE('',#11684,#11808,#5941,.T.);
#14768=EDGE_CURVE('',#11685,#11807,#216,.T.);
#14769=EDGE_CURVE('',#11809,#11678,#217,.T.);
#14770=EDGE_CURVE('',#11809,#11810,#5942,.T.);
#14771=EDGE_CURVE('',#11810,#11679,#5943,.T.);
#14772=EDGE_CURVE('',#11680,#11810,#5944,.T.);
#14773=EDGE_CURVE('',#11681,#11809,#218,.T.);
#14774=EDGE_CURVE('',#11811,#11674,#219,.T.);
#14775=EDGE_CURVE('',#11811,#11812,#5945,.T.);
#14776=EDGE_CURVE('',#11812,#11675,#5946,.T.);
#14777=EDGE_CURVE('',#11676,#11812,#5947,.T.);
#14778=EDGE_CURVE('',#11677,#11811,#220,.T.);
#14779=EDGE_CURVE('',#11813,#11670,#221,.T.);
#14780=EDGE_CURVE('',#11813,#11814,#5948,.T.);
#14781=EDGE_CURVE('',#11814,#11671,#5949,.T.);
#14782=EDGE_CURVE('',#11672,#11814,#5950,.T.);
#14783=EDGE_CURVE('',#11673,#11813,#222,.T.);
#14784=EDGE_CURVE('',#11815,#11666,#223,.T.);
#14785=EDGE_CURVE('',#11815,#11816,#5951,.T.);
#14786=EDGE_CURVE('',#11816,#11667,#5952,.T.);
#14787=EDGE_CURVE('',#11668,#11816,#5953,.T.);
#14788=EDGE_CURVE('',#11669,#11815,#224,.T.);
#14789=EDGE_CURVE('',#11817,#11662,#225,.T.);
#14790=EDGE_CURVE('',#11817,#11818,#5954,.T.);
#14791=EDGE_CURVE('',#11818,#11663,#5955,.T.);
#14792=EDGE_CURVE('',#11664,#11818,#5956,.T.);
#14793=EDGE_CURVE('',#11665,#11817,#226,.T.);
#14794=EDGE_CURVE('',#11819,#11658,#227,.T.);
#14795=EDGE_CURVE('',#11819,#11820,#5957,.T.);
#14796=EDGE_CURVE('',#11820,#11659,#5958,.T.);
#14797=EDGE_CURVE('',#11660,#11820,#5959,.T.);
#14798=EDGE_CURVE('',#11661,#11819,#228,.T.);
#14799=EDGE_CURVE('',#11821,#11654,#229,.T.);
#14800=EDGE_CURVE('',#11821,#11822,#5960,.T.);
#14801=EDGE_CURVE('',#11822,#11655,#5961,.T.);
#14802=EDGE_CURVE('',#11656,#11822,#5962,.T.);
#14803=EDGE_CURVE('',#11657,#11821,#230,.T.);
#14804=EDGE_CURVE('',#11823,#11790,#231,.T.);
#14805=EDGE_CURVE('',#11823,#11824,#5963,.T.);
#14806=EDGE_CURVE('',#11824,#11648,#5964,.T.);
#14807=EDGE_CURVE('',#11652,#11824,#5965,.T.);
#14808=EDGE_CURVE('',#11653,#11823,#232,.T.);
#14809=EDGE_CURVE('',#11825,#11786,#233,.T.);
#14810=EDGE_CURVE('',#11825,#11826,#5966,.T.);
#14811=EDGE_CURVE('',#11826,#11787,#5967,.T.);
#14812=EDGE_CURVE('',#11788,#11826,#5968,.T.);
#14813=EDGE_CURVE('',#11789,#11825,#234,.T.);
#14814=EDGE_CURVE('',#11827,#11782,#235,.T.);
#14815=EDGE_CURVE('',#11827,#11828,#5969,.T.);
#14816=EDGE_CURVE('',#11828,#11783,#5970,.T.);
#14817=EDGE_CURVE('',#11784,#11828,#5971,.T.);
#14818=EDGE_CURVE('',#11785,#11827,#236,.T.);
#14819=EDGE_CURVE('',#11829,#11778,#237,.T.);
#14820=EDGE_CURVE('',#11829,#11830,#5972,.T.);
#14821=EDGE_CURVE('',#11830,#11779,#5973,.T.);
#14822=EDGE_CURVE('',#11780,#11830,#5974,.T.);
#14823=EDGE_CURVE('',#11781,#11829,#238,.T.);
#14824=EDGE_CURVE('',#11831,#11774,#239,.T.);
#14825=EDGE_CURVE('',#11831,#11832,#5975,.T.);
#14826=EDGE_CURVE('',#11832,#11775,#5976,.T.);
#14827=EDGE_CURVE('',#11776,#11832,#5977,.T.);
#14828=EDGE_CURVE('',#11777,#11831,#240,.T.);
#14829=EDGE_CURVE('',#11833,#11770,#241,.T.);
#14830=EDGE_CURVE('',#11833,#11834,#5978,.T.);
#14831=EDGE_CURVE('',#11834,#11771,#5979,.T.);
#14832=EDGE_CURVE('',#11772,#11834,#5980,.T.);
#14833=EDGE_CURVE('',#11773,#11833,#242,.T.);
#14834=EDGE_CURVE('',#11835,#11766,#243,.T.);
#14835=EDGE_CURVE('',#11835,#11836,#5981,.T.);
#14836=EDGE_CURVE('',#11836,#11767,#5982,.T.);
#14837=EDGE_CURVE('',#11768,#11836,#5983,.T.);
#14838=EDGE_CURVE('',#11769,#11835,#244,.T.);
#14839=EDGE_CURVE('',#11837,#11762,#245,.T.);
#14840=EDGE_CURVE('',#11837,#11838,#5984,.T.);
#14841=EDGE_CURVE('',#11838,#11763,#5985,.T.);
#14842=EDGE_CURVE('',#11764,#11838,#5986,.T.);
#14843=EDGE_CURVE('',#11765,#11837,#246,.T.);
#14844=EDGE_CURVE('',#11839,#11758,#247,.T.);
#14845=EDGE_CURVE('',#11839,#11840,#5987,.T.);
#14846=EDGE_CURVE('',#11840,#11759,#5988,.T.);
#14847=EDGE_CURVE('',#11760,#11840,#5989,.T.);
#14848=EDGE_CURVE('',#11761,#11839,#248,.T.);
#14849=EDGE_CURVE('',#11841,#11754,#249,.T.);
#14850=EDGE_CURVE('',#11841,#11842,#5990,.T.);
#14851=EDGE_CURVE('',#11842,#11755,#5991,.T.);
#14852=EDGE_CURVE('',#11756,#11842,#5992,.T.);
#14853=EDGE_CURVE('',#11757,#11841,#250,.T.);
#14854=EDGE_CURVE('',#11843,#11750,#251,.T.);
#14855=EDGE_CURVE('',#11843,#11844,#5993,.T.);
#14856=EDGE_CURVE('',#11844,#11751,#5994,.T.);
#14857=EDGE_CURVE('',#11752,#11844,#5995,.T.);
#14858=EDGE_CURVE('',#11753,#11843,#252,.T.);
#14859=EDGE_CURVE('',#11845,#11746,#253,.T.);
#14860=EDGE_CURVE('',#11845,#11846,#5996,.T.);
#14861=EDGE_CURVE('',#11846,#11747,#5997,.T.);
#14862=EDGE_CURVE('',#11748,#11846,#5998,.T.);
#14863=EDGE_CURVE('',#11749,#11845,#254,.T.);
#14864=EDGE_CURVE('',#11847,#11742,#255,.T.);
#14865=EDGE_CURVE('',#11847,#11848,#5999,.T.);
#14866=EDGE_CURVE('',#11848,#11743,#6000,.T.);
#14867=EDGE_CURVE('',#11744,#11848,#6001,.T.);
#14868=EDGE_CURVE('',#11745,#11847,#256,.T.);
#14869=EDGE_CURVE('',#11849,#11738,#257,.T.);
#14870=EDGE_CURVE('',#11849,#11850,#6002,.T.);
#14871=EDGE_CURVE('',#11850,#11739,#6003,.T.);
#14872=EDGE_CURVE('',#11740,#11850,#6004,.T.);
#14873=EDGE_CURVE('',#11741,#11849,#258,.T.);
#14874=EDGE_CURVE('',#11851,#11734,#259,.T.);
#14875=EDGE_CURVE('',#11851,#11852,#6005,.T.);
#14876=EDGE_CURVE('',#11852,#11735,#6006,.T.);
#14877=EDGE_CURVE('',#11736,#11852,#6007,.T.);
#14878=EDGE_CURVE('',#11737,#11851,#260,.T.);
#14879=EDGE_CURVE('',#11853,#11730,#261,.T.);
#14880=EDGE_CURVE('',#11853,#11854,#6008,.T.);
#14881=EDGE_CURVE('',#11854,#11731,#6009,.T.);
#14882=EDGE_CURVE('',#11732,#11854,#6010,.T.);
#14883=EDGE_CURVE('',#11733,#11853,#262,.T.);
#14884=EDGE_CURVE('',#11855,#11726,#263,.T.);
#14885=EDGE_CURVE('',#11855,#11856,#6011,.T.);
#14886=EDGE_CURVE('',#11856,#11727,#6012,.T.);
#14887=EDGE_CURVE('',#11728,#11856,#6013,.T.);
#14888=EDGE_CURVE('',#11729,#11855,#264,.T.);
#14889=EDGE_CURVE('',#11857,#11722,#265,.T.);
#14890=EDGE_CURVE('',#11857,#11858,#6014,.T.);
#14891=EDGE_CURVE('',#11858,#11723,#6015,.T.);
#14892=EDGE_CURVE('',#11724,#11858,#6016,.T.);
#14893=EDGE_CURVE('',#11725,#11857,#266,.T.);
#14894=EDGE_CURVE('',#11859,#11718,#267,.T.);
#14895=EDGE_CURVE('',#11859,#11860,#6017,.T.);
#14896=EDGE_CURVE('',#11860,#11719,#6018,.T.);
#14897=EDGE_CURVE('',#11720,#11860,#6019,.T.);
#14898=EDGE_CURVE('',#11721,#11859,#268,.T.);
#14899=EDGE_CURVE('',#11651,#11640,#10596,.T.);
#14900=EDGE_CURVE('',#11823,#11861,#6020,.T.);
#14901=EDGE_CURVE('',#11861,#11861,#10597,.T.);
#14902=EDGE_CURVE('',#11862,#11862,#10598,.T.);
#14903=EDGE_CURVE('',#11863,#11864,#269,.T.);
#14904=EDGE_CURVE('',#11863,#11865,#10599,.T.);
#14905=EDGE_CURVE('',#11866,#11865,#270,.T.);
#14906=EDGE_CURVE('',#11867,#11866,#271,.T.);
#14907=EDGE_CURVE('',#11867,#11868,#10600,.T.);
#14908=EDGE_CURVE('',#11869,#11868,#272,.T.);
#14909=EDGE_CURVE('',#11870,#11869,#273,.T.);
#14910=EDGE_CURVE('',#11870,#11871,#10601,.T.);
#14911=EDGE_CURVE('',#11872,#11871,#274,.T.);
#14912=EDGE_CURVE('',#11873,#11872,#275,.T.);
#14913=EDGE_CURVE('',#11873,#11874,#10602,.T.);
#14914=EDGE_CURVE('',#11875,#11874,#276,.T.);
#14915=EDGE_CURVE('',#11876,#11875,#277,.T.);
#14916=EDGE_CURVE('',#11876,#11877,#10603,.T.);
#14917=EDGE_CURVE('',#11878,#11877,#278,.T.);
#14918=EDGE_CURVE('',#11879,#11878,#279,.T.);
#14919=EDGE_CURVE('',#11879,#11880,#10604,.T.);
#14920=EDGE_CURVE('',#11864,#11880,#280,.T.);
#14921=EDGE_CURVE('',#11864,#11862,#6021,.T.);
#14922=EDGE_CURVE('',#11868,#11881,#6022,.T.);
#14923=EDGE_CURVE('',#11882,#11867,#6023,.T.);
#14924=EDGE_CURVE('',#11881,#11882,#10605,.T.);
#14925=EDGE_CURVE('',#11871,#11883,#6024,.T.);
#14926=EDGE_CURVE('',#11884,#11870,#6025,.T.);
#14927=EDGE_CURVE('',#11883,#11884,#10606,.T.);
#14928=EDGE_CURVE('',#11885,#11863,#6026,.T.);
#14929=EDGE_CURVE('',#11886,#11885,#10607,.T.);
#14930=EDGE_CURVE('',#11865,#11886,#6027,.T.);
#14931=EDGE_CURVE('',#11874,#11887,#6028,.T.);
#14932=EDGE_CURVE('',#11888,#11873,#6029,.T.);
#14933=EDGE_CURVE('',#11887,#11888,#10608,.T.);
#14934=EDGE_CURVE('',#11889,#11879,#6030,.T.);
#14935=EDGE_CURVE('',#11890,#11889,#10609,.T.);
#14936=EDGE_CURVE('',#11880,#11890,#6031,.T.);
#14937=EDGE_CURVE('',#11891,#11876,#6032,.T.);
#14938=EDGE_CURVE('',#11892,#11891,#10610,.T.);
#14939=EDGE_CURVE('',#11877,#11892,#6033,.T.);
#14940=EDGE_CURVE('',#11888,#11887,#6034,.T.);
#14941=EDGE_CURVE('',#11872,#11893,#6035,.T.);
#14942=EDGE_CURVE('',#11893,#11894,#6036,.T.);
#14943=EDGE_CURVE('',#11875,#11894,#6037,.T.);
#14944=EDGE_CURVE('',#11884,#11883,#6038,.T.);
#14945=EDGE_CURVE('',#11869,#11895,#6039,.T.);
#14946=EDGE_CURVE('',#11895,#11893,#6040,.T.);
#14947=EDGE_CURVE('',#11882,#11881,#6041,.T.);
#14948=EDGE_CURVE('',#11866,#11896,#6042,.T.);
#14949=EDGE_CURVE('',#11896,#11895,#6043,.T.);
#14950=EDGE_CURVE('',#11885,#11886,#6044,.T.);
#14951=EDGE_CURVE('',#11889,#11890,#6045,.T.);
#14952=EDGE_CURVE('',#11891,#11892,#6046,.T.);
#14953=EDGE_CURVE('',#11897,#11896,#6047,.T.);
#14954=EDGE_CURVE('',#11897,#11896,#10611,.T.);
#14955=EDGE_CURVE('',#11896,#11895,#10612,.T.);
#14956=EDGE_CURVE('',#11895,#11893,#10613,.T.);
#14957=EDGE_CURVE('',#11893,#11894,#10614,.T.);
#14958=EDGE_CURVE('',#11894,#11898,#6048,.T.);
#14959=EDGE_CURVE('',#11894,#11898,#10615,.T.);
#14960=EDGE_CURVE('',#11898,#11897,#6049,.T.);
#14961=EDGE_CURVE('',#11898,#11897,#10616,.T.);
#14962=EDGE_CURVE('',#11899,#11897,#6050,.T.);
#14963=EDGE_CURVE('',#11864,#11897,#6051,.T.);
#14964=EDGE_CURVE('',#11878,#11898,#6052,.T.);
#19212=ORIENTED_EDGE('',*,*,#14467,.F.);
#19213=ORIENTED_EDGE('',*,*,#14468,.F.);
#19214=ORIENTED_EDGE('',*,*,#14469,.F.);
#19215=ORIENTED_EDGE('',*,*,#14470,.T.);
#19216=ORIENTED_EDGE('',*,*,#14471,.F.);
#19217=ORIENTED_EDGE('',*,*,#14472,.F.);
#19218=ORIENTED_EDGE('',*,*,#14473,.F.);
#19219=ORIENTED_EDGE('',*,*,#14467,.T.);
#19220=ORIENTED_EDGE('',*,*,#14474,.T.);
#19221=ORIENTED_EDGE('',*,*,#14475,.T.);
#19222=ORIENTED_EDGE('',*,*,#14476,.F.);
#19223=ORIENTED_EDGE('',*,*,#14477,.F.);
#19224=ORIENTED_EDGE('',*,*,#14478,.F.);
#19225=ORIENTED_EDGE('',*,*,#14471,.T.);
#19226=ORIENTED_EDGE('',*,*,#14479,.T.);
#19227=ORIENTED_EDGE('',*,*,#14480,.F.);
#19228=ORIENTED_EDGE('',*,*,#14481,.F.);
#19229=ORIENTED_EDGE('',*,*,#14482,.F.);
#19230=ORIENTED_EDGE('',*,*,#14476,.T.);
#19231=ORIENTED_EDGE('',*,*,#14483,.T.);
#19232=ORIENTED_EDGE('',*,*,#14484,.T.);
#19233=ORIENTED_EDGE('',*,*,#14485,.F.);
#19234=ORIENTED_EDGE('',*,*,#14486,.F.);
#19235=ORIENTED_EDGE('',*,*,#14480,.T.);
#19236=ORIENTED_EDGE('',*,*,#14487,.T.);
#19237=ORIENTED_EDGE('',*,*,#14488,.F.);
#19238=ORIENTED_EDGE('',*,*,#14489,.F.);
#19239=ORIENTED_EDGE('',*,*,#14490,.F.);
#19240=ORIENTED_EDGE('',*,*,#14485,.T.);
#19241=ORIENTED_EDGE('',*,*,#14491,.T.);
#19242=ORIENTED_EDGE('',*,*,#14492,.T.);
#19243=ORIENTED_EDGE('',*,*,#14493,.F.);
#19244=ORIENTED_EDGE('',*,*,#14494,.F.);
#19245=ORIENTED_EDGE('',*,*,#14488,.T.);
#19246=ORIENTED_EDGE('',*,*,#14495,.T.);
#19247=ORIENTED_EDGE('',*,*,#14496,.F.);
#19248=ORIENTED_EDGE('',*,*,#14497,.F.);
#19249=ORIENTED_EDGE('',*,*,#14498,.F.);
#19250=ORIENTED_EDGE('',*,*,#14493,.T.);
#19251=ORIENTED_EDGE('',*,*,#14499,.T.);
#19252=ORIENTED_EDGE('',*,*,#14500,.T.);
#19253=ORIENTED_EDGE('',*,*,#14501,.F.);
#19254=ORIENTED_EDGE('',*,*,#14502,.F.);
#19255=ORIENTED_EDGE('',*,*,#14503,.F.);
#19256=ORIENTED_EDGE('',*,*,#14496,.T.);
#19257=ORIENTED_EDGE('',*,*,#14504,.T.);
#19258=ORIENTED_EDGE('',*,*,#14505,.F.);
#19259=ORIENTED_EDGE('',*,*,#14506,.F.);
#19260=ORIENTED_EDGE('',*,*,#14501,.T.);
#19261=ORIENTED_EDGE('',*,*,#14507,.T.);
#19262=ORIENTED_EDGE('',*,*,#14508,.T.);
#19263=ORIENTED_EDGE('',*,*,#14509,.F.);
#19264=ORIENTED_EDGE('',*,*,#14510,.F.);
#19265=ORIENTED_EDGE('',*,*,#14511,.F.);
#19266=ORIENTED_EDGE('',*,*,#14505,.T.);
#19267=ORIENTED_EDGE('',*,*,#14512,.T.);
#19268=ORIENTED_EDGE('',*,*,#14513,.T.);
#19269=ORIENTED_EDGE('',*,*,#14514,.F.);
#19270=ORIENTED_EDGE('',*,*,#14515,.T.);
#19271=ORIENTED_EDGE('',*,*,#14516,.F.);
#19272=ORIENTED_EDGE('',*,*,#14517,.T.);
#19273=ORIENTED_EDGE('',*,*,#14518,.F.);
#19274=ORIENTED_EDGE('',*,*,#14519,.T.);
#19275=ORIENTED_EDGE('',*,*,#14514,.T.);
#19276=ORIENTED_EDGE('',*,*,#14520,.T.);
#19277=ORIENTED_EDGE('',*,*,#14521,.F.);
#19278=ORIENTED_EDGE('',*,*,#14522,.T.);
#19279=ORIENTED_EDGE('',*,*,#14518,.T.);
#19280=ORIENTED_EDGE('',*,*,#14523,.T.);
#19281=ORIENTED_EDGE('',*,*,#14524,.F.);
#19282=ORIENTED_EDGE('',*,*,#14525,.T.);
#19283=ORIENTED_EDGE('',*,*,#14521,.T.);
#19284=ORIENTED_EDGE('',*,*,#14526,.T.);
#19285=ORIENTED_EDGE('',*,*,#14527,.F.);
#19286=ORIENTED_EDGE('',*,*,#14528,.T.);
#19287=ORIENTED_EDGE('',*,*,#14524,.T.);
#19288=ORIENTED_EDGE('',*,*,#14529,.T.);
#19289=ORIENTED_EDGE('',*,*,#14530,.F.);
#19290=ORIENTED_EDGE('',*,*,#14531,.T.);
#19291=ORIENTED_EDGE('',*,*,#14527,.T.);
#19292=ORIENTED_EDGE('',*,*,#14532,.T.);
#19293=ORIENTED_EDGE('',*,*,#14533,.F.);
#19294=ORIENTED_EDGE('',*,*,#14534,.T.);
#19295=ORIENTED_EDGE('',*,*,#14530,.T.);
#19296=ORIENTED_EDGE('',*,*,#14535,.T.);
#19297=ORIENTED_EDGE('',*,*,#14536,.F.);
#19298=ORIENTED_EDGE('',*,*,#14537,.T.);
#19299=ORIENTED_EDGE('',*,*,#14533,.T.);
#19300=ORIENTED_EDGE('',*,*,#14538,.T.);
#19301=ORIENTED_EDGE('',*,*,#14539,.F.);
#19302=ORIENTED_EDGE('',*,*,#14540,.T.);
#19303=ORIENTED_EDGE('',*,*,#14536,.T.);
#19304=ORIENTED_EDGE('',*,*,#14541,.T.);
#19305=ORIENTED_EDGE('',*,*,#14542,.F.);
#19306=ORIENTED_EDGE('',*,*,#14543,.T.);
#19307=ORIENTED_EDGE('',*,*,#14539,.T.);
#19308=ORIENTED_EDGE('',*,*,#14544,.T.);
#19309=ORIENTED_EDGE('',*,*,#14545,.F.);
#19310=ORIENTED_EDGE('',*,*,#14546,.T.);
#19311=ORIENTED_EDGE('',*,*,#14542,.T.);
#19312=ORIENTED_EDGE('',*,*,#14547,.T.);
#19313=ORIENTED_EDGE('',*,*,#14545,.T.);
#19314=ORIENTED_EDGE('',*,*,#14548,.T.);
#19315=ORIENTED_EDGE('',*,*,#14549,.F.);
#19316=ORIENTED_EDGE('',*,*,#14550,.T.);
#19317=ORIENTED_EDGE('',*,*,#14509,.T.);
#19318=ORIENTED_EDGE('',*,*,#14551,.T.);
#19319=ORIENTED_EDGE('',*,*,#14552,.T.);
#19320=ORIENTED_EDGE('',*,*,#14553,.F.);
#19321=ORIENTED_EDGE('',*,*,#14554,.F.);
#19322=ORIENTED_EDGE('',*,*,#14555,.F.);
#19323=ORIENTED_EDGE('',*,*,#14556,.F.);
#19324=ORIENTED_EDGE('',*,*,#14557,.T.);
#19325=ORIENTED_EDGE('',*,*,#14553,.T.);
#19326=ORIENTED_EDGE('',*,*,#14558,.T.);
#19327=ORIENTED_EDGE('',*,*,#14559,.F.);
#19328=ORIENTED_EDGE('',*,*,#14557,.F.);
#19329=ORIENTED_EDGE('',*,*,#14560,.F.);
#19330=ORIENTED_EDGE('',*,*,#14548,.F.);
#19331=ORIENTED_EDGE('',*,*,#14547,.F.);
#19332=ORIENTED_EDGE('',*,*,#14544,.F.);
#19333=ORIENTED_EDGE('',*,*,#14541,.F.);
#19334=ORIENTED_EDGE('',*,*,#14538,.F.);
#19335=ORIENTED_EDGE('',*,*,#14535,.F.);
#19336=ORIENTED_EDGE('',*,*,#14532,.F.);
#19337=ORIENTED_EDGE('',*,*,#14529,.F.);
#19338=ORIENTED_EDGE('',*,*,#14526,.F.);
#19339=ORIENTED_EDGE('',*,*,#14523,.F.);
#19340=ORIENTED_EDGE('',*,*,#14520,.F.);
#19341=ORIENTED_EDGE('',*,*,#14517,.F.);
#19342=ORIENTED_EDGE('',*,*,#14561,.F.);
#19343=ORIENTED_EDGE('',*,*,#14468,.T.);
#19344=ORIENTED_EDGE('',*,*,#14473,.T.);
#19345=ORIENTED_EDGE('',*,*,#14472,.T.);
#19346=ORIENTED_EDGE('',*,*,#14478,.T.);
#19347=ORIENTED_EDGE('',*,*,#14477,.T.);
#19348=ORIENTED_EDGE('',*,*,#14482,.T.);
#19349=ORIENTED_EDGE('',*,*,#14481,.T.);
#19350=ORIENTED_EDGE('',*,*,#14486,.T.);
#19351=ORIENTED_EDGE('',*,*,#14490,.T.);
#19352=ORIENTED_EDGE('',*,*,#14489,.T.);
#19353=ORIENTED_EDGE('',*,*,#14494,.T.);
#19354=ORIENTED_EDGE('',*,*,#14498,.T.);
#19355=ORIENTED_EDGE('',*,*,#14497,.T.);
#19356=ORIENTED_EDGE('',*,*,#14503,.T.);
#19357=ORIENTED_EDGE('',*,*,#14502,.T.);
#19358=ORIENTED_EDGE('',*,*,#14506,.T.);
#19359=ORIENTED_EDGE('',*,*,#14511,.T.);
#19360=ORIENTED_EDGE('',*,*,#14510,.T.);
#19361=ORIENTED_EDGE('',*,*,#14555,.T.);
#19362=ORIENTED_EDGE('',*,*,#14554,.T.);
#19363=ORIENTED_EDGE('',*,*,#14562,.F.);
#19364=ORIENTED_EDGE('',*,*,#14563,.T.);
#19365=ORIENTED_EDGE('',*,*,#14469,.T.);
#19366=ORIENTED_EDGE('',*,*,#14561,.T.);
#19367=ORIENTED_EDGE('',*,*,#14564,.F.);
#19368=ORIENTED_EDGE('',*,*,#14558,.F.);
#19369=ORIENTED_EDGE('',*,*,#14552,.F.);
#19370=ORIENTED_EDGE('',*,*,#14551,.F.);
#19371=ORIENTED_EDGE('',*,*,#14513,.F.);
#19372=ORIENTED_EDGE('',*,*,#14512,.F.);
#19373=ORIENTED_EDGE('',*,*,#14508,.F.);
#19374=ORIENTED_EDGE('',*,*,#14507,.F.);
#19375=ORIENTED_EDGE('',*,*,#14504,.F.);
#19376=ORIENTED_EDGE('',*,*,#14500,.F.);
#19377=ORIENTED_EDGE('',*,*,#14499,.F.);
#19378=ORIENTED_EDGE('',*,*,#14495,.F.);
#19379=ORIENTED_EDGE('',*,*,#14492,.F.);
#19380=ORIENTED_EDGE('',*,*,#14491,.F.);
#19381=ORIENTED_EDGE('',*,*,#14487,.F.);
#19382=ORIENTED_EDGE('',*,*,#14484,.F.);
#19383=ORIENTED_EDGE('',*,*,#14483,.F.);
#19384=ORIENTED_EDGE('',*,*,#14479,.F.);
#19385=ORIENTED_EDGE('',*,*,#14475,.F.);
#19386=ORIENTED_EDGE('',*,*,#14474,.F.);
#19387=ORIENTED_EDGE('',*,*,#14470,.F.);
#19388=ORIENTED_EDGE('',*,*,#14563,.F.);
#19389=ORIENTED_EDGE('',*,*,#14565,.F.);
#19390=ORIENTED_EDGE('',*,*,#14515,.F.);
#19391=ORIENTED_EDGE('',*,*,#14519,.F.);
#19392=ORIENTED_EDGE('',*,*,#14522,.F.);
#19393=ORIENTED_EDGE('',*,*,#14525,.F.);
#19394=ORIENTED_EDGE('',*,*,#14528,.F.);
#19395=ORIENTED_EDGE('',*,*,#14531,.F.);
#19396=ORIENTED_EDGE('',*,*,#14534,.F.);
#19397=ORIENTED_EDGE('',*,*,#14537,.F.);
#19398=ORIENTED_EDGE('',*,*,#14540,.F.);
#19399=ORIENTED_EDGE('',*,*,#14543,.F.);
#19400=ORIENTED_EDGE('',*,*,#14546,.F.);
#19401=ORIENTED_EDGE('',*,*,#14550,.F.);
#19402=ORIENTED_EDGE('',*,*,#14566,.T.);
#19403=ORIENTED_EDGE('',*,*,#14567,.T.);
#19404=ORIENTED_EDGE('',*,*,#14564,.T.);
#19405=ORIENTED_EDGE('',*,*,#14516,.T.);
#19406=ORIENTED_EDGE('',*,*,#14565,.T.);
#19407=ORIENTED_EDGE('',*,*,#14562,.T.);
#19408=ORIENTED_EDGE('',*,*,#14567,.F.);
#19409=ORIENTED_EDGE('',*,*,#14568,.F.);
#19410=ORIENTED_EDGE('',*,*,#14566,.F.);
#19411=ORIENTED_EDGE('',*,*,#14556,.T.);
#19412=ORIENTED_EDGE('',*,*,#14569,.T.);
#19413=ORIENTED_EDGE('',*,*,#14570,.T.);
#19414=ORIENTED_EDGE('',*,*,#14569,.F.);
#19415=ORIENTED_EDGE('',*,*,#14559,.T.);
#19416=ORIENTED_EDGE('',*,*,#14549,.T.);
#19417=ORIENTED_EDGE('',*,*,#14560,.T.);
#19418=ORIENTED_EDGE('',*,*,#14570,.F.);
#19419=ORIENTED_EDGE('',*,*,#14571,.F.);
#19420=ORIENTED_EDGE('',*,*,#14572,.T.);
#19421=ORIENTED_EDGE('',*,*,#14573,.T.);
#19422=ORIENTED_EDGE('',*,*,#14574,.F.);
#19423=ORIENTED_EDGE('',*,*,#14575,.F.);
#19424=ORIENTED_EDGE('',*,*,#14573,.F.);
#19425=ORIENTED_EDGE('',*,*,#14576,.F.);
#19426=ORIENTED_EDGE('',*,*,#14577,.F.);
#19427=ORIENTED_EDGE('',*,*,#14578,.F.);
#19428=ORIENTED_EDGE('',*,*,#14576,.T.);
#19429=ORIENTED_EDGE('',*,*,#14572,.F.);
#19430=ORIENTED_EDGE('',*,*,#14579,.T.);
#19431=ORIENTED_EDGE('',*,*,#14580,.T.);
#19432=ORIENTED_EDGE('',*,*,#14581,.F.);
#19433=ORIENTED_EDGE('',*,*,#14582,.F.);
#19434=ORIENTED_EDGE('',*,*,#14580,.F.);
#19435=ORIENTED_EDGE('',*,*,#14583,.T.);
#19436=ORIENTED_EDGE('',*,*,#14584,.T.);
#19437=ORIENTED_EDGE('',*,*,#14585,.F.);
#19438=ORIENTED_EDGE('',*,*,#14586,.T.);
#19439=ORIENTED_EDGE('',*,*,#14587,.T.);
#19440=ORIENTED_EDGE('',*,*,#14588,.T.);
#19441=ORIENTED_EDGE('',*,*,#14589,.F.);
#19442=ORIENTED_EDGE('',*,*,#14590,.T.);
#19443=ORIENTED_EDGE('',*,*,#14591,.T.);
#19444=ORIENTED_EDGE('',*,*,#14592,.T.);
#19445=ORIENTED_EDGE('',*,*,#14593,.F.);
#19446=ORIENTED_EDGE('',*,*,#14594,.T.);
#19447=ORIENTED_EDGE('',*,*,#14595,.T.);
#19448=ORIENTED_EDGE('',*,*,#14596,.T.);
#19449=ORIENTED_EDGE('',*,*,#14597,.F.);
#19450=ORIENTED_EDGE('',*,*,#14598,.T.);
#19451=ORIENTED_EDGE('',*,*,#14599,.T.);
#19452=ORIENTED_EDGE('',*,*,#14600,.T.);
#19453=ORIENTED_EDGE('',*,*,#14601,.F.);
#19454=ORIENTED_EDGE('',*,*,#14602,.T.);
#19455=ORIENTED_EDGE('',*,*,#14603,.T.);
#19456=ORIENTED_EDGE('',*,*,#14604,.T.);
#19457=ORIENTED_EDGE('',*,*,#14605,.F.);
#19458=ORIENTED_EDGE('',*,*,#14606,.T.);
#19459=ORIENTED_EDGE('',*,*,#14607,.T.);
#19460=ORIENTED_EDGE('',*,*,#14608,.T.);
#19461=ORIENTED_EDGE('',*,*,#14609,.F.);
#19462=ORIENTED_EDGE('',*,*,#14610,.T.);
#19463=ORIENTED_EDGE('',*,*,#14611,.T.);
#19464=ORIENTED_EDGE('',*,*,#14612,.T.);
#19465=ORIENTED_EDGE('',*,*,#14613,.F.);
#19466=ORIENTED_EDGE('',*,*,#14614,.T.);
#19467=ORIENTED_EDGE('',*,*,#14615,.T.);
#19468=ORIENTED_EDGE('',*,*,#14616,.T.);
#19469=ORIENTED_EDGE('',*,*,#14617,.F.);
#19470=ORIENTED_EDGE('',*,*,#14618,.T.);
#19471=ORIENTED_EDGE('',*,*,#14619,.T.);
#19472=ORIENTED_EDGE('',*,*,#14620,.T.);
#19473=ORIENTED_EDGE('',*,*,#14621,.F.);
#19474=ORIENTED_EDGE('',*,*,#14622,.T.);
#19475=ORIENTED_EDGE('',*,*,#14623,.T.);
#19476=ORIENTED_EDGE('',*,*,#14624,.T.);
#19477=ORIENTED_EDGE('',*,*,#14625,.F.);
#19478=ORIENTED_EDGE('',*,*,#14626,.T.);
#19479=ORIENTED_EDGE('',*,*,#14627,.T.);
#19480=ORIENTED_EDGE('',*,*,#14628,.T.);
#19481=ORIENTED_EDGE('',*,*,#14629,.F.);
#19482=ORIENTED_EDGE('',*,*,#14630,.T.);
#19483=ORIENTED_EDGE('',*,*,#14631,.T.);
#19484=ORIENTED_EDGE('',*,*,#14632,.T.);
#19485=ORIENTED_EDGE('',*,*,#14633,.F.);
#19486=ORIENTED_EDGE('',*,*,#14634,.T.);
#19487=ORIENTED_EDGE('',*,*,#14635,.T.);
#19488=ORIENTED_EDGE('',*,*,#14636,.T.);
#19489=ORIENTED_EDGE('',*,*,#14637,.F.);
#19490=ORIENTED_EDGE('',*,*,#14638,.T.);
#19491=ORIENTED_EDGE('',*,*,#14639,.T.);
#19492=ORIENTED_EDGE('',*,*,#14640,.T.);
#19493=ORIENTED_EDGE('',*,*,#14641,.F.);
#19494=ORIENTED_EDGE('',*,*,#14642,.T.);
#19495=ORIENTED_EDGE('',*,*,#14643,.T.);
#19496=ORIENTED_EDGE('',*,*,#14644,.T.);
#19497=ORIENTED_EDGE('',*,*,#14645,.F.);
#19498=ORIENTED_EDGE('',*,*,#14646,.T.);
#19499=ORIENTED_EDGE('',*,*,#14647,.T.);
#19500=ORIENTED_EDGE('',*,*,#14648,.T.);
#19501=ORIENTED_EDGE('',*,*,#14649,.F.);
#19502=ORIENTED_EDGE('',*,*,#14574,.T.);
#19503=ORIENTED_EDGE('',*,*,#14575,.T.);
#19504=ORIENTED_EDGE('',*,*,#14578,.T.);
#19505=ORIENTED_EDGE('',*,*,#14650,.F.);
#19506=ORIENTED_EDGE('',*,*,#14651,.T.);
#19507=ORIENTED_EDGE('',*,*,#14652,.T.);
#19508=ORIENTED_EDGE('',*,*,#14653,.T.);
#19509=ORIENTED_EDGE('',*,*,#14654,.F.);
#19510=ORIENTED_EDGE('',*,*,#14655,.T.);
#19511=ORIENTED_EDGE('',*,*,#14656,.T.);
#19512=ORIENTED_EDGE('',*,*,#14657,.T.);
#19513=ORIENTED_EDGE('',*,*,#14658,.F.);
#19514=ORIENTED_EDGE('',*,*,#14659,.T.);
#19515=ORIENTED_EDGE('',*,*,#14660,.T.);
#19516=ORIENTED_EDGE('',*,*,#14661,.T.);
#19517=ORIENTED_EDGE('',*,*,#14662,.F.);
#19518=ORIENTED_EDGE('',*,*,#14663,.T.);
#19519=ORIENTED_EDGE('',*,*,#14664,.T.);
#19520=ORIENTED_EDGE('',*,*,#14665,.T.);
#19521=ORIENTED_EDGE('',*,*,#14666,.F.);
#19522=ORIENTED_EDGE('',*,*,#14667,.T.);
#19523=ORIENTED_EDGE('',*,*,#14668,.T.);
#19524=ORIENTED_EDGE('',*,*,#14669,.T.);
#19525=ORIENTED_EDGE('',*,*,#14670,.F.);
#19526=ORIENTED_EDGE('',*,*,#14671,.T.);
#19527=ORIENTED_EDGE('',*,*,#14672,.T.);
#19528=ORIENTED_EDGE('',*,*,#14673,.T.);
#19529=ORIENTED_EDGE('',*,*,#14674,.F.);
#19530=ORIENTED_EDGE('',*,*,#14675,.T.);
#19531=ORIENTED_EDGE('',*,*,#14676,.T.);
#19532=ORIENTED_EDGE('',*,*,#14677,.T.);
#19533=ORIENTED_EDGE('',*,*,#14678,.F.);
#19534=ORIENTED_EDGE('',*,*,#14679,.T.);
#19535=ORIENTED_EDGE('',*,*,#14680,.T.);
#19536=ORIENTED_EDGE('',*,*,#14681,.T.);
#19537=ORIENTED_EDGE('',*,*,#14682,.F.);
#19538=ORIENTED_EDGE('',*,*,#14683,.T.);
#19539=ORIENTED_EDGE('',*,*,#14684,.T.);
#19540=ORIENTED_EDGE('',*,*,#14685,.T.);
#19541=ORIENTED_EDGE('',*,*,#14686,.F.);
#19542=ORIENTED_EDGE('',*,*,#14687,.T.);
#19543=ORIENTED_EDGE('',*,*,#14688,.T.);
#19544=ORIENTED_EDGE('',*,*,#14689,.T.);
#19545=ORIENTED_EDGE('',*,*,#14690,.F.);
#19546=ORIENTED_EDGE('',*,*,#14691,.T.);
#19547=ORIENTED_EDGE('',*,*,#14692,.T.);
#19548=ORIENTED_EDGE('',*,*,#14693,.T.);
#19549=ORIENTED_EDGE('',*,*,#14694,.F.);
#19550=ORIENTED_EDGE('',*,*,#14695,.T.);
#19551=ORIENTED_EDGE('',*,*,#14696,.T.);
#19552=ORIENTED_EDGE('',*,*,#14697,.T.);
#19553=ORIENTED_EDGE('',*,*,#14698,.F.);
#19554=ORIENTED_EDGE('',*,*,#14699,.T.);
#19555=ORIENTED_EDGE('',*,*,#14700,.T.);
#19556=ORIENTED_EDGE('',*,*,#14701,.T.);
#19557=ORIENTED_EDGE('',*,*,#14702,.F.);
#19558=ORIENTED_EDGE('',*,*,#14703,.T.);
#19559=ORIENTED_EDGE('',*,*,#14704,.T.);
#19560=ORIENTED_EDGE('',*,*,#14705,.T.);
#19561=ORIENTED_EDGE('',*,*,#14706,.F.);
#19562=ORIENTED_EDGE('',*,*,#14707,.T.);
#19563=ORIENTED_EDGE('',*,*,#14708,.T.);
#19564=ORIENTED_EDGE('',*,*,#14709,.T.);
#19565=ORIENTED_EDGE('',*,*,#14710,.F.);
#19566=ORIENTED_EDGE('',*,*,#14711,.T.);
#19567=ORIENTED_EDGE('',*,*,#14712,.T.);
#19568=ORIENTED_EDGE('',*,*,#14713,.T.);
#19569=ORIENTED_EDGE('',*,*,#14714,.F.);
#19570=ORIENTED_EDGE('',*,*,#14715,.T.);
#19571=ORIENTED_EDGE('',*,*,#14716,.T.);
#19572=ORIENTED_EDGE('',*,*,#14717,.T.);
#19573=ORIENTED_EDGE('',*,*,#14718,.F.);
#19574=ORIENTED_EDGE('',*,*,#14719,.T.);
#19575=ORIENTED_EDGE('',*,*,#14720,.T.);
#19576=ORIENTED_EDGE('',*,*,#14721,.T.);
#19577=ORIENTED_EDGE('',*,*,#14722,.F.);
#19578=ORIENTED_EDGE('',*,*,#14723,.T.);
#19579=ORIENTED_EDGE('',*,*,#14724,.F.);
#19580=ORIENTED_EDGE('',*,*,#14725,.T.);
#19581=ORIENTED_EDGE('',*,*,#14726,.T.);
#19582=ORIENTED_EDGE('',*,*,#14646,.F.);
#19583=ORIENTED_EDGE('',*,*,#14647,.F.);
#19584=ORIENTED_EDGE('',*,*,#14726,.F.);
#19585=ORIENTED_EDGE('',*,*,#14727,.F.);
#19586=ORIENTED_EDGE('',*,*,#14728,.F.);
#19587=ORIENTED_EDGE('',*,*,#14648,.F.);
#19588=ORIENTED_EDGE('',*,*,#14727,.T.);
#19589=ORIENTED_EDGE('',*,*,#14725,.F.);
#19590=ORIENTED_EDGE('',*,*,#14729,.F.);
#19591=ORIENTED_EDGE('',*,*,#14730,.T.);
#19592=ORIENTED_EDGE('',*,*,#14731,.T.);
#19593=ORIENTED_EDGE('',*,*,#14642,.F.);
#19594=ORIENTED_EDGE('',*,*,#14643,.F.);
#19595=ORIENTED_EDGE('',*,*,#14731,.F.);
#19596=ORIENTED_EDGE('',*,*,#14732,.F.);
#19597=ORIENTED_EDGE('',*,*,#14733,.F.);
#19598=ORIENTED_EDGE('',*,*,#14644,.F.);
#19599=ORIENTED_EDGE('',*,*,#14732,.T.);
#19600=ORIENTED_EDGE('',*,*,#14730,.F.);
#19601=ORIENTED_EDGE('',*,*,#14734,.F.);
#19602=ORIENTED_EDGE('',*,*,#14735,.T.);
#19603=ORIENTED_EDGE('',*,*,#14736,.T.);
#19604=ORIENTED_EDGE('',*,*,#14638,.F.);
#19605=ORIENTED_EDGE('',*,*,#14639,.F.);
#19606=ORIENTED_EDGE('',*,*,#14736,.F.);
#19607=ORIENTED_EDGE('',*,*,#14737,.F.);
#19608=ORIENTED_EDGE('',*,*,#14738,.F.);
#19609=ORIENTED_EDGE('',*,*,#14640,.F.);
#19610=ORIENTED_EDGE('',*,*,#14737,.T.);
#19611=ORIENTED_EDGE('',*,*,#14735,.F.);
#19612=ORIENTED_EDGE('',*,*,#14739,.F.);
#19613=ORIENTED_EDGE('',*,*,#14740,.T.);
#19614=ORIENTED_EDGE('',*,*,#14741,.T.);
#19615=ORIENTED_EDGE('',*,*,#14634,.F.);
#19616=ORIENTED_EDGE('',*,*,#14635,.F.);
#19617=ORIENTED_EDGE('',*,*,#14741,.F.);
#19618=ORIENTED_EDGE('',*,*,#14742,.F.);
#19619=ORIENTED_EDGE('',*,*,#14743,.F.);
#19620=ORIENTED_EDGE('',*,*,#14636,.F.);
#19621=ORIENTED_EDGE('',*,*,#14742,.T.);
#19622=ORIENTED_EDGE('',*,*,#14740,.F.);
#19623=ORIENTED_EDGE('',*,*,#14744,.F.);
#19624=ORIENTED_EDGE('',*,*,#14745,.T.);
#19625=ORIENTED_EDGE('',*,*,#14746,.T.);
#19626=ORIENTED_EDGE('',*,*,#14630,.F.);
#19627=ORIENTED_EDGE('',*,*,#14631,.F.);
#19628=ORIENTED_EDGE('',*,*,#14746,.F.);
#19629=ORIENTED_EDGE('',*,*,#14747,.F.);
#19630=ORIENTED_EDGE('',*,*,#14748,.F.);
#19631=ORIENTED_EDGE('',*,*,#14632,.F.);
#19632=ORIENTED_EDGE('',*,*,#14747,.T.);
#19633=ORIENTED_EDGE('',*,*,#14745,.F.);
#19634=ORIENTED_EDGE('',*,*,#14749,.F.);
#19635=ORIENTED_EDGE('',*,*,#14750,.T.);
#19636=ORIENTED_EDGE('',*,*,#14751,.T.);
#19637=ORIENTED_EDGE('',*,*,#14626,.F.);
#19638=ORIENTED_EDGE('',*,*,#14627,.F.);
#19639=ORIENTED_EDGE('',*,*,#14751,.F.);
#19640=ORIENTED_EDGE('',*,*,#14752,.F.);
#19641=ORIENTED_EDGE('',*,*,#14753,.F.);
#19642=ORIENTED_EDGE('',*,*,#14628,.F.);
#19643=ORIENTED_EDGE('',*,*,#14752,.T.);
#19644=ORIENTED_EDGE('',*,*,#14750,.F.);
#19645=ORIENTED_EDGE('',*,*,#14754,.F.);
#19646=ORIENTED_EDGE('',*,*,#14755,.T.);
#19647=ORIENTED_EDGE('',*,*,#14756,.T.);
#19648=ORIENTED_EDGE('',*,*,#14622,.F.);
#19649=ORIENTED_EDGE('',*,*,#14623,.F.);
#19650=ORIENTED_EDGE('',*,*,#14756,.F.);
#19651=ORIENTED_EDGE('',*,*,#14757,.F.);
#19652=ORIENTED_EDGE('',*,*,#14758,.F.);
#19653=ORIENTED_EDGE('',*,*,#14624,.F.);
#19654=ORIENTED_EDGE('',*,*,#14757,.T.);
#19655=ORIENTED_EDGE('',*,*,#14755,.F.);
#19656=ORIENTED_EDGE('',*,*,#14759,.F.);
#19657=ORIENTED_EDGE('',*,*,#14760,.T.);
#19658=ORIENTED_EDGE('',*,*,#14761,.T.);
#19659=ORIENTED_EDGE('',*,*,#14618,.F.);
#19660=ORIENTED_EDGE('',*,*,#14619,.F.);
#19661=ORIENTED_EDGE('',*,*,#14761,.F.);
#19662=ORIENTED_EDGE('',*,*,#14762,.F.);
#19663=ORIENTED_EDGE('',*,*,#14763,.F.);
#19664=ORIENTED_EDGE('',*,*,#14620,.F.);
#19665=ORIENTED_EDGE('',*,*,#14762,.T.);
#19666=ORIENTED_EDGE('',*,*,#14760,.F.);
#19667=ORIENTED_EDGE('',*,*,#14764,.F.);
#19668=ORIENTED_EDGE('',*,*,#14765,.T.);
#19669=ORIENTED_EDGE('',*,*,#14766,.T.);
#19670=ORIENTED_EDGE('',*,*,#14614,.F.);
#19671=ORIENTED_EDGE('',*,*,#14615,.F.);
#19672=ORIENTED_EDGE('',*,*,#14766,.F.);
#19673=ORIENTED_EDGE('',*,*,#14767,.F.);
#19674=ORIENTED_EDGE('',*,*,#14768,.F.);
#19675=ORIENTED_EDGE('',*,*,#14616,.F.);
#19676=ORIENTED_EDGE('',*,*,#14767,.T.);
#19677=ORIENTED_EDGE('',*,*,#14765,.F.);
#19678=ORIENTED_EDGE('',*,*,#14769,.F.);
#19679=ORIENTED_EDGE('',*,*,#14770,.T.);
#19680=ORIENTED_EDGE('',*,*,#14771,.T.);
#19681=ORIENTED_EDGE('',*,*,#14610,.F.);
#19682=ORIENTED_EDGE('',*,*,#14611,.F.);
#19683=ORIENTED_EDGE('',*,*,#14771,.F.);
#19684=ORIENTED_EDGE('',*,*,#14772,.F.);
#19685=ORIENTED_EDGE('',*,*,#14773,.F.);
#19686=ORIENTED_EDGE('',*,*,#14612,.F.);
#19687=ORIENTED_EDGE('',*,*,#14772,.T.);
#19688=ORIENTED_EDGE('',*,*,#14770,.F.);
#19689=ORIENTED_EDGE('',*,*,#14774,.F.);
#19690=ORIENTED_EDGE('',*,*,#14775,.T.);
#19691=ORIENTED_EDGE('',*,*,#14776,.T.);
#19692=ORIENTED_EDGE('',*,*,#14606,.F.);
#19693=ORIENTED_EDGE('',*,*,#14607,.F.);
#19694=ORIENTED_EDGE('',*,*,#14776,.F.);
#19695=ORIENTED_EDGE('',*,*,#14777,.F.);
#19696=ORIENTED_EDGE('',*,*,#14778,.F.);
#19697=ORIENTED_EDGE('',*,*,#14608,.F.);
#19698=ORIENTED_EDGE('',*,*,#14777,.T.);
#19699=ORIENTED_EDGE('',*,*,#14775,.F.);
#19700=ORIENTED_EDGE('',*,*,#14779,.F.);
#19701=ORIENTED_EDGE('',*,*,#14780,.T.);
#19702=ORIENTED_EDGE('',*,*,#14781,.T.);
#19703=ORIENTED_EDGE('',*,*,#14602,.F.);
#19704=ORIENTED_EDGE('',*,*,#14603,.F.);
#19705=ORIENTED_EDGE('',*,*,#14781,.F.);
#19706=ORIENTED_EDGE('',*,*,#14782,.F.);
#19707=ORIENTED_EDGE('',*,*,#14783,.F.);
#19708=ORIENTED_EDGE('',*,*,#14604,.F.);
#19709=ORIENTED_EDGE('',*,*,#14782,.T.);
#19710=ORIENTED_EDGE('',*,*,#14780,.F.);
#19711=ORIENTED_EDGE('',*,*,#14784,.F.);
#19712=ORIENTED_EDGE('',*,*,#14785,.T.);
#19713=ORIENTED_EDGE('',*,*,#14786,.T.);
#19714=ORIENTED_EDGE('',*,*,#14598,.F.);
#19715=ORIENTED_EDGE('',*,*,#14599,.F.);
#19716=ORIENTED_EDGE('',*,*,#14786,.F.);
#19717=ORIENTED_EDGE('',*,*,#14787,.F.);
#19718=ORIENTED_EDGE('',*,*,#14788,.F.);
#19719=ORIENTED_EDGE('',*,*,#14600,.F.);
#19720=ORIENTED_EDGE('',*,*,#14787,.T.);
#19721=ORIENTED_EDGE('',*,*,#14785,.F.);
#19722=ORIENTED_EDGE('',*,*,#14789,.F.);
#19723=ORIENTED_EDGE('',*,*,#14790,.T.);
#19724=ORIENTED_EDGE('',*,*,#14791,.T.);
#19725=ORIENTED_EDGE('',*,*,#14594,.F.);
#19726=ORIENTED_EDGE('',*,*,#14595,.F.);
#19727=ORIENTED_EDGE('',*,*,#14791,.F.);
#19728=ORIENTED_EDGE('',*,*,#14792,.F.);
#19729=ORIENTED_EDGE('',*,*,#14793,.F.);
#19730=ORIENTED_EDGE('',*,*,#14596,.F.);
#19731=ORIENTED_EDGE('',*,*,#14792,.T.);
#19732=ORIENTED_EDGE('',*,*,#14790,.F.);
#19733=ORIENTED_EDGE('',*,*,#14794,.F.);
#19734=ORIENTED_EDGE('',*,*,#14795,.T.);
#19735=ORIENTED_EDGE('',*,*,#14796,.T.);
#19736=ORIENTED_EDGE('',*,*,#14590,.F.);
#19737=ORIENTED_EDGE('',*,*,#14591,.F.);
#19738=ORIENTED_EDGE('',*,*,#14796,.F.);
#19739=ORIENTED_EDGE('',*,*,#14797,.F.);
#19740=ORIENTED_EDGE('',*,*,#14798,.F.);
#19741=ORIENTED_EDGE('',*,*,#14592,.F.);
#19742=ORIENTED_EDGE('',*,*,#14797,.T.);
#19743=ORIENTED_EDGE('',*,*,#14795,.F.);
#19744=ORIENTED_EDGE('',*,*,#14799,.F.);
#19745=ORIENTED_EDGE('',*,*,#14800,.T.);
#19746=ORIENTED_EDGE('',*,*,#14801,.T.);
#19747=ORIENTED_EDGE('',*,*,#14586,.F.);
#19748=ORIENTED_EDGE('',*,*,#14587,.F.);
#19749=ORIENTED_EDGE('',*,*,#14801,.F.);
#19750=ORIENTED_EDGE('',*,*,#14802,.F.);
#19751=ORIENTED_EDGE('',*,*,#14803,.F.);
#19752=ORIENTED_EDGE('',*,*,#14588,.F.);
#19753=ORIENTED_EDGE('',*,*,#14802,.T.);
#19754=ORIENTED_EDGE('',*,*,#14800,.F.);
#19755=ORIENTED_EDGE('',*,*,#14804,.F.);
#19756=ORIENTED_EDGE('',*,*,#14805,.T.);
#19757=ORIENTED_EDGE('',*,*,#14806,.T.);
#19758=ORIENTED_EDGE('',*,*,#14723,.F.);
#19759=ORIENTED_EDGE('',*,*,#14579,.F.);
#19760=ORIENTED_EDGE('',*,*,#14806,.F.);
#19761=ORIENTED_EDGE('',*,*,#14807,.F.);
#19762=ORIENTED_EDGE('',*,*,#14583,.F.);
#19763=ORIENTED_EDGE('',*,*,#14808,.F.);
#19764=ORIENTED_EDGE('',*,*,#14584,.F.);
#19765=ORIENTED_EDGE('',*,*,#14807,.T.);
#19766=ORIENTED_EDGE('',*,*,#14805,.F.);
#19767=ORIENTED_EDGE('',*,*,#14809,.F.);
#19768=ORIENTED_EDGE('',*,*,#14810,.T.);
#19769=ORIENTED_EDGE('',*,*,#14811,.T.);
#19770=ORIENTED_EDGE('',*,*,#14719,.F.);
#19771=ORIENTED_EDGE('',*,*,#14720,.F.);
#19772=ORIENTED_EDGE('',*,*,#14811,.F.);
#19773=ORIENTED_EDGE('',*,*,#14812,.F.);
#19774=ORIENTED_EDGE('',*,*,#14813,.F.);
#19775=ORIENTED_EDGE('',*,*,#14721,.F.);
#19776=ORIENTED_EDGE('',*,*,#14812,.T.);
#19777=ORIENTED_EDGE('',*,*,#14810,.F.);
#19778=ORIENTED_EDGE('',*,*,#14814,.F.);
#19779=ORIENTED_EDGE('',*,*,#14815,.T.);
#19780=ORIENTED_EDGE('',*,*,#14816,.T.);
#19781=ORIENTED_EDGE('',*,*,#14715,.F.);
#19782=ORIENTED_EDGE('',*,*,#14716,.F.);
#19783=ORIENTED_EDGE('',*,*,#14816,.F.);
#19784=ORIENTED_EDGE('',*,*,#14817,.F.);
#19785=ORIENTED_EDGE('',*,*,#14818,.F.);
#19786=ORIENTED_EDGE('',*,*,#14717,.F.);
#19787=ORIENTED_EDGE('',*,*,#14817,.T.);
#19788=ORIENTED_EDGE('',*,*,#14815,.F.);
#19789=ORIENTED_EDGE('',*,*,#14819,.F.);
#19790=ORIENTED_EDGE('',*,*,#14820,.T.);
#19791=ORIENTED_EDGE('',*,*,#14821,.T.);
#19792=ORIENTED_EDGE('',*,*,#14711,.F.);
#19793=ORIENTED_EDGE('',*,*,#14712,.F.);
#19794=ORIENTED_EDGE('',*,*,#14821,.F.);
#19795=ORIENTED_EDGE('',*,*,#14822,.F.);
#19796=ORIENTED_EDGE('',*,*,#14823,.F.);
#19797=ORIENTED_EDGE('',*,*,#14713,.F.);
#19798=ORIENTED_EDGE('',*,*,#14822,.T.);
#19799=ORIENTED_EDGE('',*,*,#14820,.F.);
#19800=ORIENTED_EDGE('',*,*,#14824,.F.);
#19801=ORIENTED_EDGE('',*,*,#14825,.T.);
#19802=ORIENTED_EDGE('',*,*,#14826,.T.);
#19803=ORIENTED_EDGE('',*,*,#14707,.F.);
#19804=ORIENTED_EDGE('',*,*,#14708,.F.);
#19805=ORIENTED_EDGE('',*,*,#14826,.F.);
#19806=ORIENTED_EDGE('',*,*,#14827,.F.);
#19807=ORIENTED_EDGE('',*,*,#14828,.F.);
#19808=ORIENTED_EDGE('',*,*,#14709,.F.);
#19809=ORIENTED_EDGE('',*,*,#14827,.T.);
#19810=ORIENTED_EDGE('',*,*,#14825,.F.);
#19811=ORIENTED_EDGE('',*,*,#14829,.F.);
#19812=ORIENTED_EDGE('',*,*,#14830,.T.);
#19813=ORIENTED_EDGE('',*,*,#14831,.T.);
#19814=ORIENTED_EDGE('',*,*,#14703,.F.);
#19815=ORIENTED_EDGE('',*,*,#14704,.F.);
#19816=ORIENTED_EDGE('',*,*,#14831,.F.);
#19817=ORIENTED_EDGE('',*,*,#14832,.F.);
#19818=ORIENTED_EDGE('',*,*,#14833,.F.);
#19819=ORIENTED_EDGE('',*,*,#14705,.F.);
#19820=ORIENTED_EDGE('',*,*,#14832,.T.);
#19821=ORIENTED_EDGE('',*,*,#14830,.F.);
#19822=ORIENTED_EDGE('',*,*,#14834,.F.);
#19823=ORIENTED_EDGE('',*,*,#14835,.T.);
#19824=ORIENTED_EDGE('',*,*,#14836,.T.);
#19825=ORIENTED_EDGE('',*,*,#14699,.F.);
#19826=ORIENTED_EDGE('',*,*,#14700,.F.);
#19827=ORIENTED_EDGE('',*,*,#14836,.F.);
#19828=ORIENTED_EDGE('',*,*,#14837,.F.);
#19829=ORIENTED_EDGE('',*,*,#14838,.F.);
#19830=ORIENTED_EDGE('',*,*,#14701,.F.);
#19831=ORIENTED_EDGE('',*,*,#14837,.T.);
#19832=ORIENTED_EDGE('',*,*,#14835,.F.);
#19833=ORIENTED_EDGE('',*,*,#14839,.F.);
#19834=ORIENTED_EDGE('',*,*,#14840,.T.);
#19835=ORIENTED_EDGE('',*,*,#14841,.T.);
#19836=ORIENTED_EDGE('',*,*,#14695,.F.);
#19837=ORIENTED_EDGE('',*,*,#14696,.F.);
#19838=ORIENTED_EDGE('',*,*,#14841,.F.);
#19839=ORIENTED_EDGE('',*,*,#14842,.F.);
#19840=ORIENTED_EDGE('',*,*,#14843,.F.);
#19841=ORIENTED_EDGE('',*,*,#14697,.F.);
#19842=ORIENTED_EDGE('',*,*,#14842,.T.);
#19843=ORIENTED_EDGE('',*,*,#14840,.F.);
#19844=ORIENTED_EDGE('',*,*,#14844,.F.);
#19845=ORIENTED_EDGE('',*,*,#14845,.T.);
#19846=ORIENTED_EDGE('',*,*,#14846,.T.);
#19847=ORIENTED_EDGE('',*,*,#14691,.F.);
#19848=ORIENTED_EDGE('',*,*,#14692,.F.);
#19849=ORIENTED_EDGE('',*,*,#14846,.F.);
#19850=ORIENTED_EDGE('',*,*,#14847,.F.);
#19851=ORIENTED_EDGE('',*,*,#14848,.F.);
#19852=ORIENTED_EDGE('',*,*,#14693,.F.);
#19853=ORIENTED_EDGE('',*,*,#14847,.T.);
#19854=ORIENTED_EDGE('',*,*,#14845,.F.);
#19855=ORIENTED_EDGE('',*,*,#14849,.F.);
#19856=ORIENTED_EDGE('',*,*,#14850,.T.);
#19857=ORIENTED_EDGE('',*,*,#14851,.T.);
#19858=ORIENTED_EDGE('',*,*,#14687,.F.);
#19859=ORIENTED_EDGE('',*,*,#14688,.F.);
#19860=ORIENTED_EDGE('',*,*,#14851,.F.);
#19861=ORIENTED_EDGE('',*,*,#14852,.F.);
#19862=ORIENTED_EDGE('',*,*,#14853,.F.);
#19863=ORIENTED_EDGE('',*,*,#14689,.F.);
#19864=ORIENTED_EDGE('',*,*,#14852,.T.);
#19865=ORIENTED_EDGE('',*,*,#14850,.F.);
#19866=ORIENTED_EDGE('',*,*,#14854,.F.);
#19867=ORIENTED_EDGE('',*,*,#14855,.T.);
#19868=ORIENTED_EDGE('',*,*,#14856,.T.);
#19869=ORIENTED_EDGE('',*,*,#14683,.F.);
#19870=ORIENTED_EDGE('',*,*,#14684,.F.);
#19871=ORIENTED_EDGE('',*,*,#14856,.F.);
#19872=ORIENTED_EDGE('',*,*,#14857,.F.);
#19873=ORIENTED_EDGE('',*,*,#14858,.F.);
#19874=ORIENTED_EDGE('',*,*,#14685,.F.);
#19875=ORIENTED_EDGE('',*,*,#14857,.T.);
#19876=ORIENTED_EDGE('',*,*,#14855,.F.);
#19877=ORIENTED_EDGE('',*,*,#14859,.F.);
#19878=ORIENTED_EDGE('',*,*,#14860,.T.);
#19879=ORIENTED_EDGE('',*,*,#14861,.T.);
#19880=ORIENTED_EDGE('',*,*,#14679,.F.);
#19881=ORIENTED_EDGE('',*,*,#14680,.F.);
#19882=ORIENTED_EDGE('',*,*,#14861,.F.);
#19883=ORIENTED_EDGE('',*,*,#14862,.F.);
#19884=ORIENTED_EDGE('',*,*,#14863,.F.);
#19885=ORIENTED_EDGE('',*,*,#14681,.F.);
#19886=ORIENTED_EDGE('',*,*,#14862,.T.);
#19887=ORIENTED_EDGE('',*,*,#14860,.F.);
#19888=ORIENTED_EDGE('',*,*,#14864,.F.);
#19889=ORIENTED_EDGE('',*,*,#14865,.T.);
#19890=ORIENTED_EDGE('',*,*,#14866,.T.);
#19891=ORIENTED_EDGE('',*,*,#14675,.F.);
#19892=ORIENTED_EDGE('',*,*,#14676,.F.);
#19893=ORIENTED_EDGE('',*,*,#14866,.F.);
#19894=ORIENTED_EDGE('',*,*,#14867,.F.);
#19895=ORIENTED_EDGE('',*,*,#14868,.F.);
#19896=ORIENTED_EDGE('',*,*,#14677,.F.);
#19897=ORIENTED_EDGE('',*,*,#14867,.T.);
#19898=ORIENTED_EDGE('',*,*,#14865,.F.);
#19899=ORIENTED_EDGE('',*,*,#14869,.F.);
#19900=ORIENTED_EDGE('',*,*,#14870,.T.);
#19901=ORIENTED_EDGE('',*,*,#14871,.T.);
#19902=ORIENTED_EDGE('',*,*,#14671,.F.);
#19903=ORIENTED_EDGE('',*,*,#14672,.F.);
#19904=ORIENTED_EDGE('',*,*,#14871,.F.);
#19905=ORIENTED_EDGE('',*,*,#14872,.F.);
#19906=ORIENTED_EDGE('',*,*,#14873,.F.);
#19907=ORIENTED_EDGE('',*,*,#14673,.F.);
#19908=ORIENTED_EDGE('',*,*,#14872,.T.);
#19909=ORIENTED_EDGE('',*,*,#14870,.F.);
#19910=ORIENTED_EDGE('',*,*,#14874,.F.);
#19911=ORIENTED_EDGE('',*,*,#14875,.T.);
#19912=ORIENTED_EDGE('',*,*,#14876,.T.);
#19913=ORIENTED_EDGE('',*,*,#14667,.F.);
#19914=ORIENTED_EDGE('',*,*,#14668,.F.);
#19915=ORIENTED_EDGE('',*,*,#14876,.F.);
#19916=ORIENTED_EDGE('',*,*,#14877,.F.);
#19917=ORIENTED_EDGE('',*,*,#14878,.F.);
#19918=ORIENTED_EDGE('',*,*,#14669,.F.);
#19919=ORIENTED_EDGE('',*,*,#14877,.T.);
#19920=ORIENTED_EDGE('',*,*,#14875,.F.);
#19921=ORIENTED_EDGE('',*,*,#14879,.F.);
#19922=ORIENTED_EDGE('',*,*,#14880,.T.);
#19923=ORIENTED_EDGE('',*,*,#14881,.T.);
#19924=ORIENTED_EDGE('',*,*,#14663,.F.);
#19925=ORIENTED_EDGE('',*,*,#14664,.F.);
#19926=ORIENTED_EDGE('',*,*,#14881,.F.);
#19927=ORIENTED_EDGE('',*,*,#14882,.F.);
#19928=ORIENTED_EDGE('',*,*,#14883,.F.);
#19929=ORIENTED_EDGE('',*,*,#14665,.F.);
#19930=ORIENTED_EDGE('',*,*,#14882,.T.);
#19931=ORIENTED_EDGE('',*,*,#14880,.F.);
#19932=ORIENTED_EDGE('',*,*,#14884,.F.);
#19933=ORIENTED_EDGE('',*,*,#14885,.T.);
#19934=ORIENTED_EDGE('',*,*,#14886,.T.);
#19935=ORIENTED_EDGE('',*,*,#14659,.F.);
#19936=ORIENTED_EDGE('',*,*,#14660,.F.);
#19937=ORIENTED_EDGE('',*,*,#14886,.F.);
#19938=ORIENTED_EDGE('',*,*,#14887,.F.);
#19939=ORIENTED_EDGE('',*,*,#14888,.F.);
#19940=ORIENTED_EDGE('',*,*,#14661,.F.);
#19941=ORIENTED_EDGE('',*,*,#14887,.T.);
#19942=ORIENTED_EDGE('',*,*,#14885,.F.);
#19943=ORIENTED_EDGE('',*,*,#14889,.F.);
#19944=ORIENTED_EDGE('',*,*,#14890,.T.);
#19945=ORIENTED_EDGE('',*,*,#14891,.T.);
#19946=ORIENTED_EDGE('',*,*,#14655,.F.);
#19947=ORIENTED_EDGE('',*,*,#14656,.F.);
#19948=ORIENTED_EDGE('',*,*,#14891,.F.);
#19949=ORIENTED_EDGE('',*,*,#14892,.F.);
#19950=ORIENTED_EDGE('',*,*,#14893,.F.);
#19951=ORIENTED_EDGE('',*,*,#14657,.F.);
#19952=ORIENTED_EDGE('',*,*,#14892,.T.);
#19953=ORIENTED_EDGE('',*,*,#14890,.F.);
#19954=ORIENTED_EDGE('',*,*,#14894,.F.);
#19955=ORIENTED_EDGE('',*,*,#14895,.T.);
#19956=ORIENTED_EDGE('',*,*,#14896,.T.);
#19957=ORIENTED_EDGE('',*,*,#14651,.F.);
#19958=ORIENTED_EDGE('',*,*,#14652,.F.);
#19959=ORIENTED_EDGE('',*,*,#14896,.F.);
#19960=ORIENTED_EDGE('',*,*,#14897,.F.);
#19961=ORIENTED_EDGE('',*,*,#14898,.F.);
#19962=ORIENTED_EDGE('',*,*,#14653,.F.);
#19963=ORIENTED_EDGE('',*,*,#14897,.T.);
#19964=ORIENTED_EDGE('',*,*,#14895,.F.);
#19965=ORIENTED_EDGE('',*,*,#14581,.T.);
#19966=ORIENTED_EDGE('',*,*,#14582,.T.);
#19967=ORIENTED_EDGE('',*,*,#14899,.T.);
#19968=ORIENTED_EDGE('',*,*,#14568,.T.);
#19969=ORIENTED_EDGE('',*,*,#14899,.F.);
#19970=ORIENTED_EDGE('',*,*,#14804,.T.);
#19971=ORIENTED_EDGE('',*,*,#14722,.T.);
#19972=ORIENTED_EDGE('',*,*,#14813,.T.);
#19973=ORIENTED_EDGE('',*,*,#14809,.T.);
#19974=ORIENTED_EDGE('',*,*,#14718,.T.);
#19975=ORIENTED_EDGE('',*,*,#14818,.T.);
#19976=ORIENTED_EDGE('',*,*,#14814,.T.);
#19977=ORIENTED_EDGE('',*,*,#14714,.T.);
#19978=ORIENTED_EDGE('',*,*,#14823,.T.);
#19979=ORIENTED_EDGE('',*,*,#14819,.T.);
#19980=ORIENTED_EDGE('',*,*,#14710,.T.);
#19981=ORIENTED_EDGE('',*,*,#14828,.T.);
#19982=ORIENTED_EDGE('',*,*,#14824,.T.);
#19983=ORIENTED_EDGE('',*,*,#14706,.T.);
#19984=ORIENTED_EDGE('',*,*,#14833,.T.);
#19985=ORIENTED_EDGE('',*,*,#14829,.T.);
#19986=ORIENTED_EDGE('',*,*,#14702,.T.);
#19987=ORIENTED_EDGE('',*,*,#14838,.T.);
#19988=ORIENTED_EDGE('',*,*,#14834,.T.);
#19989=ORIENTED_EDGE('',*,*,#14698,.T.);
#19990=ORIENTED_EDGE('',*,*,#14843,.T.);
#19991=ORIENTED_EDGE('',*,*,#14839,.T.);
#19992=ORIENTED_EDGE('',*,*,#14694,.T.);
#19993=ORIENTED_EDGE('',*,*,#14848,.T.);
#19994=ORIENTED_EDGE('',*,*,#14844,.T.);
#19995=ORIENTED_EDGE('',*,*,#14690,.T.);
#19996=ORIENTED_EDGE('',*,*,#14853,.T.);
#19997=ORIENTED_EDGE('',*,*,#14849,.T.);
#19998=ORIENTED_EDGE('',*,*,#14686,.T.);
#19999=ORIENTED_EDGE('',*,*,#14858,.T.);
#20000=ORIENTED_EDGE('',*,*,#14854,.T.);
#20001=ORIENTED_EDGE('',*,*,#14682,.T.);
#20002=ORIENTED_EDGE('',*,*,#14863,.T.);
#20003=ORIENTED_EDGE('',*,*,#14859,.T.);
#20004=ORIENTED_EDGE('',*,*,#14678,.T.);
#20005=ORIENTED_EDGE('',*,*,#14868,.T.);
#20006=ORIENTED_EDGE('',*,*,#14864,.T.);
#20007=ORIENTED_EDGE('',*,*,#14674,.T.);
#20008=ORIENTED_EDGE('',*,*,#14873,.T.);
#20009=ORIENTED_EDGE('',*,*,#14869,.T.);
#20010=ORIENTED_EDGE('',*,*,#14670,.T.);
#20011=ORIENTED_EDGE('',*,*,#14878,.T.);
#20012=ORIENTED_EDGE('',*,*,#14874,.T.);
#20013=ORIENTED_EDGE('',*,*,#14666,.T.);
#20014=ORIENTED_EDGE('',*,*,#14883,.T.);
#20015=ORIENTED_EDGE('',*,*,#14879,.T.);
#20016=ORIENTED_EDGE('',*,*,#14662,.T.);
#20017=ORIENTED_EDGE('',*,*,#14888,.T.);
#20018=ORIENTED_EDGE('',*,*,#14884,.T.);
#20019=ORIENTED_EDGE('',*,*,#14658,.T.);
#20020=ORIENTED_EDGE('',*,*,#14893,.T.);
#20021=ORIENTED_EDGE('',*,*,#14889,.T.);
#20022=ORIENTED_EDGE('',*,*,#14654,.T.);
#20023=ORIENTED_EDGE('',*,*,#14898,.T.);
#20024=ORIENTED_EDGE('',*,*,#14894,.T.);
#20025=ORIENTED_EDGE('',*,*,#14650,.T.);
#20026=ORIENTED_EDGE('',*,*,#14577,.T.);
#20027=ORIENTED_EDGE('',*,*,#14571,.T.);
#20028=ORIENTED_EDGE('',*,*,#14649,.T.);
#20029=ORIENTED_EDGE('',*,*,#14728,.T.);
#20030=ORIENTED_EDGE('',*,*,#14724,.T.);
#20031=ORIENTED_EDGE('',*,*,#14645,.T.);
#20032=ORIENTED_EDGE('',*,*,#14733,.T.);
#20033=ORIENTED_EDGE('',*,*,#14729,.T.);
#20034=ORIENTED_EDGE('',*,*,#14641,.T.);
#20035=ORIENTED_EDGE('',*,*,#14738,.T.);
#20036=ORIENTED_EDGE('',*,*,#14734,.T.);
#20037=ORIENTED_EDGE('',*,*,#14637,.T.);
#20038=ORIENTED_EDGE('',*,*,#14743,.T.);
#20039=ORIENTED_EDGE('',*,*,#14739,.T.);
#20040=ORIENTED_EDGE('',*,*,#14633,.T.);
#20041=ORIENTED_EDGE('',*,*,#14748,.T.);
#20042=ORIENTED_EDGE('',*,*,#14744,.T.);
#20043=ORIENTED_EDGE('',*,*,#14629,.T.);
#20044=ORIENTED_EDGE('',*,*,#14753,.T.);
#20045=ORIENTED_EDGE('',*,*,#14749,.T.);
#20046=ORIENTED_EDGE('',*,*,#14625,.T.);
#20047=ORIENTED_EDGE('',*,*,#14758,.T.);
#20048=ORIENTED_EDGE('',*,*,#14754,.T.);
#20049=ORIENTED_EDGE('',*,*,#14621,.T.);
#20050=ORIENTED_EDGE('',*,*,#14763,.T.);
#20051=ORIENTED_EDGE('',*,*,#14759,.T.);
#20052=ORIENTED_EDGE('',*,*,#14617,.T.);
#20053=ORIENTED_EDGE('',*,*,#14768,.T.);
#20054=ORIENTED_EDGE('',*,*,#14764,.T.);
#20055=ORIENTED_EDGE('',*,*,#14613,.T.);
#20056=ORIENTED_EDGE('',*,*,#14773,.T.);
#20057=ORIENTED_EDGE('',*,*,#14769,.T.);
#20058=ORIENTED_EDGE('',*,*,#14609,.T.);
#20059=ORIENTED_EDGE('',*,*,#14778,.T.);
#20060=ORIENTED_EDGE('',*,*,#14774,.T.);
#20061=ORIENTED_EDGE('',*,*,#14605,.T.);
#20062=ORIENTED_EDGE('',*,*,#14783,.T.);
#20063=ORIENTED_EDGE('',*,*,#14779,.T.);
#20064=ORIENTED_EDGE('',*,*,#14601,.T.);
#20065=ORIENTED_EDGE('',*,*,#14788,.T.);
#20066=ORIENTED_EDGE('',*,*,#14784,.T.);
#20067=ORIENTED_EDGE('',*,*,#14597,.T.);
#20068=ORIENTED_EDGE('',*,*,#14793,.T.);
#20069=ORIENTED_EDGE('',*,*,#14789,.T.);
#20070=ORIENTED_EDGE('',*,*,#14593,.T.);
#20071=ORIENTED_EDGE('',*,*,#14798,.T.);
#20072=ORIENTED_EDGE('',*,*,#14794,.T.);
#20073=ORIENTED_EDGE('',*,*,#14589,.T.);
#20074=ORIENTED_EDGE('',*,*,#14803,.T.);
#20075=ORIENTED_EDGE('',*,*,#14799,.T.);
#20076=ORIENTED_EDGE('',*,*,#14585,.T.);
#20077=ORIENTED_EDGE('',*,*,#14808,.T.);
#20078=ORIENTED_EDGE('',*,*,#14900,.T.);
#20079=ORIENTED_EDGE('',*,*,#14901,.T.);
#20080=ORIENTED_EDGE('',*,*,#14900,.F.);
#20081=ORIENTED_EDGE('',*,*,#14901,.F.);
#20082=ORIENTED_EDGE('',*,*,#14902,.T.);
#20083=ORIENTED_EDGE('',*,*,#14903,.F.);
#20084=ORIENTED_EDGE('',*,*,#14904,.T.);
#20085=ORIENTED_EDGE('',*,*,#14905,.F.);
#20086=ORIENTED_EDGE('',*,*,#14906,.F.);
#20087=ORIENTED_EDGE('',*,*,#14907,.T.);
#20088=ORIENTED_EDGE('',*,*,#14908,.F.);
#20089=ORIENTED_EDGE('',*,*,#14909,.F.);
#20090=ORIENTED_EDGE('',*,*,#14910,.T.);
#20091=ORIENTED_EDGE('',*,*,#14911,.F.);
#20092=ORIENTED_EDGE('',*,*,#14912,.F.);
#20093=ORIENTED_EDGE('',*,*,#14913,.T.);
#20094=ORIENTED_EDGE('',*,*,#14914,.F.);
#20095=ORIENTED_EDGE('',*,*,#14915,.F.);
#20096=ORIENTED_EDGE('',*,*,#14916,.T.);
#20097=ORIENTED_EDGE('',*,*,#14917,.F.);
#20098=ORIENTED_EDGE('',*,*,#14918,.F.);
#20099=ORIENTED_EDGE('',*,*,#14919,.T.);
#20100=ORIENTED_EDGE('',*,*,#14920,.F.);
#20101=ORIENTED_EDGE('',*,*,#14921,.T.);
#20102=ORIENTED_EDGE('',*,*,#14902,.F.);
#20103=ORIENTED_EDGE('',*,*,#14921,.F.);
#20104=ORIENTED_EDGE('',*,*,#14922,.F.);
#20105=ORIENTED_EDGE('',*,*,#14907,.F.);
#20106=ORIENTED_EDGE('',*,*,#14923,.F.);
#20107=ORIENTED_EDGE('',*,*,#14924,.F.);
#20108=ORIENTED_EDGE('',*,*,#14925,.F.);
#20109=ORIENTED_EDGE('',*,*,#14910,.F.);
#20110=ORIENTED_EDGE('',*,*,#14926,.F.);
#20111=ORIENTED_EDGE('',*,*,#14927,.F.);
#20112=ORIENTED_EDGE('',*,*,#14928,.F.);
#20113=ORIENTED_EDGE('',*,*,#14929,.F.);
#20114=ORIENTED_EDGE('',*,*,#14930,.F.);
#20115=ORIENTED_EDGE('',*,*,#14904,.F.);
#20116=ORIENTED_EDGE('',*,*,#14931,.F.);
#20117=ORIENTED_EDGE('',*,*,#14913,.F.);
#20118=ORIENTED_EDGE('',*,*,#14932,.F.);
#20119=ORIENTED_EDGE('',*,*,#14933,.F.);
#20120=ORIENTED_EDGE('',*,*,#14934,.F.);
#20121=ORIENTED_EDGE('',*,*,#14935,.F.);
#20122=ORIENTED_EDGE('',*,*,#14936,.F.);
#20123=ORIENTED_EDGE('',*,*,#14919,.F.);
#20124=ORIENTED_EDGE('',*,*,#14937,.F.);
#20125=ORIENTED_EDGE('',*,*,#14938,.F.);
#20126=ORIENTED_EDGE('',*,*,#14939,.F.);
#20127=ORIENTED_EDGE('',*,*,#14916,.F.);
#20128=ORIENTED_EDGE('',*,*,#14914,.T.);
#20129=ORIENTED_EDGE('',*,*,#14931,.T.);
#20130=ORIENTED_EDGE('',*,*,#14940,.F.);
#20131=ORIENTED_EDGE('',*,*,#14932,.T.);
#20132=ORIENTED_EDGE('',*,*,#14912,.T.);
#20133=ORIENTED_EDGE('',*,*,#14941,.T.);
#20134=ORIENTED_EDGE('',*,*,#14942,.T.);
#20135=ORIENTED_EDGE('',*,*,#14943,.F.);
#20136=ORIENTED_EDGE('',*,*,#14911,.T.);
#20137=ORIENTED_EDGE('',*,*,#14925,.T.);
#20138=ORIENTED_EDGE('',*,*,#14944,.F.);
#20139=ORIENTED_EDGE('',*,*,#14926,.T.);
#20140=ORIENTED_EDGE('',*,*,#14909,.T.);
#20141=ORIENTED_EDGE('',*,*,#14945,.T.);
#20142=ORIENTED_EDGE('',*,*,#14946,.T.);
#20143=ORIENTED_EDGE('',*,*,#14941,.F.);
#20144=ORIENTED_EDGE('',*,*,#14908,.T.);
#20145=ORIENTED_EDGE('',*,*,#14922,.T.);
#20146=ORIENTED_EDGE('',*,*,#14947,.F.);
#20147=ORIENTED_EDGE('',*,*,#14923,.T.);
#20148=ORIENTED_EDGE('',*,*,#14906,.T.);
#20149=ORIENTED_EDGE('',*,*,#14948,.T.);
#20150=ORIENTED_EDGE('',*,*,#14949,.T.);
#20151=ORIENTED_EDGE('',*,*,#14945,.F.);
#20152=ORIENTED_EDGE('',*,*,#14924,.T.);
#20153=ORIENTED_EDGE('',*,*,#14947,.T.);
#20154=ORIENTED_EDGE('',*,*,#14927,.T.);
#20155=ORIENTED_EDGE('',*,*,#14944,.T.);
#20156=ORIENTED_EDGE('',*,*,#14929,.T.);
#20157=ORIENTED_EDGE('',*,*,#14950,.T.);
#20158=ORIENTED_EDGE('',*,*,#14933,.T.);
#20159=ORIENTED_EDGE('',*,*,#14940,.T.);
#20160=ORIENTED_EDGE('',*,*,#14935,.T.);
#20161=ORIENTED_EDGE('',*,*,#14951,.T.);
#20162=ORIENTED_EDGE('',*,*,#14938,.T.);
#20163=ORIENTED_EDGE('',*,*,#14952,.T.);
#20164=ORIENTED_EDGE('',*,*,#14953,.F.);
#20165=ORIENTED_EDGE('',*,*,#14954,.T.);
#20166=ORIENTED_EDGE('',*,*,#14949,.F.);
#20167=ORIENTED_EDGE('',*,*,#14955,.T.);
#20168=ORIENTED_EDGE('',*,*,#14946,.F.);
#20169=ORIENTED_EDGE('',*,*,#14956,.T.);
#20170=ORIENTED_EDGE('',*,*,#14942,.F.);
#20171=ORIENTED_EDGE('',*,*,#14957,.T.);
#20172=ORIENTED_EDGE('',*,*,#14958,.F.);
#20173=ORIENTED_EDGE('',*,*,#14959,.T.);
#20174=ORIENTED_EDGE('',*,*,#14960,.F.);
#20175=ORIENTED_EDGE('',*,*,#14961,.T.);
#20176=ORIENTED_EDGE('',*,*,#14962,.T.);
#20177=ORIENTED_EDGE('',*,*,#14961,.F.);
#20178=ORIENTED_EDGE('',*,*,#14959,.F.);
#20179=ORIENTED_EDGE('',*,*,#14957,.F.);
#20180=ORIENTED_EDGE('',*,*,#14956,.F.);
#20181=ORIENTED_EDGE('',*,*,#14955,.F.);
#20182=ORIENTED_EDGE('',*,*,#14954,.F.);
#20183=ORIENTED_EDGE('',*,*,#14962,.F.);
#20184=ORIENTED_EDGE('',*,*,#14903,.T.);
#20185=ORIENTED_EDGE('',*,*,#14963,.T.);
#20186=ORIENTED_EDGE('',*,*,#14953,.T.);
#20187=ORIENTED_EDGE('',*,*,#14948,.F.);
#20188=ORIENTED_EDGE('',*,*,#14905,.T.);
#20189=ORIENTED_EDGE('',*,*,#14930,.T.);
#20190=ORIENTED_EDGE('',*,*,#14950,.F.);
#20191=ORIENTED_EDGE('',*,*,#14928,.T.);
#20192=ORIENTED_EDGE('',*,*,#14918,.T.);
#20193=ORIENTED_EDGE('',*,*,#14964,.T.);
#20194=ORIENTED_EDGE('',*,*,#14960,.T.);
#20195=ORIENTED_EDGE('',*,*,#14963,.F.);
#20196=ORIENTED_EDGE('',*,*,#14920,.T.);
#20197=ORIENTED_EDGE('',*,*,#14936,.T.);
#20198=ORIENTED_EDGE('',*,*,#14951,.F.);
#20199=ORIENTED_EDGE('',*,*,#14934,.T.);
#20200=ORIENTED_EDGE('',*,*,#14915,.T.);
#20201=ORIENTED_EDGE('',*,*,#14943,.T.);
#20202=ORIENTED_EDGE('',*,*,#14958,.T.);
#20203=ORIENTED_EDGE('',*,*,#14964,.F.);
#20204=ORIENTED_EDGE('',*,*,#14917,.T.);
#20205=ORIENTED_EDGE('',*,*,#14939,.T.);
#20206=ORIENTED_EDGE('',*,*,#14952,.F.);
#20207=ORIENTED_EDGE('',*,*,#14937,.T.);
#25485=CONICAL_SURFACE('',#27635,1.2885,0.785398163397446);
#25486=CONICAL_SURFACE('',#27824,2.6,0.785398163397444);
#25487=CONICAL_SURFACE('',#27828,1.49337567297406,0.785398163397459);
#25488=CONICAL_SURFACE('',#27868,1.44337567297406,1.02974425867665);
#25864=ADVANCED_FACE('',(#2671),#2228,.T.);
#25865=ADVANCED_FACE('',(#2672),#2229,.T.);
#25866=ADVANCED_FACE('',(#2673),#2230,.T.);
#25867=ADVANCED_FACE('',(#2674),#2231,.T.);
#25868=ADVANCED_FACE('',(#2675),#2232,.T.);
#25869=ADVANCED_FACE('',(#2676),#2233,.T.);
#25870=ADVANCED_FACE('',(#2677),#2234,.T.);
#25871=ADVANCED_FACE('',(#2678),#2235,.T.);
#25872=ADVANCED_FACE('',(#2679),#2236,.T.);
#25873=ADVANCED_FACE('',(#2680),#2237,.T.);
#25874=ADVANCED_FACE('',(#2681),#2238,.T.);
#25875=ADVANCED_FACE('',(#2682),#2239,.T.);
#25876=ADVANCED_FACE('',(#2683),#2240,.T.);
#25877=ADVANCED_FACE('',(#2684),#2241,.T.);
#25878=ADVANCED_FACE('',(#2685),#2242,.T.);
#25879=ADVANCED_FACE('',(#2686),#2243,.T.);
#25880=ADVANCED_FACE('',(#2687),#2244,.T.);
#25881=ADVANCED_FACE('',(#2688),#2245,.T.);
#25882=ADVANCED_FACE('',(#2689),#2246,.T.);
#25883=ADVANCED_FACE('',(#2690),#2247,.T.);
#25884=ADVANCED_FACE('',(#2691),#2248,.T.);
#25885=ADVANCED_FACE('',(#2692),#2249,.T.);
#25886=ADVANCED_FACE('',(#2693),#2250,.T.);
#25887=ADVANCED_FACE('',(#2694),#2251,.T.);
#25888=ADVANCED_FACE('',(#2695),#1284,.T.);
#25889=ADVANCED_FACE('',(#2696),#897,.F.);
#25890=ADVANCED_FACE('',(#2697),#1285,.F.);
#25891=ADVANCED_FACE('',(#2698),#898,.F.);
#25892=ADVANCED_FACE('',(#2699),#503,.F.);
#25893=ADVANCED_FACE('',(#2700,#1017),#1286,.F.);
#25894=ADVANCED_FACE('',(#2701),#25485,.T.);
#25895=ADVANCED_FACE('',(#2702),#1287,.F.);
#25896=ADVANCED_FACE('',(#2703),#1288,.F.);
#25897=ADVANCED_FACE('',(#2704),#1289,.F.);
#25898=ADVANCED_FACE('',(#2705),#1290,.F.);
#25899=ADVANCED_FACE('',(#2706),#2252,.T.);
#25900=ADVANCED_FACE('',(#2707),#1291,.F.);
#25901=ADVANCED_FACE('',(#2708),#1292,.F.);
#25902=ADVANCED_FACE('',(#2709),#1293,.F.);
#25903=ADVANCED_FACE('',(#2710),#1294,.F.);
#25904=ADVANCED_FACE('',(#2711),#1295,.F.);
#25905=ADVANCED_FACE('',(#2712),#1296,.F.);
#25906=ADVANCED_FACE('',(#2713),#1297,.F.);
#25907=ADVANCED_FACE('',(#2714),#1298,.F.);
#25908=ADVANCED_FACE('',(#2715),#1299,.F.);
#25909=ADVANCED_FACE('',(#2716),#1300,.F.);
#25910=ADVANCED_FACE('',(#2717),#1301,.F.);
#25911=ADVANCED_FACE('',(#2718),#1302,.F.);
#25912=ADVANCED_FACE('',(#2719),#1303,.F.);
#25913=ADVANCED_FACE('',(#2720),#1304,.F.);
#25914=ADVANCED_FACE('',(#2721),#1305,.F.);
#25915=ADVANCED_FACE('',(#2722),#1306,.F.);
#25916=ADVANCED_FACE('',(#2723),#1307,.F.);
#25917=ADVANCED_FACE('',(#2724),#1308,.F.);
#25918=ADVANCED_FACE('',(#2725),#1309,.F.);
#25919=ADVANCED_FACE('',(#2726),#1310,.F.);
#25920=ADVANCED_FACE('',(#2727),#1311,.F.);
#25921=ADVANCED_FACE('',(#2728),#1312,.F.);
#25922=ADVANCED_FACE('',(#2729),#1313,.F.);
#25923=ADVANCED_FACE('',(#2730),#1314,.F.);
#25924=ADVANCED_FACE('',(#2731),#1315,.F.);
#25925=ADVANCED_FACE('',(#2732),#1316,.F.);
#25926=ADVANCED_FACE('',(#2733),#1317,.F.);
#25927=ADVANCED_FACE('',(#2734),#1318,.F.);
#25928=ADVANCED_FACE('',(#2735),#1319,.F.);
#25929=ADVANCED_FACE('',(#2736),#1320,.F.);
#25930=ADVANCED_FACE('',(#2737),#1321,.F.);
#25931=ADVANCED_FACE('',(#2738),#1322,.F.);
#25932=ADVANCED_FACE('',(#2739),#1323,.F.);
#25933=ADVANCED_FACE('',(#2740),#1324,.F.);
#25934=ADVANCED_FACE('',(#2741),#1325,.F.);
#25935=ADVANCED_FACE('',(#2742),#1326,.F.);
#25936=ADVANCED_FACE('',(#2743),#1327,.F.);
#25937=ADVANCED_FACE('',(#2744),#1328,.F.);
#25938=ADVANCED_FACE('',(#2745),#1329,.F.);
#25939=ADVANCED_FACE('',(#2746),#1330,.F.);
#25940=ADVANCED_FACE('',(#2747),#1331,.F.);
#25941=ADVANCED_FACE('',(#2748),#1332,.F.);
#25942=ADVANCED_FACE('',(#2749),#1333,.F.);
#25943=ADVANCED_FACE('',(#2750),#1334,.F.);
#25944=ADVANCED_FACE('',(#2751),#1335,.F.);
#25945=ADVANCED_FACE('',(#2752),#1336,.F.);
#25946=ADVANCED_FACE('',(#2753),#1337,.F.);
#25947=ADVANCED_FACE('',(#2754),#1338,.F.);
#25948=ADVANCED_FACE('',(#2755),#1339,.F.);
#25949=ADVANCED_FACE('',(#2756),#1340,.F.);
#25950=ADVANCED_FACE('',(#2757),#1341,.F.);
#25951=ADVANCED_FACE('',(#2758),#1342,.F.);
#25952=ADVANCED_FACE('',(#2759),#1343,.F.);
#25953=ADVANCED_FACE('',(#2760),#1344,.F.);
#25954=ADVANCED_FACE('',(#2761),#1345,.F.);
#25955=ADVANCED_FACE('',(#2762),#1346,.F.);
#25956=ADVANCED_FACE('',(#2763),#1347,.F.);
#25957=ADVANCED_FACE('',(#2764),#1348,.F.);
#25958=ADVANCED_FACE('',(#2765),#1349,.F.);
#25959=ADVANCED_FACE('',(#2766),#1350,.F.);
#25960=ADVANCED_FACE('',(#2767),#1351,.F.);
#25961=ADVANCED_FACE('',(#2768),#1352,.F.);
#25962=ADVANCED_FACE('',(#2769),#1353,.F.);
#25963=ADVANCED_FACE('',(#2770),#1354,.F.);
#25964=ADVANCED_FACE('',(#2771),#1355,.F.);
#25965=ADVANCED_FACE('',(#2772),#1356,.F.);
#25966=ADVANCED_FACE('',(#2773),#1357,.F.);
#25967=ADVANCED_FACE('',(#2774),#1358,.F.);
#25968=ADVANCED_FACE('',(#2775),#1359,.F.);
#25969=ADVANCED_FACE('',(#2776),#1360,.F.);
#25970=ADVANCED_FACE('',(#2777),#1361,.F.);
#25971=ADVANCED_FACE('',(#2778),#1362,.F.);
#25972=ADVANCED_FACE('',(#2779),#1363,.F.);
#25973=ADVANCED_FACE('',(#2780),#1364,.F.);
#25974=ADVANCED_FACE('',(#2781),#1365,.F.);
#25975=ADVANCED_FACE('',(#2782),#1366,.F.);
#25976=ADVANCED_FACE('',(#2783),#1367,.F.);
#25977=ADVANCED_FACE('',(#2784),#1368,.F.);
#25978=ADVANCED_FACE('',(#2785),#1369,.F.);
#25979=ADVANCED_FACE('',(#2786),#1370,.F.);
#25980=ADVANCED_FACE('',(#2787),#1371,.F.);
#25981=ADVANCED_FACE('',(#2788),#1372,.F.);
#25982=ADVANCED_FACE('',(#2789),#1373,.F.);
#25983=ADVANCED_FACE('',(#2790),#1374,.F.);
#25984=ADVANCED_FACE('',(#2791),#1375,.F.);
#25985=ADVANCED_FACE('',(#2792),#1376,.F.);
#25986=ADVANCED_FACE('',(#2793),#1377,.F.);
#25987=ADVANCED_FACE('',(#2794),#1378,.F.);
#25988=ADVANCED_FACE('',(#2795),#1379,.F.);
#25989=ADVANCED_FACE('',(#2796),#1380,.F.);
#25990=ADVANCED_FACE('',(#2797),#1381,.F.);
#25991=ADVANCED_FACE('',(#2798),#1382,.F.);
#25992=ADVANCED_FACE('',(#2799),#1383,.F.);
#25993=ADVANCED_FACE('',(#2800),#1384,.F.);
#25994=ADVANCED_FACE('',(#2801),#1385,.F.);
#25995=ADVANCED_FACE('',(#2802),#1386,.F.);
#25996=ADVANCED_FACE('',(#2803),#1387,.F.);
#25997=ADVANCED_FACE('',(#2804),#1388,.F.);
#25998=ADVANCED_FACE('',(#2805),#1389,.F.);
#25999=ADVANCED_FACE('',(#2806),#1390,.F.);
#26000=ADVANCED_FACE('',(#2807),#1391,.F.);
#26001=ADVANCED_FACE('',(#2808),#1392,.F.);
#26002=ADVANCED_FACE('',(#2809),#1393,.F.);
#26003=ADVANCED_FACE('',(#2810),#1394,.F.);
#26004=ADVANCED_FACE('',(#2811),#1395,.F.);
#26005=ADVANCED_FACE('',(#2812),#504,.T.);
#26006=ADVANCED_FACE('',(#2813),#25486,.T.);
#26007=ADVANCED_FACE('',(#2814,#1018),#1396,.T.);
#26008=ADVANCED_FACE('',(#2815),#25487,.F.);
#26009=ADVANCED_FACE('',(#2816),#2253,.T.);
#26010=ADVANCED_FACE('',(#2817),#2254,.T.);
#26011=ADVANCED_FACE('',(#2818),#2255,.T.);
#26012=ADVANCED_FACE('',(#2819),#2256,.T.);
#26013=ADVANCED_FACE('',(#2820),#2257,.T.);
#26014=ADVANCED_FACE('',(#2821),#2258,.T.);
#26015=ADVANCED_FACE('',(#2822),#1397,.F.);
#26016=ADVANCED_FACE('',(#2823),#1398,.F.);
#26017=ADVANCED_FACE('',(#2824),#1399,.F.);
#26018=ADVANCED_FACE('',(#2825),#1400,.T.);
#26019=ADVANCED_FACE('',(#2826),#1401,.T.);
#26020=ADVANCED_FACE('',(#2827),#1402,.T.);
#26021=ADVANCED_FACE('',(#2828),#1403,.T.);
#26022=ADVANCED_FACE('',(#2829),#1404,.T.);
#26023=ADVANCED_FACE('',(#2830),#1405,.T.);
#26024=ADVANCED_FACE('',(#2831),#1406,.F.);
#26025=ADVANCED_FACE('',(#2832),#1407,.F.);
#26026=ADVANCED_FACE('',(#2833),#1408,.F.);
#26027=ADVANCED_FACE('',(#2834),#1409,.F.);
#26028=ADVANCED_FACE('',(#2835),#1410,.F.);
#26029=ADVANCED_FACE('',(#2836),#1411,.F.);
#26030=ADVANCED_FACE('',(#2837),#25488,.F.);
#26031=ADVANCED_FACE('',(#2838),#1412,.F.);
#26032=ADVANCED_FACE('',(#2839),#1413,.F.);
#26033=ADVANCED_FACE('',(#2840),#1414,.F.);
#26933=CLOSED_SHELL('',(#25864,#25865,#25866,#25867,#25868,#25869,#25870,
#25871,#25872,#25873,#25874,#25875,#25876,#25877,#25878,#25879,#25880,#25881,
#25882,#25883,#25884,#25885,#25886,#25887,#25888,#25889,#25890,#25891,#25892,
#25893,#25894,#25895,#25896,#25897,#25898,#25899,#25900,#25901,#25902,#25903,
#25904,#25905,#25906,#25907,#25908,#25909,#25910,#25911,#25912,#25913,#25914,
#25915,#25916,#25917,#25918,#25919,#25920,#25921,#25922,#25923,#25924,#25925,
#25926,#25927,#25928,#25929,#25930,#25931,#25932,#25933,#25934,#25935,#25936,
#25937,#25938,#25939,#25940,#25941,#25942,#25943,#25944,#25945,#25946,#25947,
#25948,#25949,#25950,#25951,#25952,#25953,#25954,#25955,#25956,#25957,#25958,
#25959,#25960,#25961,#25962,#25963,#25964,#25965,#25966,#25967,#25968,#25969,
#25970,#25971,#25972,#25973,#25974,#25975,#25976,#25977,#25978,#25979,#25980,
#25981,#25982,#25983,#25984,#25985,#25986,#25987,#25988,#25989,#25990,#25991,
#25992,#25993,#25994,#25995,#25996,#25997,#25998,#25999,#26000,#26001,#26002,
#26003,#26004,#26005,#26006,#26007,#26008,#26009,#26010,#26011,#26012,#26013,
#26014,#26015,#26016,#26017,#26018,#26019,#26020,#26021,#26022,#26023,#26024,
#26025,#26026,#26027,#26028,#26029,#26030,#26031,#26032,#26033));
#27595=AXIS2_PLACEMENT_3D('',#42113,#30788,#30789);
#27596=AXIS2_PLACEMENT_3D('',#42114,#30790,#30791);
#27597=AXIS2_PLACEMENT_3D('',#42217,#30793,#30794);
#27598=AXIS2_PLACEMENT_3D('',#42279,#30795,#30796);
#27599=AXIS2_PLACEMENT_3D('',#42523,#30798,#30799);
#27600=AXIS2_PLACEMENT_3D('',#42836,#30801,#30802);
#27601=AXIS2_PLACEMENT_3D('',#43219,#30804,#30805);
#27602=AXIS2_PLACEMENT_3D('',#43575,#30807,#30808);
#27603=AXIS2_PLACEMENT_3D('',#43951,#30810,#30811);
#27604=AXIS2_PLACEMENT_3D('',#44323,#30813,#30814);
#27605=AXIS2_PLACEMENT_3D('',#44571,#30816,#30817);
#27606=AXIS2_PLACEMENT_3D('',#44900,#30819,#30820);
#27607=AXIS2_PLACEMENT_3D('',#45261,#30822,#30823);
#27608=AXIS2_PLACEMENT_3D('',#45504,#30825,#30826);
#27609=AXIS2_PLACEMENT_3D('',#45568,#30828,#30829);
#27610=AXIS2_PLACEMENT_3D('',#45574,#30830,#30831);
#27611=AXIS2_PLACEMENT_3D('',#45922,#30833,#30834);
#27612=AXIS2_PLACEMENT_3D('',#46108,#30836,#30837);
#27613=AXIS2_PLACEMENT_3D('',#46456,#30839,#30840);
#27614=AXIS2_PLACEMENT_3D('',#46804,#30842,#30843);
#27615=AXIS2_PLACEMENT_3D('',#46990,#30845,#30846);
#27616=AXIS2_PLACEMENT_3D('',#47176,#30848,#30849);
#27617=AXIS2_PLACEMENT_3D('',#47524,#30851,#30852);
#27618=AXIS2_PLACEMENT_3D('',#47710,#30854,#30855);
#27619=AXIS2_PLACEMENT_3D('',#48058,#30857,#30858);
#27620=AXIS2_PLACEMENT_3D('',#48406,#30860,#30861);
#27621=AXIS2_PLACEMENT_3D('',#48569,#30862,#30863);
#27622=AXIS2_PLACEMENT_3D('',#48578,#30864,#30865);
#27623=AXIS2_PLACEMENT_3D('',#48664,#30866,#30867);
#27624=AXIS2_PLACEMENT_3D('',#48755,#30868,#30869);
#27625=AXIS2_PLACEMENT_3D('',#48758,#30870,#30871);
#27626=AXIS2_PLACEMENT_3D('',#48923,#30872,#30873);
#27627=AXIS2_PLACEMENT_3D('',#49310,#30874,#30875);
#27628=AXIS2_PLACEMENT_3D('',#49313,#30876,#30877);
#27629=AXIS2_PLACEMENT_3D('',#49396,#30878,#30879);
#27630=AXIS2_PLACEMENT_3D('',#49701,#30880,#30881);
#27631=AXIS2_PLACEMENT_3D('',#49703,#30882,#30883);
#27632=AXIS2_PLACEMENT_3D('',#49704,#30884,#30885);
#27633=AXIS2_PLACEMENT_3D('',#49705,#30886,#30887);
#27634=AXIS2_PLACEMENT_3D('',#49707,#30888,#30889);
#27635=AXIS2_PLACEMENT_3D('',#49708,#30890,#30891);
#27636=AXIS2_PLACEMENT_3D('',#49711,#30893,#30894);
#27637=AXIS2_PLACEMENT_3D('',#49712,#30895,#30896);
#27638=AXIS2_PLACEMENT_3D('',#49713,#30897,#30898);
#27639=AXIS2_PLACEMENT_3D('',#49724,#30902,#30903);
#27640=AXIS2_PLACEMENT_3D('',#49726,#30904,#30905);
#27641=AXIS2_PLACEMENT_3D('',#49728,#30907,#30908);
#27642=AXIS2_PLACEMENT_3D('',#49734,#30910,#30911);
#27643=AXIS2_PLACEMENT_3D('',#49737,#30912,#30913);
#27644=AXIS2_PLACEMENT_3D('',#49741,#30915,#30916);
#27645=AXIS2_PLACEMENT_3D('',#49742,#30917,#30918);
#27646=AXIS2_PLACEMENT_3D('',#49744,#30919,#30920);
#27647=AXIS2_PLACEMENT_3D('',#49748,#30922,#30923);
#27648=AXIS2_PLACEMENT_3D('',#49752,#30925,#30926);
#27649=AXIS2_PLACEMENT_3D('',#49756,#30928,#30929);
#27650=AXIS2_PLACEMENT_3D('',#49760,#30931,#30932);
#27651=AXIS2_PLACEMENT_3D('',#49764,#30934,#30935);
#27652=AXIS2_PLACEMENT_3D('',#49768,#30937,#30938);
#27653=AXIS2_PLACEMENT_3D('',#49772,#30940,#30941);
#27654=AXIS2_PLACEMENT_3D('',#49776,#30943,#30944);
#27655=AXIS2_PLACEMENT_3D('',#49780,#30946,#30947);
#27656=AXIS2_PLACEMENT_3D('',#49784,#30949,#30950);
#27657=AXIS2_PLACEMENT_3D('',#49788,#30952,#30953);
#27658=AXIS2_PLACEMENT_3D('',#49792,#30955,#30956);
#27659=AXIS2_PLACEMENT_3D('',#49796,#30958,#30959);
#27660=AXIS2_PLACEMENT_3D('',#49800,#30961,#30962);
#27661=AXIS2_PLACEMENT_3D('',#49804,#30964,#30965);
#27662=AXIS2_PLACEMENT_3D('',#49808,#30967,#30968);
#27663=AXIS2_PLACEMENT_3D('',#49812,#30970,#30971);
#27664=AXIS2_PLACEMENT_3D('',#49816,#30973,#30974);
#27665=AXIS2_PLACEMENT_3D('',#49820,#30976,#30977);
#27666=AXIS2_PLACEMENT_3D('',#49824,#30979,#30980);
#27667=AXIS2_PLACEMENT_3D('',#49828,#30982,#30983);
#27668=AXIS2_PLACEMENT_3D('',#49832,#30985,#30986);
#27669=AXIS2_PLACEMENT_3D('',#49836,#30988,#30989);
#27670=AXIS2_PLACEMENT_3D('',#49840,#30991,#30992);
#27671=AXIS2_PLACEMENT_3D('',#49844,#30994,#30995);
#27672=AXIS2_PLACEMENT_3D('',#49848,#30997,#30998);
#27673=AXIS2_PLACEMENT_3D('',#49852,#31000,#31001);
#27674=AXIS2_PLACEMENT_3D('',#49856,#31003,#31004);
#27675=AXIS2_PLACEMENT_3D('',#49860,#31006,#31007);
#27676=AXIS2_PLACEMENT_3D('',#49864,#31009,#31010);
#27677=AXIS2_PLACEMENT_3D('',#49868,#31012,#31013);
#27678=AXIS2_PLACEMENT_3D('',#49872,#31015,#31016);
#27679=AXIS2_PLACEMENT_3D('',#49875,#31018,#31019);
#27680=AXIS2_PLACEMENT_3D('',#49877,#31020,#31021);
#27681=AXIS2_PLACEMENT_3D('',#49881,#31023,#31024);
#27682=AXIS2_PLACEMENT_3D('',#49885,#31026,#31027);
#27683=AXIS2_PLACEMENT_3D('',#49889,#31029,#31030);
#27684=AXIS2_PLACEMENT_3D('',#49893,#31032,#31033);
#27685=AXIS2_PLACEMENT_3D('',#49897,#31035,#31036);
#27686=AXIS2_PLACEMENT_3D('',#49901,#31038,#31039);
#27687=AXIS2_PLACEMENT_3D('',#49905,#31041,#31042);
#27688=AXIS2_PLACEMENT_3D('',#49909,#31044,#31045);
#27689=AXIS2_PLACEMENT_3D('',#49913,#31047,#31048);
#27690=AXIS2_PLACEMENT_3D('',#49917,#31050,#31051);
#27691=AXIS2_PLACEMENT_3D('',#49921,#31053,#31054);
#27692=AXIS2_PLACEMENT_3D('',#49925,#31056,#31057);
#27693=AXIS2_PLACEMENT_3D('',#49929,#31059,#31060);
#27694=AXIS2_PLACEMENT_3D('',#49933,#31062,#31063);
#27695=AXIS2_PLACEMENT_3D('',#49937,#31065,#31066);
#27696=AXIS2_PLACEMENT_3D('',#49941,#31068,#31069);
#27697=AXIS2_PLACEMENT_3D('',#49945,#31071,#31072);
#27698=AXIS2_PLACEMENT_3D('',#49949,#31074,#31075);
#27699=AXIS2_PLACEMENT_3D('',#49953,#31077,#31078);
#27700=AXIS2_PLACEMENT_3D('',#49957,#31080,#31081);
#27701=AXIS2_PLACEMENT_3D('',#49961,#31083,#31084);
#27702=AXIS2_PLACEMENT_3D('',#49965,#31086,#31087);
#27703=AXIS2_PLACEMENT_3D('',#49969,#31089,#31090);
#27704=AXIS2_PLACEMENT_3D('',#49973,#31092,#31093);
#27705=AXIS2_PLACEMENT_3D('',#49977,#31095,#31096);
#27706=AXIS2_PLACEMENT_3D('',#49981,#31098,#31099);
#27707=AXIS2_PLACEMENT_3D('',#49985,#31101,#31102);
#27708=AXIS2_PLACEMENT_3D('',#49989,#31104,#31105);
#27709=AXIS2_PLACEMENT_3D('',#49993,#31107,#31108);
#27710=AXIS2_PLACEMENT_3D('',#49997,#31110,#31111);
#27711=AXIS2_PLACEMENT_3D('',#50001,#31113,#31114);
#27712=AXIS2_PLACEMENT_3D('',#50005,#31116,#31117);
#27713=AXIS2_PLACEMENT_3D('',#50009,#31119,#31120);
#27714=AXIS2_PLACEMENT_3D('',#50013,#31122,#31123);
#27715=AXIS2_PLACEMENT_3D('',#50017,#31125,#31126);
#27716=AXIS2_PLACEMENT_3D('',#50021,#31128,#31129);
#27717=AXIS2_PLACEMENT_3D('',#50023,#31131,#31132);
#27718=AXIS2_PLACEMENT_3D('',#50031,#31135,#31136);
#27719=AXIS2_PLACEMENT_3D('',#50033,#31138,#31139);
#27720=AXIS2_PLACEMENT_3D('',#50037,#31140,#31141);
#27721=AXIS2_PLACEMENT_3D('',#50045,#31144,#31145);
#27722=AXIS2_PLACEMENT_3D('',#50047,#31147,#31148);
#27723=AXIS2_PLACEMENT_3D('',#50051,#31149,#31150);
#27724=AXIS2_PLACEMENT_3D('',#50059,#31153,#31154);
#27725=AXIS2_PLACEMENT_3D('',#50061,#31156,#31157);
#27726=AXIS2_PLACEMENT_3D('',#50065,#31158,#31159);
#27727=AXIS2_PLACEMENT_3D('',#50073,#31162,#31163);
#27728=AXIS2_PLACEMENT_3D('',#50075,#31165,#31166);
#27729=AXIS2_PLACEMENT_3D('',#50079,#31167,#31168);
#27730=AXIS2_PLACEMENT_3D('',#50087,#31171,#31172);
#27731=AXIS2_PLACEMENT_3D('',#50089,#31174,#31175);
#27732=AXIS2_PLACEMENT_3D('',#50093,#31176,#31177);
#27733=AXIS2_PLACEMENT_3D('',#50101,#31180,#31181);
#27734=AXIS2_PLACEMENT_3D('',#50103,#31183,#31184);
#27735=AXIS2_PLACEMENT_3D('',#50107,#31185,#31186);
#27736=AXIS2_PLACEMENT_3D('',#50115,#31189,#31190);
#27737=AXIS2_PLACEMENT_3D('',#50117,#31192,#31193);
#27738=AXIS2_PLACEMENT_3D('',#50121,#31194,#31195);
#27739=AXIS2_PLACEMENT_3D('',#50129,#31198,#31199);
#27740=AXIS2_PLACEMENT_3D('',#50131,#31201,#31202);
#27741=AXIS2_PLACEMENT_3D('',#50135,#31203,#31204);
#27742=AXIS2_PLACEMENT_3D('',#50143,#31207,#31208);
#27743=AXIS2_PLACEMENT_3D('',#50145,#31210,#31211);
#27744=AXIS2_PLACEMENT_3D('',#50149,#31212,#31213);
#27745=AXIS2_PLACEMENT_3D('',#50157,#31216,#31217);
#27746=AXIS2_PLACEMENT_3D('',#50159,#31219,#31220);
#27747=AXIS2_PLACEMENT_3D('',#50163,#31221,#31222);
#27748=AXIS2_PLACEMENT_3D('',#50171,#31225,#31226);
#27749=AXIS2_PLACEMENT_3D('',#50173,#31228,#31229);
#27750=AXIS2_PLACEMENT_3D('',#50177,#31230,#31231);
#27751=AXIS2_PLACEMENT_3D('',#50185,#31234,#31235);
#27752=AXIS2_PLACEMENT_3D('',#50187,#31237,#31238);
#27753=AXIS2_PLACEMENT_3D('',#50191,#31239,#31240);
#27754=AXIS2_PLACEMENT_3D('',#50199,#31243,#31244);
#27755=AXIS2_PLACEMENT_3D('',#50201,#31246,#31247);
#27756=AXIS2_PLACEMENT_3D('',#50205,#31248,#31249);
#27757=AXIS2_PLACEMENT_3D('',#50213,#31252,#31253);
#27758=AXIS2_PLACEMENT_3D('',#50215,#31255,#31256);
#27759=AXIS2_PLACEMENT_3D('',#50219,#31257,#31258);
#27760=AXIS2_PLACEMENT_3D('',#50227,#31261,#31262);
#27761=AXIS2_PLACEMENT_3D('',#50229,#31264,#31265);
#27762=AXIS2_PLACEMENT_3D('',#50233,#31266,#31267);
#27763=AXIS2_PLACEMENT_3D('',#50241,#31270,#31271);
#27764=AXIS2_PLACEMENT_3D('',#50243,#31273,#31274);
#27765=AXIS2_PLACEMENT_3D('',#50247,#31275,#31276);
#27766=AXIS2_PLACEMENT_3D('',#50255,#31279,#31280);
#27767=AXIS2_PLACEMENT_3D('',#50257,#31282,#31283);
#27768=AXIS2_PLACEMENT_3D('',#50261,#31284,#31285);
#27769=AXIS2_PLACEMENT_3D('',#50269,#31288,#31289);
#27770=AXIS2_PLACEMENT_3D('',#50271,#31291,#31292);
#27771=AXIS2_PLACEMENT_3D('',#50275,#31293,#31294);
#27772=AXIS2_PLACEMENT_3D('',#50283,#31297,#31298);
#27773=AXIS2_PLACEMENT_3D('',#50285,#31300,#31301);
#27774=AXIS2_PLACEMENT_3D('',#50289,#31302,#31303);
#27775=AXIS2_PLACEMENT_3D('',#50297,#31306,#31307);
#27776=AXIS2_PLACEMENT_3D('',#50299,#31309,#31310);
#27777=AXIS2_PLACEMENT_3D('',#50303,#31311,#31312);
#27778=AXIS2_PLACEMENT_3D('',#50311,#31315,#31316);
#27779=AXIS2_PLACEMENT_3D('',#50313,#31318,#31319);
#27780=AXIS2_PLACEMENT_3D('',#50317,#31320,#31321);
#27781=AXIS2_PLACEMENT_3D('',#50325,#31324,#31325);
#27782=AXIS2_PLACEMENT_3D('',#50327,#31327,#31328);
#27783=AXIS2_PLACEMENT_3D('',#50331,#31329,#31330);
#27784=AXIS2_PLACEMENT_3D('',#50339,#31333,#31334);
#27785=AXIS2_PLACEMENT_3D('',#50341,#31336,#31337);
#27786=AXIS2_PLACEMENT_3D('',#50345,#31338,#31339);
#27787=AXIS2_PLACEMENT_3D('',#50353,#31342,#31343);
#27788=AXIS2_PLACEMENT_3D('',#50355,#31345,#31346);
#27789=AXIS2_PLACEMENT_3D('',#50359,#31347,#31348);
#27790=AXIS2_PLACEMENT_3D('',#50367,#31351,#31352);
#27791=AXIS2_PLACEMENT_3D('',#50369,#31354,#31355);
#27792=AXIS2_PLACEMENT_3D('',#50373,#31356,#31357);
#27793=AXIS2_PLACEMENT_3D('',#50381,#31360,#31361);
#27794=AXIS2_PLACEMENT_3D('',#50383,#31363,#31364);
#27795=AXIS2_PLACEMENT_3D('',#50387,#31365,#31366);
#27796=AXIS2_PLACEMENT_3D('',#50395,#31369,#31370);
#27797=AXIS2_PLACEMENT_3D('',#50397,#31372,#31373);
#27798=AXIS2_PLACEMENT_3D('',#50401,#31374,#31375);
#27799=AXIS2_PLACEMENT_3D('',#50409,#31378,#31379);
#27800=AXIS2_PLACEMENT_3D('',#50411,#31381,#31382);
#27801=AXIS2_PLACEMENT_3D('',#50415,#31383,#31384);
#27802=AXIS2_PLACEMENT_3D('',#50423,#31387,#31388);
#27803=AXIS2_PLACEMENT_3D('',#50425,#31390,#31391);
#27804=AXIS2_PLACEMENT_3D('',#50429,#31392,#31393);
#27805=AXIS2_PLACEMENT_3D('',#50437,#31396,#31397);
#27806=AXIS2_PLACEMENT_3D('',#50439,#31399,#31400);
#27807=AXIS2_PLACEMENT_3D('',#50443,#31401,#31402);
#27808=AXIS2_PLACEMENT_3D('',#50451,#31405,#31406);
#27809=AXIS2_PLACEMENT_3D('',#50453,#31408,#31409);
#27810=AXIS2_PLACEMENT_3D('',#50457,#31410,#31411);
#27811=AXIS2_PLACEMENT_3D('',#50465,#31414,#31415);
#27812=AXIS2_PLACEMENT_3D('',#50467,#31417,#31418);
#27813=AXIS2_PLACEMENT_3D('',#50471,#31419,#31420);
#27814=AXIS2_PLACEMENT_3D('',#50479,#31423,#31424);
#27815=AXIS2_PLACEMENT_3D('',#50481,#31426,#31427);
#27816=AXIS2_PLACEMENT_3D('',#50485,#31428,#31429);
#27817=AXIS2_PLACEMENT_3D('',#50493,#31432,#31433);
#27818=AXIS2_PLACEMENT_3D('',#50495,#31435,#31436);
#27819=AXIS2_PLACEMENT_3D('',#50499,#31437,#31438);
#27820=AXIS2_PLACEMENT_3D('',#50507,#31441,#31442);
#27821=AXIS2_PLACEMENT_3D('',#50509,#31444,#31445);
#27822=AXIS2_PLACEMENT_3D('',#50513,#31446,#31447);
#27823=AXIS2_PLACEMENT_3D('',#50514,#31448,#31449);
#27824=AXIS2_PLACEMENT_3D('',#50515,#31450,#31451);
#27825=AXIS2_PLACEMENT_3D('',#50518,#31453,#31454);
#27826=AXIS2_PLACEMENT_3D('',#50519,#31455,#31456);
#27827=AXIS2_PLACEMENT_3D('',#50521,#31457,#31458);
#27828=AXIS2_PLACEMENT_3D('',#50522,#31459,#31460);
#27829=AXIS2_PLACEMENT_3D('',#50529,#31461,#31462);
#27830=AXIS2_PLACEMENT_3D('',#50539,#31463,#31464);
#27831=AXIS2_PLACEMENT_3D('',#50549,#31465,#31466);
#27832=AXIS2_PLACEMENT_3D('',#50559,#31467,#31468);
#27833=AXIS2_PLACEMENT_3D('',#50569,#31469,#31470);
#27834=AXIS2_PLACEMENT_3D('',#50579,#31471,#31472);
#27835=AXIS2_PLACEMENT_3D('',#50584,#31474,#31475);
#27836=AXIS2_PLACEMENT_3D('',#50589,#31478,#31479);
#27837=AXIS2_PLACEMENT_3D('',#50590,#31480,#31481);
#27838=AXIS2_PLACEMENT_3D('',#50595,#31484,#31485);
#27839=AXIS2_PLACEMENT_3D('',#50596,#31486,#31487);
#27840=AXIS2_PLACEMENT_3D('',#50600,#31489,#31490);
#27841=AXIS2_PLACEMENT_3D('',#50602,#31492,#31493);
#27842=AXIS2_PLACEMENT_3D('',#50607,#31496,#31497);
#27843=AXIS2_PLACEMENT_3D('',#50608,#31498,#31499);
#27844=AXIS2_PLACEMENT_3D('',#50612,#31501,#31502);
#27845=AXIS2_PLACEMENT_3D('',#50614,#31504,#31505);
#27846=AXIS2_PLACEMENT_3D('',#50618,#31507,#31508);
#27847=AXIS2_PLACEMENT_3D('',#50620,#31510,#31511);
#27848=AXIS2_PLACEMENT_3D('',#50627,#31516,#31517);
#27849=AXIS2_PLACEMENT_3D('',#50632,#31521,#31522);
#27850=AXIS2_PLACEMENT_3D('',#50637,#31526,#31527);
#27851=AXIS2_PLACEMENT_3D('',#50638,#31528,#31529);
#27852=AXIS2_PLACEMENT_3D('',#50639,#31530,#31531);
#27853=AXIS2_PLACEMENT_3D('',#50641,#31533,#31534);
#27854=AXIS2_PLACEMENT_3D('',#50642,#31535,#31536);
#27855=AXIS2_PLACEMENT_3D('',#50644,#31538,#31539);
#27856=AXIS2_PLACEMENT_3D('',#50646,#31541,#31542);
#27857=AXIS2_PLACEMENT_3D('',#50649,#31544,#31545);
#27858=AXIS2_PLACEMENT_3D('',#50650,#31546,#31547);
#27859=AXIS2_PLACEMENT_3D('',#50651,#31548,#31549);
#27860=AXIS2_PLACEMENT_3D('',#50652,#31550,#31551);
#27861=AXIS2_PLACEMENT_3D('',#50653,#31552,#31553);
#27862=AXIS2_PLACEMENT_3D('',#50654,#31554,#31555);
#27863=AXIS2_PLACEMENT_3D('',#50655,#31556,#31557);
#27864=AXIS2_PLACEMENT_3D('',#50656,#31558,#31559);
#27865=AXIS2_PLACEMENT_3D('',#50659,#31561,#31562);
#27866=AXIS2_PLACEMENT_3D('',#50660,#31563,#31564);
#27867=AXIS2_PLACEMENT_3D('',#50662,#31566,#31567);
#27868=AXIS2_PLACEMENT_3D('',#50663,#31568,#31569);
#27869=AXIS2_PLACEMENT_3D('',#50666,#31571,#31572);
#27870=AXIS2_PLACEMENT_3D('',#50668,#31574,#31575);
#27871=AXIS2_PLACEMENT_3D('',#50670,#31577,#31578);
#30788=DIRECTION('axis',(0.,0.,1.));
#30789=DIRECTION('refdir',(1.,0.,0.));
#30790=DIRECTION('center_axis',(0.,-1.,0.));
#30791=DIRECTION('ref_axis',(-0.160423232777043,0.,-0.987048320187701));
#30792=DIRECTION('',(0.,1.,0.));
#30793=DIRECTION('center_axis',(0.,1.,0.));
#30794=DIRECTION('ref_axis',(1.,0.,5.99026163859831E-14));
#30795=DIRECTION('center_axis',(0.,-1.,0.));
#30796=DIRECTION('ref_axis',(-0.160423232777043,0.,-0.987048320187701));
#30797=DIRECTION('',(0.,1.,0.));
#30798=DIRECTION('center_axis',(0.,-1.,0.));
#30799=DIRECTION('ref_axis',(-0.160423232777043,0.,-0.987048320187701));
#30800=DIRECTION('',(0.,1.,0.));
#30801=DIRECTION('center_axis',(0.,-1.,0.));
#30802=DIRECTION('ref_axis',(-0.160423232777043,0.,-0.987048320187701));
#30803=DIRECTION('',(0.,1.,0.));
#30804=DIRECTION('center_axis',(0.,-1.,0.));
#30805=DIRECTION('ref_axis',(-0.160423232777043,0.,-0.987048320187701));
#30806=DIRECTION('',(0.,1.,0.));
#30807=DIRECTION('center_axis',(0.,-1.,0.));
#30808=DIRECTION('ref_axis',(-0.160423232777043,0.,-0.987048320187701));
#30809=DIRECTION('',(0.,1.,0.));
#30810=DIRECTION('center_axis',(0.,-1.,0.));
#30811=DIRECTION('ref_axis',(-0.160423232777043,0.,-0.987048320187701));
#30812=DIRECTION('',(0.,1.,0.));
#30813=DIRECTION('center_axis',(0.,-1.,0.));
#30814=DIRECTION('ref_axis',(-0.160423232777043,0.,-0.987048320187701));
#30815=DIRECTION('',(0.,1.,0.));
#30816=DIRECTION('center_axis',(0.,-1.,0.));
#30817=DIRECTION('ref_axis',(-0.160423232777043,0.,-0.987048320187701));
#30818=DIRECTION('',(0.,1.,0.));
#30819=DIRECTION('center_axis',(0.,-1.,0.));
#30820=DIRECTION('ref_axis',(-0.160423232777043,0.,-0.987048320187701));
#30821=DIRECTION('',(0.,1.,0.));
#30822=DIRECTION('center_axis',(0.,-1.,0.));
#30823=DIRECTION('ref_axis',(-0.160423232777043,0.,-0.987048320187701));
#30824=DIRECTION('',(0.,1.,0.));
#30825=DIRECTION('center_axis',(0.,-1.,0.));
#30826=DIRECTION('ref_axis',(1.,0.,0.));
#30827=DIRECTION('',(0.,1.,0.));
#30828=DIRECTION('center_axis',(0.,1.,0.));
#30829=DIRECTION('ref_axis',(1.,0.,0.));
#30830=DIRECTION('center_axis',(0.,-1.,0.));
#30831=DIRECTION('ref_axis',(1.,0.,0.));
#30832=DIRECTION('',(0.,1.,0.));
#30833=DIRECTION('center_axis',(0.,-1.,0.));
#30834=DIRECTION('ref_axis',(1.,0.,0.));
#30835=DIRECTION('',(0.,1.,0.));
#30836=DIRECTION('center_axis',(0.,-1.,0.));
#30837=DIRECTION('ref_axis',(1.,0.,0.));
#30838=DIRECTION('',(0.,1.,0.));
#30839=DIRECTION('center_axis',(0.,-1.,0.));
#30840=DIRECTION('ref_axis',(1.,0.,0.));
#30841=DIRECTION('',(0.,1.,0.));
#30842=DIRECTION('center_axis',(0.,-1.,0.));
#30843=DIRECTION('ref_axis',(1.,0.,0.));
#30844=DIRECTION('',(0.,1.,0.));
#30845=DIRECTION('center_axis',(0.,-1.,0.));
#30846=DIRECTION('ref_axis',(1.,0.,0.));
#30847=DIRECTION('',(0.,1.,0.));
#30848=DIRECTION('center_axis',(0.,-1.,0.));
#30849=DIRECTION('ref_axis',(1.,0.,0.));
#30850=DIRECTION('',(0.,1.,0.));
#30851=DIRECTION('center_axis',(0.,-1.,0.));
#30852=DIRECTION('ref_axis',(1.,0.,0.));
#30853=DIRECTION('',(0.,1.,0.));
#30854=DIRECTION('center_axis',(0.,-1.,0.));
#30855=DIRECTION('ref_axis',(1.,0.,0.));
#30856=DIRECTION('',(0.,1.,0.));
#30857=DIRECTION('center_axis',(0.,-1.,0.));
#30858=DIRECTION('ref_axis',(1.,0.,0.));
#30859=DIRECTION('',(0.,1.,0.));
#30860=DIRECTION('center_axis',(0.,-1.,0.));
#30861=DIRECTION('ref_axis',(1.,0.,0.));
#30862=DIRECTION('center_axis',(0.,-1.,0.));
#30863=DIRECTION('ref_axis',(1.,0.,0.));
#30864=DIRECTION('center_axis',(0.,-1.,0.));
#30865=DIRECTION('ref_axis',(-0.160423232777043,0.,-0.987048320187701));
#30866=DIRECTION('center_axis',(0.,-1.,0.));
#30867=DIRECTION('ref_axis',(1.,0.,5.99026163859831E-14));
#30868=DIRECTION('center_axis',(0.,1.,0.));
#30869=DIRECTION('ref_axis',(0.,0.,1.));
#30870=DIRECTION('center_axis',(0.,-1.,0.));
#30871=DIRECTION('ref_axis',(1.,0.,0.));
#30872=DIRECTION('center_axis',(0.,-1.,0.));
#30873=DIRECTION('ref_axis',(1.,0.,0.));
#30874=DIRECTION('center_axis',(0.,1.,0.));
#30875=DIRECTION('ref_axis',(0.,0.,1.));
#30876=DIRECTION('center_axis',(0.,1.,0.));
#30877=DIRECTION('ref_axis',(1.,0.,0.));
#30878=DIRECTION('center_axis',(0.,1.,0.));
#30879=DIRECTION('ref_axis',(1.,0.,0.));
#30880=DIRECTION('center_axis',(0.,1.,0.));
#30881=DIRECTION('ref_axis',(0.,0.,1.));
#30882=DIRECTION('center_axis',(0.,-1.,0.));
#30883=DIRECTION('ref_axis',(1.,0.,0.));
#30884=DIRECTION('center_axis',(1.,0.,-1.22464679914735E-16));
#30885=DIRECTION('ref_axis',(-1.22464679914735E-16,0.,-1.));
#30886=DIRECTION('center_axis',(0.,1.,0.));
#30887=DIRECTION('ref_axis',(1.,0.,0.));
#30888=DIRECTION('center_axis',(0.,1.,0.));
#30889=DIRECTION('ref_axis',(1.,0.,0.));
#30890=DIRECTION('center_axis',(0.,1.,0.));
#30891=DIRECTION('ref_axis',(1.,0.,0.));
#30892=DIRECTION('',(0.707106781186546,-0.707106781186549,-8.65956056235491E-17));
#30893=DIRECTION('center_axis',(0.,1.,0.));
#30894=DIRECTION('ref_axis',(1.,0.,0.));
#30895=DIRECTION('center_axis',(0.,1.,0.));
#30896=DIRECTION('ref_axis',(1.,0.,0.));
#30897=DIRECTION('center_axis',(-0.49353398197848,0.,-0.869726513699833));
#30898=DIRECTION('ref_axis',(0.869726513699833,0.,-0.49353398197848));
#30899=DIRECTION('',(0.,-1.,0.));
#30900=DIRECTION('',(0.869726513699833,0.,-0.49353398197848));
#30901=DIRECTION('',(0.,-1.,0.));
#30902=DIRECTION('center_axis',(0.,-1.,0.));
#30903=DIRECTION('ref_axis',(-0.17364817766693,0.,-0.984807753012208));
#30904=DIRECTION('center_axis',(0.,-1.,0.));
#30905=DIRECTION('ref_axis',(1.,0.,0.));
#30906=DIRECTION('',(-0.986074150277955,0.,-0.166306254102512));
#30907=DIRECTION('center_axis',(-0.166306254102512,0.,0.986074150277955));
#30908=DIRECTION('ref_axis',(-0.986074150277955,0.,-0.166306254102512));
#30909=DIRECTION('',(0.,1.,0.));
#30910=DIRECTION('center_axis',(0.,1.,0.));
#30911=DIRECTION('ref_axis',(1.,0.,0.));
#30912=DIRECTION('center_axis',(0.,-1.,0.));
#30913=DIRECTION('ref_axis',(1.,0.,0.));
#30914=DIRECTION('',(0.,-1.,0.));
#30915=DIRECTION('center_axis',(0.,-1.,0.));
#30916=DIRECTION('ref_axis',(1.,0.,0.));
#30917=DIRECTION('center_axis',(0.,-1.,0.));
#30918=DIRECTION('ref_axis',(1.,0.,0.));
#30919=DIRECTION('center_axis',(0.,-1.,0.));
#30920=DIRECTION('ref_axis',(1.,0.,0.));
#30921=DIRECTION('',(0.,1.,0.));
#30922=DIRECTION('center_axis',(0.,1.,0.));
#30923=DIRECTION('ref_axis',(1.,0.,0.));
#30924=DIRECTION('',(0.,-1.,0.));
#30925=DIRECTION('center_axis',(0.,-1.,0.));
#30926=DIRECTION('ref_axis',(1.,0.,0.));
#30927=DIRECTION('',(0.,1.,0.));
#30928=DIRECTION('center_axis',(0.,1.,0.));
#30929=DIRECTION('ref_axis',(1.,0.,0.));
#30930=DIRECTION('',(0.,-1.,0.));
#30931=DIRECTION('center_axis',(0.,-1.,0.));
#30932=DIRECTION('ref_axis',(1.,0.,0.));
#30933=DIRECTION('',(0.,1.,0.));
#30934=DIRECTION('center_axis',(0.,1.,0.));
#30935=DIRECTION('ref_axis',(1.,0.,0.));
#30936=DIRECTION('',(0.,-1.,0.));
#30937=DIRECTION('center_axis',(0.,-1.,0.));
#30938=DIRECTION('ref_axis',(1.,0.,0.));
#30939=DIRECTION('',(0.,1.,0.));
#30940=DIRECTION('center_axis',(0.,1.,0.));
#30941=DIRECTION('ref_axis',(1.,0.,0.));
#30942=DIRECTION('',(0.,-1.,0.));
#30943=DIRECTION('center_axis',(0.,-1.,0.));
#30944=DIRECTION('ref_axis',(1.,0.,0.));
#30945=DIRECTION('',(0.,1.,0.));
#30946=DIRECTION('center_axis',(0.,1.,0.));
#30947=DIRECTION('ref_axis',(1.,0.,0.));
#30948=DIRECTION('',(0.,-1.,0.));
#30949=DIRECTION('center_axis',(0.,-1.,0.));
#30950=DIRECTION('ref_axis',(1.,0.,0.));
#30951=DIRECTION('',(0.,1.,0.));
#30952=DIRECTION('center_axis',(0.,1.,0.));
#30953=DIRECTION('ref_axis',(1.,0.,0.));
#30954=DIRECTION('',(0.,-1.,0.));
#30955=DIRECTION('center_axis',(0.,-1.,0.));
#30956=DIRECTION('ref_axis',(1.,0.,0.));
#30957=DIRECTION('',(0.,1.,0.));
#30958=DIRECTION('center_axis',(0.,1.,0.));
#30959=DIRECTION('ref_axis',(1.,0.,0.));
#30960=DIRECTION('',(0.,-1.,0.));
#30961=DIRECTION('center_axis',(0.,-1.,0.));
#30962=DIRECTION('ref_axis',(1.,0.,0.));
#30963=DIRECTION('',(0.,1.,0.));
#30964=DIRECTION('center_axis',(0.,1.,0.));
#30965=DIRECTION('ref_axis',(1.,0.,0.));
#30966=DIRECTION('',(0.,-1.,0.));
#30967=DIRECTION('center_axis',(0.,-1.,0.));
#30968=DIRECTION('ref_axis',(1.,0.,0.));
#30969=DIRECTION('',(0.,1.,0.));
#30970=DIRECTION('center_axis',(0.,1.,0.));
#30971=DIRECTION('ref_axis',(1.,0.,0.));
#30972=DIRECTION('',(0.,-1.,0.));
#30973=DIRECTION('center_axis',(0.,-1.,0.));
#30974=DIRECTION('ref_axis',(1.,0.,0.));
#30975=DIRECTION('',(0.,1.,0.));
#30976=DIRECTION('center_axis',(0.,1.,0.));
#30977=DIRECTION('ref_axis',(1.,0.,0.));
#30978=DIRECTION('',(0.,-1.,0.));
#30979=DIRECTION('center_axis',(0.,-1.,0.));
#30980=DIRECTION('ref_axis',(1.,0.,0.));
#30981=DIRECTION('',(0.,1.,0.));
#30982=DIRECTION('center_axis',(0.,1.,0.));
#30983=DIRECTION('ref_axis',(1.,0.,0.));
#30984=DIRECTION('',(0.,-1.,0.));
#30985=DIRECTION('center_axis',(0.,-1.,0.));
#30986=DIRECTION('ref_axis',(1.,0.,0.));
#30987=DIRECTION('',(0.,1.,0.));
#30988=DIRECTION('center_axis',(0.,1.,0.));
#30989=DIRECTION('ref_axis',(1.,0.,0.));
#30990=DIRECTION('',(0.,-1.,0.));
#30991=DIRECTION('center_axis',(0.,-1.,0.));
#30992=DIRECTION('ref_axis',(1.,0.,0.));
#30993=DIRECTION('',(0.,1.,0.));
#30994=DIRECTION('center_axis',(0.,1.,0.));
#30995=DIRECTION('ref_axis',(1.,0.,0.));
#30996=DIRECTION('',(0.,-1.,0.));
#30997=DIRECTION('center_axis',(0.,-1.,0.));
#30998=DIRECTION('ref_axis',(1.,0.,0.));
#30999=DIRECTION('',(0.,1.,0.));
#31000=DIRECTION('center_axis',(0.,1.,0.));
#31001=DIRECTION('ref_axis',(1.,0.,0.));
#31002=DIRECTION('',(0.,-1.,0.));
#31003=DIRECTION('center_axis',(0.,-1.,0.));
#31004=DIRECTION('ref_axis',(1.,0.,0.));
#31005=DIRECTION('',(0.,1.,0.));
#31006=DIRECTION('center_axis',(0.,1.,0.));
#31007=DIRECTION('ref_axis',(1.,0.,0.));
#31008=DIRECTION('',(0.,-1.,0.));
#31009=DIRECTION('center_axis',(0.,-1.,0.));
#31010=DIRECTION('ref_axis',(1.,0.,0.));
#31011=DIRECTION('',(0.,1.,0.));
#31012=DIRECTION('center_axis',(0.,1.,0.));
#31013=DIRECTION('ref_axis',(1.,0.,0.));
#31014=DIRECTION('',(0.,-1.,0.));
#31015=DIRECTION('center_axis',(0.,-1.,0.));
#31016=DIRECTION('ref_axis',(1.,0.,0.));
#31017=DIRECTION('',(0.,1.,0.));
#31018=DIRECTION('center_axis',(0.,1.,0.));
#31019=DIRECTION('ref_axis',(1.,0.,0.));
#31020=DIRECTION('center_axis',(0.,1.,0.));
#31021=DIRECTION('ref_axis',(1.,0.,0.));
#31022=DIRECTION('',(0.,-1.,0.));
#31023=DIRECTION('center_axis',(0.,-1.,0.));
#31024=DIRECTION('ref_axis',(1.,0.,0.));
#31025=DIRECTION('',(0.,1.,0.));
#31026=DIRECTION('center_axis',(0.,1.,0.));
#31027=DIRECTION('ref_axis',(1.,0.,0.));
#31028=DIRECTION('',(0.,-1.,0.));
#31029=DIRECTION('center_axis',(0.,-1.,0.));
#31030=DIRECTION('ref_axis',(1.,0.,0.));
#31031=DIRECTION('',(0.,1.,0.));
#31032=DIRECTION('center_axis',(0.,1.,0.));
#31033=DIRECTION('ref_axis',(1.,0.,0.));
#31034=DIRECTION('',(0.,-1.,0.));
#31035=DIRECTION('center_axis',(0.,-1.,0.));
#31036=DIRECTION('ref_axis',(1.,0.,0.));
#31037=DIRECTION('',(0.,1.,0.));
#31038=DIRECTION('center_axis',(0.,1.,0.));
#31039=DIRECTION('ref_axis',(1.,0.,0.));
#31040=DIRECTION('',(0.,-1.,0.));
#31041=DIRECTION('center_axis',(0.,-1.,0.));
#31042=DIRECTION('ref_axis',(1.,0.,0.));
#31043=DIRECTION('',(0.,1.,0.));
#31044=DIRECTION('center_axis',(0.,1.,0.));
#31045=DIRECTION('ref_axis',(1.,0.,0.));
#31046=DIRECTION('',(0.,-1.,0.));
#31047=DIRECTION('center_axis',(0.,-1.,0.));
#31048=DIRECTION('ref_axis',(1.,0.,0.));
#31049=DIRECTION('',(0.,1.,0.));
#31050=DIRECTION('center_axis',(0.,1.,0.));
#31051=DIRECTION('ref_axis',(1.,0.,0.));
#31052=DIRECTION('',(0.,-1.,0.));
#31053=DIRECTION('center_axis',(0.,-1.,0.));
#31054=DIRECTION('ref_axis',(1.,0.,0.));
#31055=DIRECTION('',(0.,1.,0.));
#31056=DIRECTION('center_axis',(0.,1.,0.));
#31057=DIRECTION('ref_axis',(1.,0.,0.));
#31058=DIRECTION('',(0.,-1.,0.));
#31059=DIRECTION('center_axis',(0.,-1.,0.));
#31060=DIRECTION('ref_axis',(1.,0.,0.));
#31061=DIRECTION('',(0.,1.,0.));
#31062=DIRECTION('center_axis',(0.,1.,0.));
#31063=DIRECTION('ref_axis',(1.,0.,0.));
#31064=DIRECTION('',(0.,-1.,0.));
#31065=DIRECTION('center_axis',(0.,-1.,0.));
#31066=DIRECTION('ref_axis',(1.,0.,0.));
#31067=DIRECTION('',(0.,1.,0.));
#31068=DIRECTION('center_axis',(0.,1.,0.));
#31069=DIRECTION('ref_axis',(1.,0.,0.));
#31070=DIRECTION('',(0.,-1.,0.));
#31071=DIRECTION('center_axis',(0.,-1.,0.));
#31072=DIRECTION('ref_axis',(1.,0.,0.));
#31073=DIRECTION('',(0.,1.,0.));
#31074=DIRECTION('center_axis',(0.,1.,0.));
#31075=DIRECTION('ref_axis',(1.,0.,0.));
#31076=DIRECTION('',(0.,-1.,0.));
#31077=DIRECTION('center_axis',(0.,-1.,0.));
#31078=DIRECTION('ref_axis',(1.,0.,0.));
#31079=DIRECTION('',(0.,1.,0.));
#31080=DIRECTION('center_axis',(0.,1.,0.));
#31081=DIRECTION('ref_axis',(1.,0.,0.));
#31082=DIRECTION('',(0.,-1.,0.));
#31083=DIRECTION('center_axis',(0.,-1.,0.));
#31084=DIRECTION('ref_axis',(1.,0.,0.));
#31085=DIRECTION('',(0.,1.,0.));
#31086=DIRECTION('center_axis',(0.,1.,0.));
#31087=DIRECTION('ref_axis',(1.,0.,0.));
#31088=DIRECTION('',(0.,-1.,0.));
#31089=DIRECTION('center_axis',(0.,-1.,0.));
#31090=DIRECTION('ref_axis',(1.,0.,0.));
#31091=DIRECTION('',(0.,1.,0.));
#31092=DIRECTION('center_axis',(0.,1.,0.));
#31093=DIRECTION('ref_axis',(1.,0.,0.));
#31094=DIRECTION('',(0.,-1.,0.));
#31095=DIRECTION('center_axis',(0.,-1.,0.));
#31096=DIRECTION('ref_axis',(1.,0.,0.));
#31097=DIRECTION('',(0.,1.,0.));
#31098=DIRECTION('center_axis',(0.,1.,0.));
#31099=DIRECTION('ref_axis',(1.,0.,0.));
#31100=DIRECTION('',(0.,-1.,0.));
#31101=DIRECTION('center_axis',(0.,-1.,0.));
#31102=DIRECTION('ref_axis',(1.,0.,0.));
#31103=DIRECTION('',(0.,1.,0.));
#31104=DIRECTION('center_axis',(0.,1.,0.));
#31105=DIRECTION('ref_axis',(1.,0.,0.));
#31106=DIRECTION('',(0.,-1.,0.));
#31107=DIRECTION('center_axis',(0.,-1.,0.));
#31108=DIRECTION('ref_axis',(1.,0.,0.));
#31109=DIRECTION('',(0.,1.,0.));
#31110=DIRECTION('center_axis',(0.,1.,0.));
#31111=DIRECTION('ref_axis',(1.,0.,0.));
#31112=DIRECTION('',(0.,-1.,0.));
#31113=DIRECTION('center_axis',(0.,-1.,0.));
#31114=DIRECTION('ref_axis',(1.,0.,0.));
#31115=DIRECTION('',(0.,1.,0.));
#31116=DIRECTION('center_axis',(0.,1.,0.));
#31117=DIRECTION('ref_axis',(1.,0.,0.));
#31118=DIRECTION('',(0.,-1.,0.));
#31119=DIRECTION('center_axis',(0.,-1.,0.));
#31120=DIRECTION('ref_axis',(1.,0.,0.));
#31121=DIRECTION('',(0.,1.,0.));
#31122=DIRECTION('center_axis',(0.,1.,0.));
#31123=DIRECTION('ref_axis',(1.,0.,0.));
#31124=DIRECTION('',(0.,-1.,0.));
#31125=DIRECTION('center_axis',(0.,-1.,0.));
#31126=DIRECTION('ref_axis',(1.,0.,0.));
#31127=DIRECTION('',(0.,1.,0.));
#31128=DIRECTION('center_axis',(0.,1.,0.));
#31129=DIRECTION('ref_axis',(1.,0.,0.));
#31130=DIRECTION('',(0.,-1.,0.));
#31131=DIRECTION('center_axis',(-0.637062515999983,0.,-0.770812137104607));
#31132=DIRECTION('ref_axis',(0.770812137104607,0.,-0.637062515999983));
#31133=DIRECTION('',(0.,-1.,0.));
#31134=DIRECTION('',(0.770812137104607,0.,-0.637062515999983));
#31135=DIRECTION('center_axis',(0.,-1.,0.));
#31136=DIRECTION('ref_axis',(-0.342020143325669,0.,-0.939692620785908));
#31137=DIRECTION('',(-0.99997224619817,0.,0.00745029082566251));
#31138=DIRECTION('center_axis',(0.00745029082566245,0.,0.99997224619817));
#31139=DIRECTION('ref_axis',(-0.99997224619817,0.,0.00745029082566245));
#31140=DIRECTION('center_axis',(-0.761234227842014,0.,-0.648477023773219));
#31141=DIRECTION('ref_axis',(0.648477023773219,0.,-0.761234227842014));
#31142=DIRECTION('',(0.,-1.,0.));
#31143=DIRECTION('',(0.648477023773219,0.,-0.761234227842014));
#31144=DIRECTION('center_axis',(0.,-1.,0.));
#31145=DIRECTION('ref_axis',(-0.5,0.,-0.866025403784438));
#31146=DIRECTION('',(-0.983486691428025,0.,0.180980462437127));
#31147=DIRECTION('center_axis',(0.180980462437127,0.,0.983486691428025));
#31148=DIRECTION('ref_axis',(-0.983486691428025,0.,0.180980462437127));
#31149=DIRECTION('center_axis',(-0.862276222874171,0.,-0.50643826421969));
#31150=DIRECTION('ref_axis',(0.50643826421969,0.,-0.862276222874171));
#31151=DIRECTION('',(0.,-1.,0.));
#31152=DIRECTION('',(0.50643826421969,0.,-0.862276222874171));
#31153=DIRECTION('center_axis',(0.,-1.,0.));
#31154=DIRECTION('ref_axis',(-0.64278760968654,0.,-0.766044443118978));
#31155=DIRECTION('',(-0.937118391207119,0.,0.349011634277972));
#31156=DIRECTION('center_axis',(0.349011634277973,0.,0.937118391207119));
#31157=DIRECTION('ref_axis',(-0.937118391207119,0.,0.349011634277973));
#31158=DIRECTION('center_axis',(-0.937118391207119,0.,-0.349011634277972));
#31159=DIRECTION('ref_axis',(0.349011634277972,0.,-0.937118391207119));
#31160=DIRECTION('',(0.,-1.,0.));
#31161=DIRECTION('',(0.349011634277972,0.,-0.937118391207119));
#31162=DIRECTION('center_axis',(0.,-1.,0.));
#31163=DIRECTION('ref_axis',(-0.766044443118978,0.,-0.642787609686539));
#31164=DIRECTION('',(-0.862276222874171,0.,0.50643826421969));
#31165=DIRECTION('center_axis',(0.50643826421969,0.,0.862276222874171));
#31166=DIRECTION('ref_axis',(-0.862276222874171,0.,0.50643826421969));
#31167=DIRECTION('center_axis',(-0.983486691428025,0.,-0.180980462437127));
#31168=DIRECTION('ref_axis',(0.180980462437127,0.,-0.983486691428025));
#31169=DIRECTION('',(0.,-1.,0.));
#31170=DIRECTION('',(0.180980462437127,0.,-0.983486691428025));
#31171=DIRECTION('center_axis',(0.,-1.,0.));
#31172=DIRECTION('ref_axis',(-0.866025403784439,0.,-0.5));
#31173=DIRECTION('',(-0.761234227842014,0.,0.64847702377322));
#31174=DIRECTION('center_axis',(0.648477023773219,0.,0.761234227842014));
#31175=DIRECTION('ref_axis',(-0.761234227842014,0.,0.648477023773219));
#31176=DIRECTION('center_axis',(-0.99997224619817,0.,-0.00745029082566118));
#31177=DIRECTION('ref_axis',(0.00745029082566118,0.,-0.99997224619817));
#31178=DIRECTION('',(0.,-1.,0.));
#31179=DIRECTION('',(0.00745029082566118,0.,-0.99997224619817));
#31180=DIRECTION('center_axis',(0.,-1.,0.));
#31181=DIRECTION('ref_axis',(-0.939692620785909,0.,-0.342020143325668));
#31182=DIRECTION('',(-0.637062515999982,0.,0.770812137104608));
#31183=DIRECTION('center_axis',(0.770812137104608,0.,0.637062515999982));
#31184=DIRECTION('ref_axis',(-0.637062515999982,0.,0.770812137104608));
#31185=DIRECTION('center_axis',(-0.986074150277955,0.,0.166306254102512));
#31186=DIRECTION('ref_axis',(-0.166306254102512,0.,-0.986074150277955));
#31187=DIRECTION('',(0.,-1.,0.));
#31188=DIRECTION('',(-0.166306254102512,0.,-0.986074150277955));
#31189=DIRECTION('center_axis',(0.,-1.,0.));
#31190=DIRECTION('ref_axis',(-0.984807753012208,0.,-0.17364817766693));
#31191=DIRECTION('',(-0.493533981978479,0.,0.869726513699833));
#31192=DIRECTION('center_axis',(0.869726513699833,0.,0.493533981978479));
#31193=DIRECTION('ref_axis',(-0.493533981978479,0.,0.869726513699833));
#31194=DIRECTION('center_axis',(-0.942214690279141,0.,0.335009667654806));
#31195=DIRECTION('ref_axis',(-0.335009667654806,0.,-0.94221469027914));
#31196=DIRECTION('',(0.,-1.,0.));
#31197=DIRECTION('',(-0.335009667654806,0.,-0.94221469027914));
#31198=DIRECTION('center_axis',(0.,-1.,0.));
#31199=DIRECTION('ref_axis',(-1.,0.,1.83697019872103E-16));
#31200=DIRECTION('',(-0.335009667654805,0.,0.942214690279141));
#31201=DIRECTION('center_axis',(0.942214690279141,0.,0.335009667654805));
#31202=DIRECTION('ref_axis',(-0.335009667654805,0.,0.942214690279141));
#31203=DIRECTION('center_axis',(-0.869726513699833,0.,0.49353398197848));
#31204=DIRECTION('ref_axis',(-0.49353398197848,0.,-0.869726513699833));
#31205=DIRECTION('',(0.,-1.,0.));
#31206=DIRECTION('',(-0.49353398197848,0.,-0.869726513699833));
#31207=DIRECTION('center_axis',(0.,-1.,0.));
#31208=DIRECTION('ref_axis',(-0.984807753012208,0.,0.17364817766693));
#31209=DIRECTION('',(-0.166306254102512,0.,0.986074150277955));
#31210=DIRECTION('center_axis',(0.986074150277955,0.,0.166306254102512));
#31211=DIRECTION('ref_axis',(-0.166306254102512,0.,0.986074150277955));
#31212=DIRECTION('center_axis',(-0.770812137104607,0.,0.637062515999983));
#31213=DIRECTION('ref_axis',(-0.637062515999983,0.,-0.770812137104607));
#31214=DIRECTION('',(0.,-1.,0.));
#31215=DIRECTION('',(-0.637062515999983,0.,-0.770812137104607));
#31216=DIRECTION('center_axis',(0.,-1.,0.));
#31217=DIRECTION('ref_axis',(-0.939692620785908,0.,0.342020143325669));
#31218=DIRECTION('',(0.0074502908256624,0.,0.99997224619817));
#31219=DIRECTION('center_axis',(0.99997224619817,0.,-0.00745029082566234));
#31220=DIRECTION('ref_axis',(0.00745029082566234,0.,0.99997224619817));
#31221=DIRECTION('center_axis',(-0.648477023773219,0.,0.761234227842014));
#31222=DIRECTION('ref_axis',(-0.761234227842014,0.,-0.648477023773219));
#31223=DIRECTION('',(0.,-1.,0.));
#31224=DIRECTION('',(-0.761234227842014,0.,-0.648477023773219));
#31225=DIRECTION('center_axis',(0.,-1.,0.));
#31226=DIRECTION('ref_axis',(-0.866025403784438,0.,0.5));
#31227=DIRECTION('',(0.180980462437127,0.,0.983486691428025));
#31228=DIRECTION('center_axis',(0.983486691428025,0.,-0.180980462437127));
#31229=DIRECTION('ref_axis',(0.180980462437127,0.,0.983486691428025));
#31230=DIRECTION('center_axis',(-0.50643826421969,0.,0.862276222874171));
#31231=DIRECTION('ref_axis',(-0.862276222874171,0.,-0.50643826421969));
#31232=DIRECTION('',(0.,-1.,0.));
#31233=DIRECTION('',(-0.862276222874171,0.,-0.50643826421969));
#31234=DIRECTION('center_axis',(0.,-1.,0.));
#31235=DIRECTION('ref_axis',(-0.766044443118978,0.,0.642787609686539));
#31236=DIRECTION('',(0.349011634277972,0.,0.937118391207119));
#31237=DIRECTION('center_axis',(0.937118391207119,0.,-0.349011634277972));
#31238=DIRECTION('ref_axis',(0.349011634277972,0.,0.937118391207119));
#31239=DIRECTION('center_axis',(-0.349011634277972,0.,0.937118391207119));
#31240=DIRECTION('ref_axis',(-0.937118391207119,0.,-0.349011634277972));
#31241=DIRECTION('',(0.,-1.,0.));
#31242=DIRECTION('',(-0.937118391207119,0.,-0.349011634277972));
#31243=DIRECTION('center_axis',(0.,-1.,0.));
#31244=DIRECTION('ref_axis',(-0.642787609686539,0.,0.766044443118978));
#31245=DIRECTION('',(0.50643826421969,0.,0.862276222874171));
#31246=DIRECTION('center_axis',(0.862276222874171,0.,-0.50643826421969));
#31247=DIRECTION('ref_axis',(0.50643826421969,0.,0.862276222874171));
#31248=DIRECTION('center_axis',(-0.180980462437126,0.,0.983486691428025));
#31249=DIRECTION('ref_axis',(-0.983486691428025,0.,-0.180980462437126));
#31250=DIRECTION('',(0.,-1.,0.));
#31251=DIRECTION('',(-0.983486691428025,0.,-0.180980462437126));
#31252=DIRECTION('center_axis',(0.,-1.,0.));
#31253=DIRECTION('ref_axis',(-0.5,0.,0.866025403784439));
#31254=DIRECTION('',(0.64847702377322,0.,0.761234227842014));
#31255=DIRECTION('center_axis',(0.761234227842014,0.,-0.64847702377322));
#31256=DIRECTION('ref_axis',(0.64847702377322,0.,0.761234227842014));
#31257=DIRECTION('center_axis',(-0.00745029082566162,0.,0.99997224619817));
#31258=DIRECTION('ref_axis',(-0.99997224619817,0.,-0.00745029082566162));
#31259=DIRECTION('',(0.,-1.,0.));
#31260=DIRECTION('',(-0.99997224619817,0.,-0.00745029082566162));
#31261=DIRECTION('center_axis',(0.,-1.,0.));
#31262=DIRECTION('ref_axis',(-0.342020143325669,0.,0.939692620785908));
#31263=DIRECTION('',(0.770812137104607,0.,0.637062515999983));
#31264=DIRECTION('center_axis',(0.637062515999983,0.,-0.770812137104607));
#31265=DIRECTION('ref_axis',(0.770812137104607,0.,0.637062515999983));
#31266=DIRECTION('center_axis',(0.166306254102512,0.,0.986074150277955));
#31267=DIRECTION('ref_axis',(-0.986074150277955,0.,0.166306254102512));
#31268=DIRECTION('',(0.,-1.,0.));
#31269=DIRECTION('',(-0.986074150277955,0.,0.166306254102512));
#31270=DIRECTION('center_axis',(0.,-1.,0.));
#31271=DIRECTION('ref_axis',(-0.17364817766693,0.,0.984807753012208));
#31272=DIRECTION('',(0.869726513699833,0.,0.493533981978479));
#31273=DIRECTION('center_axis',(0.493533981978479,0.,-0.869726513699833));
#31274=DIRECTION('ref_axis',(0.869726513699833,0.,0.493533981978479));
#31275=DIRECTION('center_axis',(0.335009667654806,0.,0.942214690279141));
#31276=DIRECTION('ref_axis',(-0.94221469027914,0.,0.335009667654806));
#31277=DIRECTION('',(0.,-1.,0.));
#31278=DIRECTION('',(-0.94221469027914,0.,0.335009667654806));
#31279=DIRECTION('center_axis',(0.,-1.,0.));
#31280=DIRECTION('ref_axis',(1.22464679914735E-16,0.,1.));
#31281=DIRECTION('',(0.94221469027914,0.,0.335009667654806));
#31282=DIRECTION('center_axis',(0.335009667654806,0.,-0.942214690279141));
#31283=DIRECTION('ref_axis',(0.94221469027914,0.,0.335009667654806));
#31284=DIRECTION('center_axis',(0.49353398197848,0.,0.869726513699833));
#31285=DIRECTION('ref_axis',(-0.869726513699833,0.,0.49353398197848));
#31286=DIRECTION('',(0.,-1.,0.));
#31287=DIRECTION('',(-0.869726513699833,0.,0.49353398197848));
#31288=DIRECTION('center_axis',(0.,-1.,0.));
#31289=DIRECTION('ref_axis',(0.173648177666931,0.,0.984807753012208));
#31290=DIRECTION('',(0.986074150277955,0.,0.166306254102511));
#31291=DIRECTION('center_axis',(0.166306254102511,0.,-0.986074150277955));
#31292=DIRECTION('ref_axis',(0.986074150277955,0.,0.166306254102511));
#31293=DIRECTION('center_axis',(0.637062515999983,0.,0.770812137104607));
#31294=DIRECTION('ref_axis',(-0.770812137104607,0.,0.637062515999983));
#31295=DIRECTION('',(0.,-1.,0.));
#31296=DIRECTION('',(-0.770812137104607,0.,0.637062515999983));
#31297=DIRECTION('center_axis',(0.,-1.,0.));
#31298=DIRECTION('ref_axis',(0.342020143325669,0.,0.939692620785908));
#31299=DIRECTION('',(0.99997224619817,0.,-0.0074502908256619));
#31300=DIRECTION('center_axis',(-0.0074502908256619,0.,-0.99997224619817));
#31301=DIRECTION('ref_axis',(0.99997224619817,0.,-0.0074502908256619));
#31302=DIRECTION('center_axis',(0.761234227842014,0.,0.64847702377322));
#31303=DIRECTION('ref_axis',(-0.64847702377322,0.,0.761234227842014));
#31304=DIRECTION('',(0.,-1.,0.));
#31305=DIRECTION('',(-0.64847702377322,0.,0.761234227842014));
#31306=DIRECTION('center_axis',(0.,-1.,0.));
#31307=DIRECTION('ref_axis',(0.5,0.,0.866025403784439));
#31308=DIRECTION('',(0.983486691428025,0.,-0.180980462437127));
#31309=DIRECTION('center_axis',(-0.180980462437127,0.,-0.983486691428025));
#31310=DIRECTION('ref_axis',(0.983486691428025,0.,-0.180980462437127));
#31311=DIRECTION('center_axis',(0.862276222874171,0.,0.50643826421969));
#31312=DIRECTION('ref_axis',(-0.50643826421969,0.,0.862276222874171));
#31313=DIRECTION('',(0.,-1.,0.));
#31314=DIRECTION('',(-0.50643826421969,0.,0.862276222874171));
#31315=DIRECTION('center_axis',(0.,-1.,0.));
#31316=DIRECTION('ref_axis',(0.642787609686539,0.,0.766044443118978));
#31317=DIRECTION('',(0.937118391207119,0.,-0.349011634277972));
#31318=DIRECTION('center_axis',(-0.349011634277972,0.,-0.937118391207119));
#31319=DIRECTION('ref_axis',(0.937118391207119,0.,-0.349011634277972));
#31320=DIRECTION('center_axis',(0.937118391207119,0.,0.349011634277972));
#31321=DIRECTION('ref_axis',(-0.349011634277972,0.,0.937118391207119));
#31322=DIRECTION('',(0.,-1.,0.));
#31323=DIRECTION('',(-0.349011634277972,0.,0.937118391207119));
#31324=DIRECTION('center_axis',(0.,-1.,0.));
#31325=DIRECTION('ref_axis',(0.766044443118978,0.,0.642787609686539));
#31326=DIRECTION('',(0.862276222874171,0.,-0.50643826421969));
#31327=DIRECTION('center_axis',(-0.50643826421969,0.,-0.862276222874171));
#31328=DIRECTION('ref_axis',(0.862276222874171,0.,-0.50643826421969));
#31329=DIRECTION('center_axis',(0.983486691428025,0.,0.180980462437126));
#31330=DIRECTION('ref_axis',(-0.180980462437126,0.,0.983486691428025));
#31331=DIRECTION('',(0.,-1.,0.));
#31332=DIRECTION('',(-0.180980462437126,0.,0.983486691428025));
#31333=DIRECTION('center_axis',(0.,-1.,0.));
#31334=DIRECTION('ref_axis',(0.866025403784439,0.,0.5));
#31335=DIRECTION('',(0.761234227842014,0.,-0.64847702377322));
#31336=DIRECTION('center_axis',(-0.64847702377322,0.,-0.761234227842014));
#31337=DIRECTION('ref_axis',(0.761234227842014,0.,-0.64847702377322));
#31338=DIRECTION('center_axis',(0.99997224619817,0.,0.00745029082566168));
#31339=DIRECTION('ref_axis',(-0.00745029082566168,0.,0.99997224619817));
#31340=DIRECTION('',(0.,-1.,0.));
#31341=DIRECTION('',(-0.00745029082566168,0.,0.99997224619817));
#31342=DIRECTION('center_axis',(0.,-1.,0.));
#31343=DIRECTION('ref_axis',(0.939692620785908,0.,0.342020143325669));
#31344=DIRECTION('',(0.637062515999983,0.,-0.770812137104607));
#31345=DIRECTION('center_axis',(-0.770812137104607,0.,-0.637062515999983));
#31346=DIRECTION('ref_axis',(0.637062515999983,0.,-0.770812137104607));
#31347=DIRECTION('center_axis',(0.986074150277955,0.,-0.166306254102512));
#31348=DIRECTION('ref_axis',(0.166306254102512,0.,0.986074150277955));
#31349=DIRECTION('',(0.,-1.,0.));
#31350=DIRECTION('',(0.166306254102512,0.,0.986074150277955));
#31351=DIRECTION('center_axis',(0.,-1.,0.));
#31352=DIRECTION('ref_axis',(0.984807753012208,0.,0.17364817766693));
#31353=DIRECTION('',(0.49353398197848,0.,-0.869726513699833));
#31354=DIRECTION('center_axis',(-0.869726513699833,0.,-0.49353398197848));
#31355=DIRECTION('ref_axis',(0.49353398197848,0.,-0.869726513699833));
#31356=DIRECTION('center_axis',(0.942214690279141,0.,-0.335009667654806));
#31357=DIRECTION('ref_axis',(0.335009667654806,0.,0.94221469027914));
#31358=DIRECTION('',(0.,-1.,0.));
#31359=DIRECTION('',(0.335009667654806,0.,0.94221469027914));
#31360=DIRECTION('center_axis',(0.,-1.,0.));
#31361=DIRECTION('ref_axis',(1.,0.,-6.12323399573677E-17));
#31362=DIRECTION('',(0.335009667654806,0.,-0.94221469027914));
#31363=DIRECTION('center_axis',(-0.942214690279141,0.,-0.335009667654806));
#31364=DIRECTION('ref_axis',(0.335009667654806,0.,-0.94221469027914));
#31365=DIRECTION('center_axis',(0.869726513699833,0.,-0.49353398197848));
#31366=DIRECTION('ref_axis',(0.49353398197848,0.,0.869726513699833));
#31367=DIRECTION('',(0.,-1.,0.));
#31368=DIRECTION('',(0.49353398197848,0.,0.869726513699833));
#31369=DIRECTION('center_axis',(0.,-1.,0.));
#31370=DIRECTION('ref_axis',(0.984807753012208,0.,-0.17364817766693));
#31371=DIRECTION('',(0.166306254102512,0.,-0.986074150277955));
#31372=DIRECTION('center_axis',(-0.986074150277955,0.,-0.166306254102512));
#31373=DIRECTION('ref_axis',(0.166306254102512,0.,-0.986074150277955));
#31374=DIRECTION('center_axis',(0.770812137104607,0.,-0.637062515999983));
#31375=DIRECTION('ref_axis',(0.637062515999983,0.,0.770812137104607));
#31376=DIRECTION('',(0.,-1.,0.));
#31377=DIRECTION('',(0.637062515999983,0.,0.770812137104607));
#31378=DIRECTION('center_axis',(0.,-1.,0.));
#31379=DIRECTION('ref_axis',(0.939692620785908,0.,-0.342020143325669));
#31380=DIRECTION('',(-0.00745029082566184,0.,-0.99997224619817));
#31381=DIRECTION('center_axis',(-0.99997224619817,0.,0.00745029082566184));
#31382=DIRECTION('ref_axis',(-0.00745029082566184,0.,-0.99997224619817));
#31383=DIRECTION('center_axis',(0.648477023773219,0.,-0.761234227842014));
#31384=DIRECTION('ref_axis',(0.761234227842014,0.,0.648477023773219));
#31385=DIRECTION('',(0.,-1.,0.));
#31386=DIRECTION('',(0.761234227842014,0.,0.64847702377322));
#31387=DIRECTION('center_axis',(0.,-1.,0.));
#31388=DIRECTION('ref_axis',(0.866025403784439,0.,-0.5));
#31389=DIRECTION('',(-0.180980462437127,0.,-0.983486691428025));
#31390=DIRECTION('center_axis',(-0.983486691428025,0.,0.180980462437127));
#31391=DIRECTION('ref_axis',(-0.180980462437127,0.,-0.983486691428025));
#31392=DIRECTION('center_axis',(0.50643826421969,0.,-0.862276222874171));
#31393=DIRECTION('ref_axis',(0.862276222874171,0.,0.50643826421969));
#31394=DIRECTION('',(0.,-1.,0.));
#31395=DIRECTION('',(0.862276222874171,0.,0.50643826421969));
#31396=DIRECTION('center_axis',(0.,-1.,0.));
#31397=DIRECTION('ref_axis',(0.766044443118978,0.,-0.642787609686539));
#31398=DIRECTION('',(-0.349011634277972,0.,-0.937118391207119));
#31399=DIRECTION('center_axis',(-0.937118391207119,0.,0.349011634277972));
#31400=DIRECTION('ref_axis',(-0.349011634277972,0.,-0.937118391207119));
#31401=DIRECTION('center_axis',(0.349011634277972,0.,-0.937118391207119));
#31402=DIRECTION('ref_axis',(0.937118391207119,0.,0.349011634277972));
#31403=DIRECTION('',(0.,-1.,0.));
#31404=DIRECTION('',(0.937118391207119,0.,0.349011634277972));
#31405=DIRECTION('center_axis',(0.,-1.,0.));
#31406=DIRECTION('ref_axis',(0.642787609686539,0.,-0.766044443118978));
#31407=DIRECTION('',(-0.50643826421969,0.,-0.862276222874171));
#31408=DIRECTION('center_axis',(-0.862276222874171,0.,0.50643826421969));
#31409=DIRECTION('ref_axis',(-0.50643826421969,0.,-0.862276222874171));
#31410=DIRECTION('center_axis',(0.180980462437127,0.,-0.983486691428025));
#31411=DIRECTION('ref_axis',(0.983486691428025,0.,0.180980462437127));
#31412=DIRECTION('',(0.,-1.,0.));
#31413=DIRECTION('',(0.983486691428025,0.,0.180980462437127));
#31414=DIRECTION('center_axis',(0.,-1.,0.));
#31415=DIRECTION('ref_axis',(0.5,0.,-0.866025403784439));
#31416=DIRECTION('',(-0.64847702377322,0.,-0.761234227842014));
#31417=DIRECTION('center_axis',(-0.761234227842014,0.,0.64847702377322));
#31418=DIRECTION('ref_axis',(-0.64847702377322,0.,-0.761234227842014));
#31419=DIRECTION('center_axis',(0.00745029082566168,0.,-0.99997224619817));
#31420=DIRECTION('ref_axis',(0.99997224619817,0.,0.00745029082566168));
#31421=DIRECTION('',(0.,-1.,0.));
#31422=DIRECTION('',(0.99997224619817,0.,0.00745029082566168));
#31423=DIRECTION('center_axis',(0.,-1.,0.));
#31424=DIRECTION('ref_axis',(0.342020143325669,0.,-0.939692620785908));
#31425=DIRECTION('',(-0.770812137104607,0.,-0.637062515999983));
#31426=DIRECTION('center_axis',(-0.637062515999983,0.,0.770812137104607));
#31427=DIRECTION('ref_axis',(-0.770812137104607,0.,-0.637062515999983));
#31428=DIRECTION('center_axis',(-0.166306254102512,0.,-0.986074150277955));
#31429=DIRECTION('ref_axis',(0.986074150277955,0.,-0.166306254102512));
#31430=DIRECTION('',(0.,-1.,0.));
#31431=DIRECTION('',(0.986074150277955,0.,-0.166306254102512));
#31432=DIRECTION('center_axis',(0.,-1.,0.));
#31433=DIRECTION('ref_axis',(0.17364817766693,0.,-0.984807753012208));
#31434=DIRECTION('',(-0.869726513699833,0.,-0.49353398197848));
#31435=DIRECTION('center_axis',(-0.49353398197848,0.,0.869726513699833));
#31436=DIRECTION('ref_axis',(-0.869726513699833,0.,-0.49353398197848));
#31437=DIRECTION('center_axis',(-0.335009667654806,0.,-0.942214690279141));
#31438=DIRECTION('ref_axis',(0.94221469027914,0.,-0.335009667654806));
#31439=DIRECTION('',(0.,-1.,0.));
#31440=DIRECTION('',(0.94221469027914,0.,-0.335009667654806));
#31441=DIRECTION('center_axis',(0.,-1.,0.));
#31442=DIRECTION('ref_axis',(0.,0.,-1.));
#31443=DIRECTION('',(-0.94221469027914,0.,-0.335009667654806));
#31444=DIRECTION('center_axis',(-0.335009667654806,0.,0.942214690279141));
#31445=DIRECTION('ref_axis',(-0.94221469027914,0.,-0.335009667654806));
#31446=DIRECTION('center_axis',(0.,1.,0.));
#31447=DIRECTION('ref_axis',(0.,0.,1.));
#31448=DIRECTION('center_axis',(-1.,0.,1.22464679914735E-16));
#31449=DIRECTION('ref_axis',(-1.22464679914735E-16,0.,-1.));
#31450=DIRECTION('center_axis',(0.,-1.,0.));
#31451=DIRECTION('ref_axis',(1.,0.,0.));
#31452=DIRECTION('',(0.707106781186544,0.707106781186551,8.6595605623549E-17));
#31453=DIRECTION('center_axis',(0.,-1.,0.));
#31454=DIRECTION('ref_axis',(1.,0.,0.));
#31455=DIRECTION('center_axis',(0.,1.,0.));
#31456=DIRECTION('ref_axis',(1.,0.,0.));
#31457=DIRECTION('center_axis',(0.,-1.,0.));
#31458=DIRECTION('ref_axis',(1.,0.,0.));
#31459=DIRECTION('center_axis',(0.,1.,0.));
#31460=DIRECTION('ref_axis',(1.,0.,0.));
#31461=DIRECTION('center_axis',(0.,-1.,0.));
#31462=DIRECTION('ref_axis',(1.,0.,0.));
#31463=DIRECTION('center_axis',(0.,-1.,0.));
#31464=DIRECTION('ref_axis',(1.,0.,0.));
#31465=DIRECTION('center_axis',(0.,-1.,0.));
#31466=DIRECTION('ref_axis',(1.,0.,0.));
#31467=DIRECTION('center_axis',(0.,-1.,0.));
#31468=DIRECTION('ref_axis',(1.,0.,0.));
#31469=DIRECTION('center_axis',(0.,-1.,0.));
#31470=DIRECTION('ref_axis',(1.,0.,0.));
#31471=DIRECTION('center_axis',(0.,-1.,0.));
#31472=DIRECTION('ref_axis',(1.,0.,0.));
#31473=DIRECTION('',(-0.707106781186555,0.70710678118654,8.65956056235503E-17));
#31474=DIRECTION('center_axis',(0.,-1.,0.));
#31475=DIRECTION('ref_axis',(1.,0.,0.));
#31476=DIRECTION('',(0.,1.,0.));
#31477=DIRECTION('',(0.,-1.,0.));
#31478=DIRECTION('center_axis',(0.,1.,0.));
#31479=DIRECTION('ref_axis',(1.,0.,0.));
#31480=DIRECTION('center_axis',(0.,-1.,0.));
#31481=DIRECTION('ref_axis',(1.,0.,0.));
#31482=DIRECTION('',(0.,1.,0.));
#31483=DIRECTION('',(0.,-1.,0.));
#31484=DIRECTION('center_axis',(0.,1.,0.));
#31485=DIRECTION('ref_axis',(1.,0.,0.));
#31486=DIRECTION('center_axis',(0.,-1.,0.));
#31487=DIRECTION('ref_axis',(1.,0.,0.));
#31488=DIRECTION('',(0.,-1.,0.));
#31489=DIRECTION('center_axis',(0.,1.,0.));
#31490=DIRECTION('ref_axis',(1.,0.,0.));
#31491=DIRECTION('',(0.,1.,0.));
#31492=DIRECTION('center_axis',(0.,-1.,0.));
#31493=DIRECTION('ref_axis',(1.,0.,0.));
#31494=DIRECTION('',(0.,1.,0.));
#31495=DIRECTION('',(0.,-1.,0.));
#31496=DIRECTION('center_axis',(0.,1.,0.));
#31497=DIRECTION('ref_axis',(1.,0.,0.));
#31498=DIRECTION('center_axis',(0.,-1.,0.));
#31499=DIRECTION('ref_axis',(1.,0.,0.));
#31500=DIRECTION('',(0.,-1.,0.));
#31501=DIRECTION('center_axis',(0.,1.,0.));
#31502=DIRECTION('ref_axis',(1.,0.,0.));
#31503=DIRECTION('',(0.,1.,0.));
#31504=DIRECTION('center_axis',(0.,-1.,0.));
#31505=DIRECTION('ref_axis',(1.,0.,0.));
#31506=DIRECTION('',(0.,-1.,0.));
#31507=DIRECTION('center_axis',(0.,1.,0.));
#31508=DIRECTION('ref_axis',(1.,0.,0.));
#31509=DIRECTION('',(0.,1.,0.));
#31510=DIRECTION('center_axis',(0.866025403784439,0.,0.5));
#31511=DIRECTION('ref_axis',(-0.5,0.,0.866025403784439));
#31512=DIRECTION('',(-0.5,0.,0.866025403784439));
#31513=DIRECTION('',(0.,-1.,0.));
#31514=DIRECTION('',(-0.5,0.,0.866025403784439));
#31515=DIRECTION('',(0.,-1.,0.));
#31516=DIRECTION('center_axis',(0.866025403784439,0.,-0.5));
#31517=DIRECTION('ref_axis',(0.5,0.,0.866025403784439));
#31518=DIRECTION('',(0.5,0.,0.866025403784439));
#31519=DIRECTION('',(0.,-1.,0.));
#31520=DIRECTION('',(0.5,0.,0.866025403784439));
#31521=DIRECTION('center_axis',(-1.92296268638356E-16,0.,-1.));
#31522=DIRECTION('ref_axis',(1.,0.,-1.92296268638356E-16));
#31523=DIRECTION('',(1.,0.,-1.92296268638356E-16));
#31524=DIRECTION('',(0.,-1.,0.));
#31525=DIRECTION('',(1.,0.,-1.92296268638356E-16));
#31526=DIRECTION('center_axis',(0.,1.,0.));
#31527=DIRECTION('ref_axis',(1.,0.,0.));
#31528=DIRECTION('center_axis',(0.,1.,0.));
#31529=DIRECTION('ref_axis',(1.,0.,0.));
#31530=DIRECTION('center_axis',(0.,1.,0.));
#31531=DIRECTION('ref_axis',(1.,0.,0.));
#31532=DIRECTION('',(0.5,0.,-0.866025403784439));
#31533=DIRECTION('center_axis',(0.,1.,0.));
#31534=DIRECTION('ref_axis',(1.,0.,0.));
#31535=DIRECTION('center_axis',(0.,1.,0.));
#31536=DIRECTION('ref_axis',(1.,0.,0.));
#31537=DIRECTION('',(-0.5,0.,-0.866025403784438));
#31538=DIRECTION('center_axis',(0.,1.,0.));
#31539=DIRECTION('ref_axis',(1.,0.,0.));
#31540=DIRECTION('',(-1.,0.,1.92296268638356E-16));
#31541=DIRECTION('center_axis',(0.,1.,0.));
#31542=DIRECTION('ref_axis',(0.,0.,1.));
#31543=DIRECTION('',(0.5,0.,-0.866025403784439));
#31544=DIRECTION('center_axis',(0.,-1.,0.));
#31545=DIRECTION('ref_axis',(1.,0.,0.));
#31546=DIRECTION('center_axis',(0.,1.,0.));
#31547=DIRECTION('ref_axis',(0.,0.,1.));
#31548=DIRECTION('center_axis',(0.,-1.,0.));
#31549=DIRECTION('ref_axis',(1.,0.,0.));
#31550=DIRECTION('center_axis',(0.,1.,0.));
#31551=DIRECTION('ref_axis',(0.,0.,1.));
#31552=DIRECTION('center_axis',(0.,-1.,0.));
#31553=DIRECTION('ref_axis',(1.,0.,0.));
#31554=DIRECTION('center_axis',(0.,1.,0.));
#31555=DIRECTION('ref_axis',(0.,0.,1.));
#31556=DIRECTION('center_axis',(0.,-1.,0.));
#31557=DIRECTION('ref_axis',(1.,0.,0.));
#31558=DIRECTION('center_axis',(0.,1.,0.));
#31559=DIRECTION('ref_axis',(0.,0.,1.));
#31560=DIRECTION('',(-1.,0.,1.92296268638356E-16));
#31561=DIRECTION('center_axis',(0.,-1.,0.));
#31562=DIRECTION('ref_axis',(1.,0.,0.));
#31563=DIRECTION('center_axis',(0.,1.,0.));
#31564=DIRECTION('ref_axis',(0.,0.,1.));
#31565=DIRECTION('',(-0.5,0.,-0.866025403784438));
#31566=DIRECTION('center_axis',(0.,-1.,0.));
#31567=DIRECTION('ref_axis',(1.,0.,0.));
#31568=DIRECTION('center_axis',(0.,1.,0.));
#31569=DIRECTION('ref_axis',(1.,0.,0.));
#31570=DIRECTION('',(-0.85716730070211,0.515038074910058,1.04972719113862E-16));
#31571=DIRECTION('center_axis',(-0.866025403784439,0.,-0.5));
#31572=DIRECTION('ref_axis',(0.5,0.,-0.866025403784439));
#31573=DIRECTION('',(0.,-1.,0.));
#31574=DIRECTION('center_axis',(-0.866025403784438,0.,0.5));
#31575=DIRECTION('ref_axis',(-0.5,0.,-0.866025403784438));
#31576=DIRECTION('',(0.,-1.,0.));
#31577=DIRECTION('center_axis',(1.92296268638356E-16,0.,1.));
#31578=DIRECTION('ref_axis',(-1.,0.,1.92296268638356E-16));
#42113=CARTESIAN_POINT('',(0.,0.,0.));
#42114=CARTESIAN_POINT('Origin',(0.,56.5393671147362,0.));
#42115=CARTESIAN_POINT('',(0.188938462403162,55.3284942881797,1.16249615910107));
#42116=CARTESIAN_POINT('',(0.188938462403162,55.4271602664287,1.16249615910107));
#42117=CARTESIAN_POINT('',(0.188938462403162,56.5393671147362,1.16249615910107));
#42118=CARTESIAN_POINT('',(-0.684640367384077,55.614964185794,-0.958312386358538));
#42119=CARTESIAN_POINT('Ctrl Pts',(-0.684640367384077,55.614964185794,-0.958312386358538));
#42120=CARTESIAN_POINT('Ctrl Pts',(-0.647016272926218,55.6118230807353,
-0.985191903120293));
#42121=CARTESIAN_POINT('Ctrl Pts',(-0.607717364810166,55.6086819756767,
-1.00991601482877));
#42122=CARTESIAN_POINT('Ctrl Pts',(-0.567023115628078,55.605540870618,-1.03226927148076));
#42123=CARTESIAN_POINT('Ctrl Pts',(-0.526385256289338,55.6024041181749,
-1.05459155332265));
#42124=CARTESIAN_POINT('Ctrl Pts',(-0.484356373687067,55.5992673657318,
-1.07454920089206));
#42125=CARTESIAN_POINT('Ctrl Pts',(-0.441245462063377,55.5961306132887,
-1.09196955301349));
#42126=CARTESIAN_POINT('Ctrl Pts',(-0.398174263826859,55.5929967503939,
-1.10937385766195));
#42127=CARTESIAN_POINT('Ctrl Pts',(-0.354023535299063,55.5898628874992,
-1.12424527627553));
#42128=CARTESIAN_POINT('Ctrl Pts',(-0.309124864566901,55.5867290246045,
-1.13645804172723));
#42129=CARTESIAN_POINT('Ctrl Pts',(-0.26424670437289,55.5835965933159,-1.14866522816317));
#42130=CARTESIAN_POINT('Ctrl Pts',(-0.218621829054994,55.5804641620274,
-1.15821601686914));
#42131=CARTESIAN_POINT('Ctrl Pts',(-0.172596925041673,55.5773317307388,
-1.16503449046205));
#42132=CARTESIAN_POINT('Ctrl Pts',(-0.12653809012124,55.5741969901302,-1.17185799083337));
#42133=CARTESIAN_POINT('Ctrl Pts',(-0.0800792025826789,55.5710622495215,
-1.17594506164065));
#42134=CARTESIAN_POINT('Ctrl Pts',(-0.0335749533691129,55.5679275089129,
-1.17727133024051));
#42135=CARTESIAN_POINT('Ctrl Pts',(0.0129453684527582,55.564791684888,-1.17859805721989));
#42136=CARTESIAN_POINT('Ctrl Pts',(0.0595105110444984,55.5616558608632,
-1.17716209426211));
#42137=CARTESIAN_POINT('Ctrl Pts',(0.105766738775078,55.5585200368383,-1.17299124441271));
#42138=CARTESIAN_POINT('Ctrl Pts',(0.152111686939792,55.5553781982359,-1.1688123947841));
#42139=CARTESIAN_POINT('Ctrl Pts',(0.198145970424446,55.5522363596335,-1.16188826620853));
#42140=CARTESIAN_POINT('Ctrl Pts',(0.243523695834775,55.5490945210311,-1.15229825655816));
#42141=CARTESIAN_POINT('Ctrl Pts',(0.278383235246138,55.5466809349469,-1.14493113279117));
#42142=CARTESIAN_POINT('Ctrl Pts',(0.312855447910416,55.5442673488626,-1.13599183356545));
#42143=CARTESIAN_POINT('Ctrl Pts',(0.346790549164388,55.5418537627784,-1.12553604007613));
#42144=CARTESIAN_POINT('Ctrl Pts',(0.393291000554971,55.5385464839361,-1.11120871824907));
#42145=CARTESIAN_POINT('Ctrl Pts',(0.439006879213796,55.5352392050939,-1.09396260540427));
#42146=CARTESIAN_POINT('Ctrl Pts',(0.483548219927332,55.5319319262516,-1.07390697060086));
#42147=CARTESIAN_POINT('Ctrl Pts',(0.526316168415577,55.5287563251382,-1.05464984132655));
#42148=CARTESIAN_POINT('Ctrl Pts',(0.568000781192846,55.5255807240248,-1.03280295445645));
#42149=CARTESIAN_POINT('Ctrl Pts',(0.608272338989886,55.5224051229114,-1.00851367076494));
#42150=CARTESIAN_POINT('Ctrl Pts',(0.648504802011408,55.5192326046044,-0.984247966595691));
#42151=CARTESIAN_POINT('Ctrl Pts',(0.687326451093157,55.5160600862973,-0.957544844920675));
#42152=CARTESIAN_POINT('Ctrl Pts',(0.724431565086706,55.5128875679902,-0.928597851605326));
#42153=CARTESIAN_POINT('Ctrl Pts',(0.761516894341772,55.5097167412948,-0.899666293054378));
#42154=CARTESIAN_POINT('Ctrl Pts',(0.796887063896899,55.5065459145994,-0.868493574724687));
#42155=CARTESIAN_POINT('Ctrl Pts',(0.830267046673704,55.5033750879041,-0.835315325914547));
#42156=CARTESIAN_POINT('Ctrl Pts',(0.863643835958174,55.5002045645645,-0.802140251296675));
#42157=CARTESIAN_POINT('Ctrl Pts',(0.895030423834373,55.4970340412249,-0.766960420664583));
#42158=CARTESIAN_POINT('Ctrl Pts',(0.924188459928365,55.4938635178853,-0.730048459374607));
#42159=CARTESIAN_POINT('Ctrl Pts',(0.95337682602575,55.4906896965875,-0.693098102497646));
#42160=CARTESIAN_POINT('Ctrl Pts',(0.98033167090894,55.4875158752897,-0.65441245809238));
#42161=CARTESIAN_POINT('Ctrl Pts',(1.0048560484622,55.484342053992,-0.614295844336366));
#42162=CARTESIAN_POINT('Ctrl Pts',(1.02939562062652,55.4811662662842,-0.574154375460518));
#42163=CARTESIAN_POINT('Ctrl Pts',(1.05150146772164,55.4779904785765,-0.532580664218136));
#42164=CARTESIAN_POINT('Ctrl Pts',(1.07102278465128,55.4748146908688,-0.489903314193535));
#42165=CARTESIAN_POINT('Ctrl Pts',(1.09057979993358,55.4716330956435,-0.447147920710251));
#42166=CARTESIAN_POINT('Ctrl Pts',(1.10754265868973,55.4684515004183,-0.403285381548701));
#42167=CARTESIAN_POINT('Ctrl Pts',(1.12180949365165,55.4652699051931,-0.358662128545834));
#42168=CARTESIAN_POINT('Ctrl Pts',(1.12598102546066,55.4643396269835,-0.345614573161628));
#42169=CARTESIAN_POINT('Ctrl Pts',(1.12992239508094,55.4634093487738,-0.332502056502935));
#42170=CARTESIAN_POINT('Ctrl Pts',(1.13363188304037,55.4624790705642,-0.319333393578473));
#42171=CARTESIAN_POINT('Ctrl Pts',(1.14681967021722,55.459171791722,-0.272516817827044));
#42172=CARTESIAN_POINT('Ctrl Pts',(1.15713407792882,55.4558645128797,-0.224769515073597));
#42173=CARTESIAN_POINT('Ctrl Pts',(1.16445277277936,55.4525572340374,-0.176478900910198));
#42174=CARTESIAN_POINT('Ctrl Pts',(1.17145972512115,55.4493908299583,-0.130245243282809));
#42175=CARTESIAN_POINT('Ctrl Pts',(1.17572092205889,55.4462244258792,-0.0835142477685342));
#42176=CARTESIAN_POINT('Ctrl Pts',(1.17717990049274,55.4430580218,-0.036640747480296));
#42177=CARTESIAN_POINT('Ctrl Pts',(1.17863739219239,55.439894844363,0.0101849875812261));
#42178=CARTESIAN_POINT('Ctrl Pts',(1.17729829867796,55.4367316669259,0.0571523830733597));
#42179=CARTESIAN_POINT('Ctrl Pts',(1.17315794086361,55.4335684894889,0.103901435450357));
#42180=CARTESIAN_POINT('Ctrl Pts',(1.1690199609782,55.4304071287574,0.150623638475473));
#42181=CARTESIAN_POINT('Ctrl Pts',(1.16208395236843,55.4272457680259,0.197127190023575));
#42182=CARTESIAN_POINT('Ctrl Pts',(1.1523972490899,55.4240844072944,0.243054814373266));
#42183=CARTESIAN_POINT('Ctrl Pts',(1.14271180180873,55.4209234564713,0.288976483655171));
#42184=CARTESIAN_POINT('Ctrl Pts',(1.13027648513076,55.4177625056482,0.33432182682512));
#42185=CARTESIAN_POINT('Ctrl Pts',(1.11518964427477,55.4146015548251,0.378744135007149));
#42186=CARTESIAN_POINT('Ctrl Pts',(1.10008747635315,55.41143739272,0.423211572824966));
#42187=CARTESIAN_POINT('Ctrl Pts',(1.08232859089022,55.4082732306148,0.466753573942334));
#42188=CARTESIAN_POINT('Ctrl Pts',(1.06206046209759,55.4051090685097,0.509040899485549));
#42189=CARTESIAN_POINT('Ctrl Pts',(1.04178013088903,55.4019430014225,0.551353684090131));
#42190=CARTESIAN_POINT('Ctrl Pts',(1.01898782249414,55.3987769343353,0.592409800546224));
#42191=CARTESIAN_POINT('Ctrl Pts',(0.993876485028458,55.3956108672481,0.631905526963863));
#42192=CARTESIAN_POINT('Ctrl Pts',(0.968719019986005,55.3924389843415,0.671473803963676));
#42193=CARTESIAN_POINT('Ctrl Pts',(0.941234358404224,55.3892671014349,0.709475521691732));
#42194=CARTESIAN_POINT('Ctrl Pts',(0.911657005503707,55.3860952185284,0.745638361953041));
#42195=CARTESIAN_POINT('Ctrl Pts',(0.902360620356654,55.3850982718023,0.757004615458256));
#42196=CARTESIAN_POINT('Ctrl Pts',(0.892857777331687,55.3841013250762,0.768189478144198));
#42197=CARTESIAN_POINT('Ctrl Pts',(0.883156488284739,55.3831043783501,0.779185266609019));
#42198=CARTESIAN_POINT('Ctrl Pts',(0.852248865205178,55.3799281763535,0.814217073587308));
#42199=CARTESIAN_POINT('Ctrl Pts',(0.819184199229053,55.3767519743569,0.847485712092019));
#42200=CARTESIAN_POINT('Ctrl Pts',(0.784191415269272,55.3735757723602,0.878714337380457));
#42201=CARTESIAN_POINT('Ctrl Pts',(0.74925332271959,55.3704045345576,0.909894154390182));
#42202=CARTESIAN_POINT('Ctrl Pts',(0.712393490439458,55.3672332967549,0.939039901289795));
#42203=CARTESIAN_POINT('Ctrl Pts',(0.673879087458413,55.3640620589522,0.965909953352908));
#42204=CARTESIAN_POINT('Ctrl Pts',(0.635404732883913,55.3608941186957,0.992752065147301));
#42205=CARTESIAN_POINT('Ctrl Pts',(0.595279668954922,55.3577261784391,1.01732284814064));
#42206=CARTESIAN_POINT('Ctrl Pts',(0.553803662632633,55.3545582381826,1.03942126481744));
#42207=CARTESIAN_POINT('Ctrl Pts',(0.512354162410747,55.3513923224638,1.06150555904361));
#42208=CARTESIAN_POINT('Ctrl Pts',(0.469555923238035,55.3482264067451,1.08112035744595));
#42209=CARTESIAN_POINT('Ctrl Pts',(0.425734792304054,55.3450604910264,1.09810971634069));
#42210=CARTESIAN_POINT('Ctrl Pts',(0.381901834291521,55.3418937208446,1.11510366056852));
#42211=CARTESIAN_POINT('Ctrl Pts',(0.337045950356933,55.3387269506629,1.12947053881549));
#42212=CARTESIAN_POINT('Ctrl Pts',(0.291512454949672,55.3355601804812,1.14110277850385));
#42213=CARTESIAN_POINT('Ctrl Pts',(0.25764674359953,55.3332048830474,1.1497543012591));
#42214=CARTESIAN_POINT('Ctrl Pts',(0.223406641651077,55.3308495856135,1.15689410636484));
#42215=CARTESIAN_POINT('Ctrl Pts',(0.188938462403162,55.3284942881797,1.16249615910107));
#42216=CARTESIAN_POINT('',(0.68466442453933,55.615,-0.95829519891849));
#42217=CARTESIAN_POINT('Origin',(0.,55.615,0.));
#42218=CARTESIAN_POINT('Ctrl Pts',(0.684664424539327,55.615,-0.958295198918492));
#42219=CARTESIAN_POINT('Ctrl Pts',(0.724491644158765,55.6116927211578,-0.929840208814693));
#42220=CARTESIAN_POINT('Ctrl Pts',(0.762577693494652,55.6083854423155,-0.898873238001395));
#42221=CARTESIAN_POINT('Ctrl Pts',(0.798605536024659,55.6050781634733,-0.865635177387546));
#42222=CARTESIAN_POINT('Ctrl Pts',(0.833972646537794,55.6018315384161,-0.83300668563167));
#42223=CARTESIAN_POINT('Ctrl Pts',(0.867356039942348,55.598584913359,-0.798190103847066));
#42224=CARTESIAN_POINT('Ctrl Pts',(0.898489640855875,55.5953382883019,-0.761453496790632));
#42225=CARTESIAN_POINT('Ctrl Pts',(0.929615873800169,55.5920924315797,-0.724725583691292));
#42226=CARTESIAN_POINT('Ctrl Pts',(0.958493033710041,55.5888465748576,-0.68607894503007));
#42227=CARTESIAN_POINT('Ctrl Pts',(0.984894406991033,55.5856007181354,-0.645815817069992));
#42228=CARTESIAN_POINT('Ctrl Pts',(1.01129880611503,55.5823544894078,-0.605548074580864));
#42229=CARTESIAN_POINT('Ctrl Pts',(1.03522657059234,55.5791082606803,-0.563663912248202));
#42230=CARTESIAN_POINT('Ctrl Pts',(1.05649480049989,55.5758620319527,-0.520493803053117));
#42231=CARTESIAN_POINT('Ctrl Pts',(1.07846295627206,55.5725089716055,-0.475902989072758));
#42232=CARTESIAN_POINT('Ctrl Pts',(1.0975931380115,55.5691559112582,-0.429940607285958));
#42233=CARTESIAN_POINT('Ctrl Pts',(1.11373706389611,55.565802850911,-0.382994536519876));
#42234=CARTESIAN_POINT('Ctrl Pts',(1.12939933028093,55.5625498302555,-0.337449117684684));
#42235=CARTESIAN_POINT('Ctrl Pts',(1.1422510072811,55.5592968096001,-0.290978437028156));
#42236=CARTESIAN_POINT('Ctrl Pts',(1.15220793960971,55.5560437889446,-0.243950663865372));
#42237=CARTESIAN_POINT('Ctrl Pts',(1.16262417817091,55.5526407087515,-0.194753532851553));
#42238=CARTESIAN_POINT('Ctrl Pts',(1.16987195765063,55.5492376285584,-0.14494728700097));
#42239=CARTESIAN_POINT('Ctrl Pts',(1.17391550254619,55.5458345483652,-0.0949602831805714));
#42240=CARTESIAN_POINT('Ctrl Pts',(1.17795904744174,55.5424314681721,-0.044973279360173));
#42241=CARTESIAN_POINT('Ctrl Pts',(1.17879841864133,55.539028387979,0.00519383608882129));
#42242=CARTESIAN_POINT('Ctrl Pts',(1.17645967332693,55.5356253077858,0.0551153294056635));
#42243=CARTESIAN_POINT('Ctrl Pts',(1.1741867668843,55.5323180289436,0.103631464568754));
#42244=CARTESIAN_POINT('Ctrl Pts',(1.16890102684614,55.5290107501013,0.152144359487931));
#42245=CARTESIAN_POINT('Ctrl Pts',(1.16060215900468,55.5257034712591,0.200244078598303));
#42246=CARTESIAN_POINT('Ctrl Pts',(1.15272296429482,55.5225634412627,0.245911398478554));
#42247=CARTESIAN_POINT('Ctrl Pts',(1.14212813743633,55.5194234112664,0.291205668470788));
#42248=CARTESIAN_POINT('Ctrl Pts',(1.12887062961706,55.51628338127,0.335776955862037));
#42249=CARTESIAN_POINT('Ctrl Pts',(1.1156282331403,55.5131469303829,0.38029743943716));
#42250=CARTESIAN_POINT('Ctrl Pts',(1.09972931778738,55.5100104794958,0.424096026327618));
#42251=CARTESIAN_POINT('Ctrl Pts',(1.08127775043472,55.5068740286087,0.466833470216989));
#42252=CARTESIAN_POINT('Ctrl Pts',(1.06283867095998,55.5037397004473,0.50954198973522));
#42253=CARTESIAN_POINT('Ctrl Pts',(1.04185058337518,55.5006053722858,0.551190264866365));
#42254=CARTESIAN_POINT('Ctrl Pts',(1.0184660634825,55.4974710441244,0.591457471027685));
#42255=CARTESIAN_POINT('Ctrl Pts',(0.995086543685758,55.4943373861474,0.631716067224168));
#42256=CARTESIAN_POINT('Ctrl Pts',(0.969311894910547,55.4912037281704,0.670593687699813));
#42257=CARTESIAN_POINT('Ctrl Pts',(0.941339996565052,55.4880700701934,0.707795219937878));
#42258=CARTESIAN_POINT('Ctrl Pts',(0.913341175156714,55.4849333960583,0.745032558797928));
#42259=CARTESIAN_POINT('Ctrl Pts',(0.883141227727676,55.4817967219231,0.780590133779324));
#42260=CARTESIAN_POINT('Ctrl Pts',(0.850979345249718,55.4786600477879,0.814204652687739));
#42261=CARTESIAN_POINT('Ctrl Pts',(0.818799488802416,55.475521620693,0.847837957384976));
#42262=CARTESIAN_POINT('Ctrl Pts',(0.784655935250263,55.4723831935981,0.879525658594153));
#42263=CARTESIAN_POINT('Ctrl Pts',(0.748823119591442,55.4692447665031,0.909042902213829));
#42264=CARTESIAN_POINT('Ctrl Pts',(0.712923282008741,55.4661004692744,0.938615355071704));
#42265=CARTESIAN_POINT('Ctrl Pts',(0.675328343043641,55.4629561720457,0.96600892074501));
#42266=CARTESIAN_POINT('Ctrl Pts',(0.636342349023049,55.459811874817,0.991041612314956));
#42267=CARTESIAN_POINT('Ctrl Pts',(0.621623720179923,55.4586247884019,1.00049236265283));
#42268=CARTESIAN_POINT('Ctrl Pts',(0.60670706636262,55.4574377019868,1.00960708054128));
#42269=CARTESIAN_POINT('Ctrl Pts',(0.591609558792355,55.4562506155717,1.01837772581961));
#42270=CARTESIAN_POINT('Ctrl Pts',(0.551182570661861,55.4530719234471,1.0418631104709));
#42271=CARTESIAN_POINT('Ctrl Pts',(0.509264752294662,55.4498932313226,1.06298989543228));
#42272=CARTESIAN_POINT('Ctrl Pts',(0.466161294741415,55.446714539198,1.08156770929286));
#42273=CARTESIAN_POINT('Ctrl Pts',(0.421968236020381,55.4434554937365,1.10061514691047));
#42274=CARTESIAN_POINT('Ctrl Pts',(0.376529229329588,55.4401964482749,1.11698257955201));
#42275=CARTESIAN_POINT('Ctrl Pts',(0.330202278749991,55.4369374028134,1.13051382902126));
#42276=CARTESIAN_POINT('Ctrl Pts',(0.283875328170395,55.4336783573518,1.14404507849051));
#42277=CARTESIAN_POINT('Ctrl Pts',(0.236661020821678,55.4304193118903,1.15473989535864));
#42278=CARTESIAN_POINT('Ctrl Pts',(0.188938462403162,55.4271602664287,1.16249615910107));
#42279=CARTESIAN_POINT('Origin',(0.,56.5393671147362,0.));
#42280=CARTESIAN_POINT('',(0.189250941525368,54.8284605668479,1.16440479426641));
#42281=CARTESIAN_POINT('',(0.188938369713633,54.9278857931129,1.16249617416573));
#42282=CARTESIAN_POINT('',(0.188938462403162,56.5393671147362,1.16249615910107));
#42283=CARTESIAN_POINT('',(-1.17764273048215,55.1906328852639,0.000476299562157373));
#42284=CARTESIAN_POINT('Ctrl Pts',(-1.17600680867674,55.1906328852639,0.000475637910860929));
#42285=CARTESIAN_POINT('Ctrl Pts',(-1.17519815942166,55.1754153574118,-0.225531174543087));
#42286=CARTESIAN_POINT('Ctrl Pts',(-1.00351486996816,55.1337395988216,-0.845634366230089));
#42287=CARTESIAN_POINT('Ctrl Pts',(0.000480427458435629,55.0656056094933,
-1.39199102275273));
#42288=CARTESIAN_POINT('Ctrl Pts',(1.16966281939467,54.9862309172792,-0.7546848720392));
#42289=CARTESIAN_POINT('Ctrl Pts',(1.26807427992724,54.9071825697306,0.567794313718899));
#42290=CARTESIAN_POINT('Ctrl Pts',(0.5691936499357,54.8545924529201,1.10219607268075));
#42291=CARTESIAN_POINT('Ctrl Pts',(0.189250941523835,54.8284605668477,1.16440479426666));
#42292=CARTESIAN_POINT('Ctrl Pts',(0.188938462403162,55.3284942881797,1.16249615910107));
#42293=CARTESIAN_POINT('Ctrl Pts',(0.142549417821131,55.3253244080164,1.17003568917784));
#42294=CARTESIAN_POINT('Ctrl Pts',(0.095747458468686,55.3221545278532,1.1747878985975));
#42295=CARTESIAN_POINT('Ctrl Pts',(0.0488931096339062,55.3189846476899,
1.17673468816481));
#42296=CARTESIAN_POINT('Ctrl Pts',(0.00194900551908925,55.3158086952305,
1.17868520704747));
#42297=CARTESIAN_POINT('Ctrl Pts',(-0.0450471295304053,55.312632742771,
1.17781958621838));
#42298=CARTESIAN_POINT('Ctrl Pts',(-0.091736027286698,55.3094567903116,
1.17417186297307));
#42299=CARTESIAN_POINT('Ctrl Pts',(-0.119800278322794,55.3075477555864,
1.17197925132906));
#42300=CARTESIAN_POINT('Ctrl Pts',(-0.147753625345882,55.3056387208611,
1.16878244602835));
#42301=CARTESIAN_POINT('Ctrl Pts',(-0.175519889908964,55.3037296861359,
1.16459771197884));
#42302=CARTESIAN_POINT('Ctrl Pts',(-0.223623142355883,55.3004224072937,
1.15734793165822));
#42303=CARTESIAN_POINT('Ctrl Pts',(-0.271388793313158,55.2971151284514,
1.14709587817919));
#42304=CARTESIAN_POINT('Ctrl Pts',(-0.318414151538062,55.2938078496091,
1.1338904226601));
#42305=CARTESIAN_POINT('Ctrl Pts',(-0.363498247483417,55.2906370991402,
1.12123010392787));
#42306=CARTESIAN_POINT('Ctrl Pts',(-0.407901374096596,55.2874663486713,
1.10585562577166));
#42307=CARTESIAN_POINT('Ctrl Pts',(-0.451276259215418,55.2842955982024,
1.08786249147975));
#42308=CARTESIAN_POINT('Ctrl Pts',(-0.49460777251013,55.2811280182602,1.06988734905235));
#42309=CARTESIAN_POINT('Ctrl Pts',(-0.536912565939944,55.277960438318,1.04929894564495));
#42310=CARTESIAN_POINT('Ctrl Pts',(-0.577860079704023,55.2747928583758,
1.02624207221516));
#42311=CARTESIAN_POINT('Ctrl Pts',(-0.618784722772805,55.2716270476437,
1.00319807689879));
#42312=CARTESIAN_POINT('Ctrl Pts',(-0.658353102238453,55.2684612369116,
0.977688615881606));
#42313=CARTESIAN_POINT('Ctrl Pts',(-0.696258635227587,55.2652954261795,
0.949904719101352));
#42314=CARTESIAN_POINT('Ctrl Pts',(-0.734159726669883,55.2621299863984,
0.922124077874288));
#42315=CARTESIAN_POINT('Ctrl Pts',(-0.770397909701557,55.2589645466174,
0.892069861365488));
#42316=CARTESIAN_POINT('Ctrl Pts',(-0.804697283430426,55.2557991068363,
0.859975199956192));
#42317=CARTESIAN_POINT('Ctrl Pts',(-0.839031720245098,55.2526304311336,
0.82784772926368));
#42318=CARTESIAN_POINT('Ctrl Pts',(-0.871422985776287,55.2494617554309,
0.79367603466084));
#42319=CARTESIAN_POINT('Ctrl Pts',(-0.901631355149056,55.2462930797282,
0.757730797785122));
#42320=CARTESIAN_POINT('Ctrl Pts',(-0.931858072785087,55.2431224794033,
0.72176372812985));
#42321=CARTESIAN_POINT('Ctrl Pts',(-0.959898923042567,55.2399518790785,
0.684021420872171));
#42322=CARTESIAN_POINT('Ctrl Pts',(-0.985556165895788,55.2367812787536,
0.644805479477954));
#42323=CARTESIAN_POINT('Ctrl Pts',(-1.01126033365124,55.233604879672,0.605517815481799));
#42324=CARTESIAN_POINT('Ctrl Pts',(-1.03457192321865,55.2304284805904,0.564751626343542));
#42325=CARTESIAN_POINT('Ctrl Pts',(-1.05533892193599,55.2272520815088,0.522833455650063));
#42326=CARTESIAN_POINT('Ctrl Pts',(-1.06165255074023,55.2262863856465,0.510089400839168));
#42327=CARTESIAN_POINT('Ctrl Pts',(-1.06773132417528,55.2253206897841,0.497239002137502));
#42328=CARTESIAN_POINT('Ctrl Pts',(-1.07357187213201,55.2243549939217,0.48429174870833));
#42329=CARTESIAN_POINT('Ctrl Pts',(-1.09455578960903,55.2208854423601,0.43777486373032));
#42330=CARTESIAN_POINT('Ctrl Pts',(-1.11254274872739,55.2174158907984,0.389825311477729));
#42331=CARTESIAN_POINT('Ctrl Pts',(-1.12735565804714,55.2139463392368,0.34082881739827));
#42332=CARTESIAN_POINT('Ctrl Pts',(-1.14212128857713,55.2104878615429,0.291988706841628));
#42333=CARTESIAN_POINT('Ctrl Pts',(-1.15373290134083,55.2070293838491,0.242108664695996));
#42334=CARTESIAN_POINT('Ctrl Pts',(-1.16206153173208,55.2035709061552,0.191593473188655));
#42335=CARTESIAN_POINT('Ctrl Pts',(-1.17035053482328,55.2001288837639,0.141318631001286));
#42336=CARTESIAN_POINT('Ctrl Pts',(-1.17538757117384,55.1966868613726,0.090415031031693));
#42337=CARTESIAN_POINT('Ctrl Pts',(-1.17709415451836,55.1932448389814,0.0392990317781458));
#42338=CARTESIAN_POINT('Ctrl Pts',(-1.1775258306479,55.1923741877422,0.0263693633936804));
#42339=CARTESIAN_POINT('Ctrl Pts',(-1.1777446660894,55.1915035365031,0.0134261765406657));
#42340=CARTESIAN_POINT('Ctrl Pts',(-1.17774990367116,55.1906328852639,0.000476342908532011));
#42341=CARTESIAN_POINT('',(-1.17774976291499,55.2893671147362,0.000747297585740462));
#42342=CARTESIAN_POINT('Ctrl Pts',(0.188938462403162,55.4271602664287,1.16249615910107));
#42343=CARTESIAN_POINT('Ctrl Pts',(0.142543930805798,55.4239919139209,1.17003658097282));
#42344=CARTESIAN_POINT('Ctrl Pts',(0.0956696598006374,55.4208235614131,
1.17479983966314));
#42345=CARTESIAN_POINT('Ctrl Pts',(0.0486749169602797,55.4176552089053,
1.17674373376658));
#42346=CARTESIAN_POINT('Ctrl Pts',(0.00168609975638459,55.4144872558998,
1.17868738276154));
#42347=CARTESIAN_POINT('Ctrl Pts',(-0.0454226027776017,55.4113193028942,
1.17781235185769));
#42348=CARTESIAN_POINT('Ctrl Pts',(-0.0922896021824091,55.4081513498887,
1.17412848182344));
#42349=CARTESIAN_POINT('Ctrl Pts',(-0.139203317783593,55.4049802391236,
1.17044093977267));
#42350=CARTESIAN_POINT('Ctrl Pts',(-0.185874293392765,55.4018091283585,
1.16393901702968));
#42351=CARTESIAN_POINT('Ctrl Pts',(-0.231945751086216,55.3986380175934,
1.15468447250885));
#42352=CARTESIAN_POINT('Ctrl Pts',(-0.278044691572742,55.3954650151803,
1.14542440741748));
#42353=CARTESIAN_POINT('Ctrl Pts',(-0.32354286360166,55.3922920127672,1.13340859486404));
#42354=CARTESIAN_POINT('Ctrl Pts',(-0.368096945434806,55.3891190103542,
1.11874916816128));
#42355=CARTESIAN_POINT('Ctrl Pts',(-0.412730857375361,55.3859403226904,
1.10406347532173));
#42356=CARTESIAN_POINT('Ctrl Pts',(-0.456416788340362,55.3827616350266,
1.08672492693345));
#42357=CARTESIAN_POINT('Ctrl Pts',(-0.498831540903763,55.3795829473629,
1.06689369493852));
#42358=CARTESIAN_POINT('Ctrl Pts',(-0.510871913694729,55.3786806060277,
1.06126415776826));
#42359=CARTESIAN_POINT('Ctrl Pts',(-0.522810011508585,55.3777782646926,
1.05543403075502));
#42360=CARTESIAN_POINT('Ctrl Pts',(-0.534638847254805,55.3768759233575,
1.04940762599957));
#42361=CARTESIAN_POINT('Ctrl Pts',(-0.577994123876299,55.3735686445152,
1.02731953121062));
#42362=CARTESIAN_POINT('Ctrl Pts',(-0.620075992746351,55.3702613656729,
1.0024903915763));
#42363=CARTESIAN_POINT('Ctrl Pts',(-0.660518998568138,55.3669540868307,
0.975094721055623));
#42364=CARTESIAN_POINT('Ctrl Pts',(-0.699351774441889,55.3637784866144,
0.948789803514913));
#42365=CARTESIAN_POINT('Ctrl Pts',(-0.736673220398442,55.3606028863982,
0.920119228874442));
#42366=CARTESIAN_POINT('Ctrl Pts',(-0.772183766357654,55.357427286182,0.889284708894574));
#42367=CARTESIAN_POINT('Ctrl Pts',(-0.807659839148315,55.3542547687964,
0.858480122659056));
#42368=CARTESIAN_POINT('Ctrl Pts',(-0.841328073571308,55.3510822514109,
0.825516112446977));
#42369=CARTESIAN_POINT('Ctrl Pts',(-0.872920461126642,55.3479097340253,
0.790635776477672));
#42370=CARTESIAN_POINT('Ctrl Pts',(-0.904496003142526,55.3447389082741,
0.755774039231701));
#42371=CARTESIAN_POINT('Ctrl Pts',(-0.933997518313652,55.3415680825229,
0.718998412134455));
#42372=CARTESIAN_POINT('Ctrl Pts',(-0.961194453248968,55.3383972567717,
0.680588190863916));
#42373=CARTESIAN_POINT('Ctrl Pts',(-0.988388786049864,55.3352267343971,
0.642181644586867));
#42374=CARTESIAN_POINT('Ctrl Pts',(-1.0132786570209,55.3320562120225,0.602141269663834));
#42375=CARTESIAN_POINT('Ctrl Pts',(-1.03567598964635,55.3288856896479,0.560776521414766));
#42376=CARTESIAN_POINT('Ctrl Pts',(-1.05809661967185,55.3257118693392,0.519368746118527));
#42377=CARTESIAN_POINT('Ctrl Pts',(-1.07801927427464,55.3225380490305,0.476634339451388));
#42378=CARTESIAN_POINT('Ctrl Pts',(-1.09530210207445,55.3193642287217,0.432906881085622));
#42379=CARTESIAN_POINT('Ctrl Pts',(-1.11259563774696,55.3161884420181,0.38915233062226));
#42380=CARTESIAN_POINT('Ctrl Pts',(-1.12724591887537,55.3130126553145,0.344404032875954));
#42381=CARTESIAN_POINT('Ctrl Pts',(-1.13916071576251,55.3098368686109,0.299011581988799));
#42382=CARTESIAN_POINT('Ctrl Pts',(-1.15109730102877,55.3066552744022,0.253536122726543));
#42383=CARTESIAN_POINT('Ctrl Pts',(-1.16028831698053,55.3034736801934,0.2074147058952));
#42384=CARTESIAN_POINT('Ctrl Pts',(-1.16669280385812,55.3002920859846,0.161006099032543));
#42385=CARTESIAN_POINT('Ctrl Pts',(-1.16856544925066,55.2993618010375,0.147436414922553));
#42386=CARTESIAN_POINT('Ctrl Pts',(-1.17020019917895,55.2984315160904,0.133842194630304));
#42387=CARTESIAN_POINT('Ctrl Pts',(-1.17159687104713,55.2975012311433,0.120232417644254));
#42388=CARTESIAN_POINT('Ctrl Pts',(-1.17566755626888,55.2947898590076,0.0805658937377747));
#42389=CARTESIAN_POINT('Ctrl Pts',(-1.17772442049394,55.2920784868719,0.0406872504911861));
#42390=CARTESIAN_POINT('Ctrl Pts',(-1.17774976291499,55.2893671147362,0.000747297585740462));
#42391=CARTESIAN_POINT('Ctrl Pts',(-1.17774972874626,55.2885481328136,0.000799336045316526));
#42392=CARTESIAN_POINT('Ctrl Pts',(-1.17778530487014,55.2852174150181,-0.051618880917269));
#42393=CARTESIAN_POINT('Ctrl Pts',(-1.17432137139241,55.2819926037606,-0.10398580942958));
#42394=CARTESIAN_POINT('Ctrl Pts',(-1.1587786970635,55.2747462179935,-0.220330615351294));
#42395=CARTESIAN_POINT('Ctrl Pts',(-1.14486848757003,55.2707271841678,-0.283881467269182));
#42396=CARTESIAN_POINT('Ctrl Pts',(-1.11931942068765,55.265134021753,-0.367021293189932));
#42397=CARTESIAN_POINT('Ctrl Pts',(-1.11225733971495,55.2637009571437,-0.38789702920972));
#42398=CARTESIAN_POINT('Ctrl Pts',(-1.10054657903341,55.2614760122246,-0.41955903527872));
#42399=CARTESIAN_POINT('Ctrl Pts',(-1.09631501846142,55.2606979448457,-0.430494971257066));
#42400=CARTESIAN_POINT('Ctrl Pts',(-1.08819702403083,55.2592502692773,-0.450578568722361));
#42401=CARTESIAN_POINT('Ctrl Pts',(-1.08435669222204,55.2585822762506,-0.45974380169608));
#42402=CARTESIAN_POINT('Ctrl Pts',(-1.07557087268419,55.2570897808557,-0.479989132667856));
#42403=CARTESIAN_POINT('Ctrl Pts',(-1.0705692668619,55.2562634068242,-0.491043475727912));
#42404=CARTESIAN_POINT('Ctrl Pts',(-1.05541525070416,55.2538245170324,-0.523203777585702));
#42405=CARTESIAN_POINT('Ctrl Pts',(-1.04480354524958,55.2521963460117,-0.544085434046534));
#42406=CARTESIAN_POINT('Ctrl Pts',(-0.98770991405417,55.2438129378895,-0.648596489679292));
#42407=CARTESIAN_POINT('Ctrl Pts',(-0.931787961229544,55.2367288952388,
-0.726645559822832));
#42408=CARTESIAN_POINT('Ctrl Pts',(-0.847041755646844,55.2275602474045,
-0.818834730872675));
#42409=CARTESIAN_POINT('Ctrl Pts',(-0.826208375415139,55.2254089250753,
-0.839851167168879));
#42410=CARTESIAN_POINT('Ctrl Pts',(-0.790816708665306,55.221944009966,-0.872960755202389));
#42411=CARTESIAN_POINT('Ctrl Pts',(-0.776719694477919,55.2206094571155,
-0.885527052501541));
#42412=CARTESIAN_POINT('Ctrl Pts',(-0.756441480146934,55.2187597522089,
-0.902746331614095));
#42413=CARTESIAN_POINT('Ctrl Pts',(-0.75050809089568,55.2182266690644,-0.90768511383862));
#42414=CARTESIAN_POINT('Ctrl Pts',(-0.740134558982428,55.2173092992901,
-0.916148472535086));
#42415=CARTESIAN_POINT('Ctrl Pts',(-0.735716919748619,55.2169231761976,
-0.919699846616618));
#42416=CARTESIAN_POINT('Ctrl Pts',(-0.725993337747847,55.2160832438266,
-0.927401805320577));
#42417=CARTESIAN_POINT('Ctrl Pts',(-0.720677221317361,55.21563034924,-0.931538932736155));
#42418=CARTESIAN_POINT('Ctrl Pts',(-0.705256120349612,55.2143337065174,
-0.943328963369739));
#42419=CARTESIAN_POINT('Ctrl Pts',(-0.695062371261651,55.2134974906239,
-0.950864901207265));
#42420=CARTESIAN_POINT('Ctrl Pts',(-0.636008765151356,55.2087587667034,
-0.993064213690707));
#42421=CARTESIAN_POINT('Ctrl Pts',(-0.584676757987412,55.205043857207,-1.02412814811633));
#42422=CARTESIAN_POINT('Ctrl Pts',(-0.479610441148176,55.1977680151588,
-1.07722320166086));
#42423=CARTESIAN_POINT('Ctrl Pts',(-0.426176031116877,55.1942151416033,
-1.09945875934819));
#42424=CARTESIAN_POINT('Ctrl Pts',(-0.338318494431742,55.1883644377274,
-1.12864762459242));
#42425=CARTESIAN_POINT('Ctrl Pts',(-0.304843402711826,55.1861342775744,
-1.13814542969933));
#42426=CARTESIAN_POINT('Ctrl Pts',(-0.257511752177355,55.1829498565127,
-1.1493366977338));
#42427=CARTESIAN_POINT('Ctrl Pts',(-0.243969430545393,55.1820353480674,
-1.15228730680109));
#42428=CARTESIAN_POINT('Ctrl Pts',(-0.220380934470313,55.1804349118546,
-1.1569923237817));
#42429=CARTESIAN_POINT('Ctrl Pts',(-0.210358025114565,55.1797525465398,
-1.15885654144547));
#42430=CARTESIAN_POINT('Ctrl Pts',(-0.189567257571492,55.1783316803772,
-1.16244493020561));
#42431=CARTESIAN_POINT('Ctrl Pts',(-0.178797164414031,55.1775926492275,
-1.16415012818113));
#42432=CARTESIAN_POINT('Ctrl Pts',(-0.150570151604026,55.1756472309721,
-1.16821829680702));
#42433=CARTESIAN_POINT('Ctrl Pts',(-0.133081741600732,55.1744334106545,
-1.17033950247483));
#42434=CARTESIAN_POINT('Ctrl Pts',(-0.0228882669816492,55.1667278577028,
-1.18120338186185));
#42435=CARTESIAN_POINT('Ctrl Pts',(0.0705179241507803,55.1599034126684,
-1.17931602784043));
#42436=CARTESIAN_POINT('Ctrl Pts',(0.199696341161701,55.1503301409976,-1.16129726466999));
#42437=CARTESIAN_POINT('Ctrl Pts',(0.236422329441821,55.1475981298246,-1.15438067831659));
#42438=CARTESIAN_POINT('Ctrl Pts',(0.287477912709399,55.1438308716834,-1.14222608477471));
#42439=CARTESIAN_POINT('Ctrl Pts',(0.302128398210021,55.142753585537,-1.13843860365688));
#42440=CARTESIAN_POINT('Ctrl Pts',(0.327959306863097,55.1408653242706,-1.13122692153458));
#42441=CARTESIAN_POINT('Ctrl Pts',(0.339169243463613,55.1400496455071,-1.12791662154292));
#42442=CARTESIAN_POINT('Ctrl Pts',(0.356505868577216,55.138795983177,-1.12251525216569));
#42443=CARTESIAN_POINT('Ctrl Pts',(0.362667397416046,55.1383519749648,-1.12053973135057));
#42444=CARTESIAN_POINT('Ctrl Pts',(0.374304986737848,55.1375167075187,-1.11670241630598));
#42445=CARTESIAN_POINT('Ctrl Pts',(0.379783834396527,55.1371249413078,-1.11485099909677));
#42446=CARTESIAN_POINT('Ctrl Pts',(0.391892151841738,55.1362620378887,-1.11065972328108));
#42447=CARTESIAN_POINT('Ctrl Pts',(0.398514642205714,55.1357920035062,-1.1083007559317));
#42448=CARTESIAN_POINT('Ctrl Pts',(0.421970704264982,55.1341326984923,-1.09970814217985));
#42449=CARTESIAN_POINT('Ctrl Pts',(0.438683322208201,55.1329605474249,-1.09314879974131));
#42450=CARTESIAN_POINT('Ctrl Pts',(0.529358251229775,55.1266226838263,-1.05514609639314));
#42451=CARTESIAN_POINT('Ctrl Pts',(0.600109195413689,55.1217457685267,-1.01657514608013));
#42452=CARTESIAN_POINT('Ctrl Pts',(0.705275321940152,55.1138337369647,-0.944407956330997));
#42453=CARTESIAN_POINT('Ctrl Pts',(0.742523673309843,55.110880311461,-0.915411205695369));
#42454=CARTESIAN_POINT('Ctrl Pts',(0.794690351953948,55.1064125720665,-0.869517425825553));
#42455=CARTESIAN_POINT('Ctrl Pts',(0.81102593353514,55.1049609202146,-0.854300966380128));
#42456=CARTESIAN_POINT('Ctrl Pts',(0.835342213669571,55.1027101026158,-0.83032427253948));
#42457=CARTESIAN_POINT('Ctrl Pts',(0.843640010916647,55.1019250696309,-0.821892040613529));
#42458=CARTESIAN_POINT('Ctrl Pts',(0.858719244636236,55.1004656984753,-0.806099525332553));
#42459=CARTESIAN_POINT('Ctrl Pts',(0.865536652797595,55.09979301014,-0.798774985727742));
#42460=CARTESIAN_POINT('Ctrl Pts',(0.880455702471621,55.0982913370803,-0.7823308773912));
#42461=CARTESIAN_POINT('Ctrl Pts',(0.888510557994411,55.0974604866322,-0.773170624405136));
#42462=CARTESIAN_POINT('Ctrl Pts',(0.912175700863119,55.0949573044256,-0.745399585917283));
#42463=CARTESIAN_POINT('Ctrl Pts',(0.927353181809483,55.0932678729912,-0.726430297473123));
#42464=CARTESIAN_POINT('Ctrl Pts',(0.994336376675785,55.0854069795649,-0.637189755074405));
#42465=CARTESIAN_POINT('Ctrl Pts',(1.03880891099775,55.078974589261,-0.561771538500964));
#42466=CARTESIAN_POINT('Ctrl Pts',(1.08845369282136,55.0700790176018,-0.451131278540514));
#42467=CARTESIAN_POINT('Ctrl Pts',(1.10102277128972,55.0675976218426,-0.419523533730215));
#42468=CARTESIAN_POINT('Ctrl Pts',(1.11901939451923,55.0636764178484,-0.367858019628456));
#42469=CARTESIAN_POINT('Ctrl Pts',(1.12531504105737,55.0622094017894,-0.348123699700449));
#42470=CARTESIAN_POINT('Ctrl Pts',(1.13332276159006,55.0602095675463,-0.320529118524553));
#42471=CARTESIAN_POINT('Ctrl Pts',(1.13547947811581,55.0596551756115,-0.312803071691913));
#42472=CARTESIAN_POINT('Ctrl Pts',(1.13903960171143,55.0587127053363,-0.299527302380195));
#42473=CARTESIAN_POINT('Ctrl Pts',(1.14048175790144,55.0583225162112,-0.293988409249102));
#42474=CARTESIAN_POINT('Ctrl Pts',(1.14349859068343,55.0574878604059,-0.282045248826515));
#42475=CARTESIAN_POINT('Ctrl Pts',(1.14505993746908,55.0570441303354,-0.275637976589591));
#42476=CARTESIAN_POINT('Ctrl Pts',(1.14931652314479,55.0557991903506,-0.257509666811821));
#42477=CARTESIAN_POINT('Ctrl Pts',(1.15188625205993,55.0550046342972,-0.245759615852099));
#42478=CARTESIAN_POINT('Ctrl Pts',(1.16866286949696,55.0494811374149,-0.162993878607308));
#42479=CARTESIAN_POINT('Ctrl Pts',(1.17647457772493,55.0450357830271,-0.0908306980814718));
#42480=CARTESIAN_POINT('Ctrl Pts',(1.17861992250281,55.0365543817954,0.0464771725981341));
#42481=CARTESIAN_POINT('Ctrl Pts',(1.17427072198975,55.0325376066607,0.111320340806615));
#42482=CARTESIAN_POINT('Ctrl Pts',(1.16131534920626,55.0269445488811,0.197304866431528));
#42483=CARTESIAN_POINT('Ctrl Pts',(1.15741269030201,55.0255083145317,0.219039527545507));
#42484=CARTESIAN_POINT('Ctrl Pts',(1.15049587333197,55.0232768939478,0.252176406502493));
#42485=CARTESIAN_POINT('Ctrl Pts',(1.14791741253601,55.022495491184,0.263665112773433));
#42486=CARTESIAN_POINT('Ctrl Pts',(1.14283262324068,55.0210405404852,0.284830729511583));
#42487=CARTESIAN_POINT('Ctrl Pts',(1.14037448914068,55.0203686010731,0.294518188008761));
#42488=CARTESIAN_POINT('Ctrl Pts',(1.13463569169775,55.0188656632129,0.315984811844149));
#42489=CARTESIAN_POINT('Ctrl Pts',(1.13129432004946,55.0180327591753,0.327746389496244));
#42490=CARTESIAN_POINT('Ctrl Pts',(1.12093920459054,55.0155676414008,0.362149323748651));
#42491=CARTESIAN_POINT('Ctrl Pts',(1.11342476060808,55.0139194431366,0.384632285434582));
#42492=CARTESIAN_POINT('Ctrl Pts',(1.07497959076489,55.0060831839344,0.489065762650575));
#42493=CARTESIAN_POINT('Ctrl Pts',(1.03565070053304,54.9996300485901,0.56761746655025));
#42494=CARTESIAN_POINT('Ctrl Pts',(0.969442531588526,54.990707116571,0.669654610185804));
#42495=CARTESIAN_POINT('Ctrl Pts',(0.949662429277538,54.9882198945523,0.697422151102629));
#42496=CARTESIAN_POINT('Ctrl Pts',(0.915953401506806,54.9842911252898,0.740644560120905));
#42497=CARTESIAN_POINT('Ctrl Pts',(0.902771317562335,54.982822225183,0.756656507838739));
#42498=CARTESIAN_POINT('Ctrl Pts',(0.883913089836965,54.980820630026,0.778368188113838));
#42499=CARTESIAN_POINT('Ctrl Pts',(0.878591895189533,54.980266284748,0.784369605151189));
#42500=CARTESIAN_POINT('Ctrl Pts',(0.869370039852177,54.9793239666549,0.794558705080641));
#42501=CARTESIAN_POINT('Ctrl Pts',(0.865499503476447,54.9789338830451,0.798773069888746));
#42502=CARTESIAN_POINT('Ctrl Pts',(0.857100945073473,54.9780992021727,0.807784961597127));
#42503=CARTESIAN_POINT('Ctrl Pts',(0.852563133054223,54.9776553437771,0.812572878971173));
#42504=CARTESIAN_POINT('Ctrl Pts',(0.839643177793984,54.9764106544644,0.825977538676623));
#42505=CARTESIAN_POINT('Ctrl Pts',(0.831168742760805,54.9756164608695,0.834504708796131));
#42506=CARTESIAN_POINT('Ctrl Pts',(0.759887831500031,54.96910190012,0.904065865912003));
#42507=CARTESIAN_POINT('Ctrl Pts',(0.690575612665228,54.9637969538521,0.958057510733683));
#42508=CARTESIAN_POINT('Ctrl Pts',(0.564118631517385,54.9546026258532,1.03564331340699));
#42509=CARTESIAN_POINT('Ctrl Pts',(0.509953626425511,54.9507945419868,1.06335925664925));
#42510=CARTESIAN_POINT('Ctrl Pts',(0.439022031967292,54.9457910238096,1.09298424626383));
#42511=CARTESIAN_POINT('Ctrl Pts',(0.424022193437949,54.9447324721056,1.09889037001887));
#42512=CARTESIAN_POINT('Ctrl Pts',(0.398974666808698,54.9429614303825,1.10816354301393));
#42513=CARTESIAN_POINT('Ctrl Pts',(0.388994032596335,54.9422548527236,1.1117062799895));
#42514=CARTESIAN_POINT('Ctrl Pts',(0.369290280166225,54.9408575239399,1.1184025262171));
#42515=CARTESIAN_POINT('Ctrl Pts',(0.35957118745721,54.9401671421677,1.1215650098626));
#42516=CARTESIAN_POINT('Ctrl Pts',(0.337993190246875,54.9386313406715,1.12827695021194));
#42517=CARTESIAN_POINT('Ctrl Pts',(0.326117142671027,54.9377840575074,1.13176669936527));
#42518=CARTESIAN_POINT('Ctrl Pts',(0.283985485277921,54.9347701025525,1.1434288060589));
#42519=CARTESIAN_POINT('Ctrl Pts',(0.253463298716431,54.9325715292742,1.15057951998783));
#42520=CARTESIAN_POINT('Ctrl Pts',(0.211467917550879,54.9295255765537,1.15866608436263));
#42521=CARTESIAN_POINT('Ctrl Pts',(0.200214607584779,54.9287074012446,1.16066346791927));
#42522=CARTESIAN_POINT('Ctrl Pts',(0.188938369713642,54.9278857931129,1.16249617416573));
#42523=CARTESIAN_POINT('Origin',(0.,56.5393671147362,0.));
#42524=CARTESIAN_POINT('',(0.188938462403164,54.3284116054606,1.16249615910106));
#42525=CARTESIAN_POINT('',(0.188938462297913,54.4261253209981,1.16249615911817));
#42526=CARTESIAN_POINT('',(0.188938462403162,56.5393671147362,1.16249615910107));
#42527=CARTESIAN_POINT('',(-1.17774953014575,54.6906328852638,-0.00105201780795915));
#42528=CARTESIAN_POINT('Ctrl Pts',(-1.17774953014575,54.6906328852638,-0.00105201780795915));
#42529=CARTESIAN_POINT('Ctrl Pts',(-1.17769714698767,54.6866752250911,-0.0596957397588973));
#42530=CARTESIAN_POINT('Ctrl Pts',(-1.17326078513928,54.6827175649183,-0.118144736281013));
#42531=CARTESIAN_POINT('Ctrl Pts',(-1.16455024767417,54.6787599047456,-0.175834533417163));
#42532=CARTESIAN_POINT('Ctrl Pts',(-1.1571934473316,54.6754173193045,-0.224558543965765));
#42533=CARTESIAN_POINT('Ctrl Pts',(-1.14678867429975,54.6720747338635,-0.272741503821657));
#42534=CARTESIAN_POINT('Ctrl Pts',(-1.13342818814217,54.6687321484224,-0.320055627703607));
#42535=CARTESIAN_POINT('Ctrl Pts',(-1.12020882427835,54.6654248695802,-0.366869988507296));
#42536=CARTESIAN_POINT('Ctrl Pts',(-1.10405318292451,54.6621175907379,-0.412973781673877));
#42537=CARTESIAN_POINT('Ctrl Pts',(-1.08506006393155,54.6588103118957,-0.457973492858332));
#42538=CARTESIAN_POINT('Ctrl Pts',(-1.06685448075384,54.6556401669565,-0.501107323865514));
#42539=CARTESIAN_POINT('Ctrl Pts',(-1.04604235028559,54.6524700220173,-0.543226257802928));
#42540=CARTESIAN_POINT('Ctrl Pts',(-1.0227617720575,54.6492998770781,-0.583997791192575));
#42541=CARTESIAN_POINT('Ctrl Pts',(-0.999504564628519,54.6461329145694,
-0.624728395043999));
#42542=CARTESIAN_POINT('Ctrl Pts',(-0.973784089242021,54.6429659520607,
-0.664113792576353));
#42543=CARTESIAN_POINT('Ctrl Pts',(-0.945785259301189,54.6397989895519,
-0.701844217607143));
#42544=CARTESIAN_POINT('Ctrl Pts',(-0.917802165167313,54.6366338069286,
-0.739553437513079));
#42545=CARTESIAN_POINT('Ctrl Pts',(-0.887543584916521,54.6334686243054,
-0.77560907957072));
#42546=CARTESIAN_POINT('Ctrl Pts',(-0.855237312034212,54.6303034416821,
-0.809730944576343));
#42547=CARTESIAN_POINT('Ctrl Pts',(-0.822934921954927,54.6271386394735,
-0.843848708567865));
#42548=CARTESIAN_POINT('Ctrl Pts',(-0.788585712944688,54.6239738372649,
-0.876032752989566));
#42549=CARTESIAN_POINT('Ctrl Pts',(-0.752455412507077,54.6208090350563,
-0.906038583443777));
#42550=CARTESIAN_POINT('Ctrl Pts',(-0.716288276356329,54.6176410062555,
-0.93607500556619));
#42551=CARTESIAN_POINT('Ctrl Pts',(-0.678336856667729,54.6144729774547,
-0.963928426297382));
#42552=CARTESIAN_POINT('Ctrl Pts',(-0.638899611772667,54.6113049486539,
-0.989394940646421));
#42553=CARTESIAN_POINT('Ctrl Pts',(-0.599438485017693,54.6081350014022,
-1.01487687665409));
#42554=CARTESIAN_POINT('Ctrl Pts',(-0.558490229227848,54.6049650541504,
-1.03796875576431));
#42555=CARTESIAN_POINT('Ctrl Pts',(-0.516378727411899,54.6017951068987,
-1.05851219755677));
#42556=CARTESIAN_POINT('Ctrl Pts',(-0.47419022450317,54.5986193633824,-1.07909320313584));
#42557=CARTESIAN_POINT('Ctrl Pts',(-0.430834748697438,54.5954436198662,
-1.09711626416715));
#42558=CARTESIAN_POINT('Ctrl Pts',(-0.38665520238492,54.5922678763499,-1.11247149040714));
#42559=CARTESIAN_POINT('Ctrl Pts',(-0.373159040957775,54.5912977363027,
-1.11716227221416));
#42560=CARTESIAN_POINT('Ctrl Pts',(-0.359586067085624,54.5903275962555,
-1.12160444674893));
#42561=CARTESIAN_POINT('Ctrl Pts',(-0.345946256988187,54.5893574562082,
-1.12579582952499));
#42562=CARTESIAN_POINT('Ctrl Pts',(-0.299447140209867,54.586050177366,-1.14008456197615));
#42563=CARTESIAN_POINT('Ctrl Pts',(-0.251952195345861,54.5827428985237,
-1.151521109822));
#42564=CARTESIAN_POINT('Ctrl Pts',(-0.203845604152202,54.5794356196815,
-1.15997501359634));
#42565=CARTESIAN_POINT('Ctrl Pts',(-0.157733757229438,54.5762654774635,
-1.16807837546566));
#42566=CARTESIAN_POINT('Ctrl Pts',(-0.11106060852584,54.5730953352455,-1.17344147846441));
#42567=CARTESIAN_POINT('Ctrl Pts',(-0.0641804021668466,54.5699251930276,
-1.17599997384256));
#42568=CARTESIAN_POINT('Ctrl Pts',(-0.0173472578631847,54.5667582332489,
-1.1785559008009));
#42569=CARTESIAN_POINT('Ctrl Pts',(0.029691977687938,54.5635912734702,-1.1783127619046));
#42570=CARTESIAN_POINT('Ctrl Pts',(0.076576767781138,54.5604243136914,-1.17525787005925));
#42571=CARTESIAN_POINT('Ctrl Pts',(0.123435207772002,54.5572591338016,-1.17220469511851));
#42572=CARTESIAN_POINT('Ctrl Pts',(0.170138817970292,54.5540939539117,-1.16634293350421));
#42573=CARTESIAN_POINT('Ctrl Pts',(0.216328640527614,54.5509287740218,-1.15771195976697));
#42574=CARTESIAN_POINT('Ctrl Pts',(0.26251291168148,54.5477639745445,-1.14908202335819));
#42575=CARTESIAN_POINT('Ctrl Pts',(0.308182969548269,54.5445991750672,-1.13768363999169));
#42576=CARTESIAN_POINT('Ctrl Pts',(0.352989274454559,54.54143437559,-1.12360742015174));
#42577=CARTESIAN_POINT('Ctrl Pts',(0.397841260845054,54.5382663494968,-1.10951684914813));
#42578=CARTESIAN_POINT('Ctrl Pts',(0.441827203933968,54.5350983234035,-1.09274316305695));
#42579=CARTESIAN_POINT('Ctrl Pts',(0.484613908187637,54.5319302973103,-1.07342648676614));
#42580=CARTESIAN_POINT('Ctrl Pts',(0.52742652278707,54.5287603527555,-1.0540981128751));
#42581=CARTESIAN_POINT('Ctrl Pts',(0.569037959078233,54.5255904082006,-1.03222394445421));
#42582=CARTESIAN_POINT('Ctrl Pts',(0.609139474858335,54.5224204636457,-1.00799016000619));
#42583=CARTESIAN_POINT('Ctrl Pts',(0.649314317073937,54.5192447227829,-0.983712063591465));
#42584=CARTESIAN_POINT('Ctrl Pts',(0.687973273422185,54.5160689819201,-0.957066063031638));
#42585=CARTESIAN_POINT('Ctrl Pts',(0.724838020934945,54.5128932410573,-0.928280618082222));
#42586=CARTESIAN_POINT('Ctrl Pts',(0.736099855229156,54.5119230820362,-0.919486934875976));
#42587=CARTESIAN_POINT('Ctrl Pts',(0.747194496707031,54.5109529230151,-0.910493858644433));
#42588=CARTESIAN_POINT('Ctrl Pts',(0.758114698226789,54.5099827639941,-0.90130858579762));
#42589=CARTESIAN_POINT('Ctrl Pts',(0.795341741067799,54.5066754851518,-0.869995926854831));
#42590=CARTESIAN_POINT('Ctrl Pts',(0.83071287117427,54.5033682063096,-0.836299528044534));
#42591=CARTESIAN_POINT('Ctrl Pts',(0.863910092825719,54.5000609274673,-0.800471369890178));
#42592=CARTESIAN_POINT('Ctrl Pts',(0.895730772895249,54.4968907868138,-0.766128846588667));
#42593=CARTESIAN_POINT('Ctrl Pts',(0.925553863000638,54.4937206461603,-0.729828340555749));
#42594=CARTESIAN_POINT('Ctrl Pts',(0.953133146393215,54.4905505055069,-0.691832543139285));
#42595=CARTESIAN_POINT('Ctrl Pts',(0.980684743215,54.4873835473263,-0.653874889329382));
#42596=CARTESIAN_POINT('Ctrl Pts',(1.00599666473445,54.4842165891458,-0.614225762145114));
#42597=CARTESIAN_POINT('Ctrl Pts',(1.02886268130304,54.4810496309653,-0.57318116291616));
#42598=CARTESIAN_POINT('Ctrl Pts',(1.05171584652856,54.4778844527041,-0.532159631903922));
#42599=CARTESIAN_POINT('Ctrl Pts',(1.07212555832836,54.4747192744429,-0.489744669280312));
#42600=CARTESIAN_POINT('Ctrl Pts',(1.08993018001366,54.4715540961818,-0.446259190600479));
#42601=CARTESIAN_POINT('Ctrl Pts',(1.10773266166441,54.4683892983607,-0.402778938677412));
#42602=CARTESIAN_POINT('Ctrl Pts',(1.12293046516394,54.4652245005396,-0.358228943358692));
#42603=CARTESIAN_POINT('Ctrl Pts',(1.13541010551767,54.4620597027184,-0.312952000773857));
#42604=CARTESIAN_POINT('Ctrl Pts',(1.14790246916459,54.4588916783099,-0.267628897258153));
#42605=CARTESIAN_POINT('Ctrl Pts',(1.15767099281451,54.4557236539014,-0.221577907227785));
#42606=CARTESIAN_POINT('Ctrl Pts',(1.16465265388608,54.4525556294928,-0.175154955100094));
#42607=CARTESIAN_POINT('Ctrl Pts',(1.17163854280376,54.4493856866412,-0.128703890880537));
#42608=CARTESIAN_POINT('Ctrl Pts',(1.17583416122577,54.4462157437895,-0.081880972708021));
#42609=CARTESIAN_POINT('Ctrl Pts',(1.17722844039909,54.4430458009378,-0.0350465635337289));
#42610=CARTESIAN_POINT('Ctrl Pts',(1.17862526903709,54.4398700617883,0.0118734832045577));
#42611=CARTESIAN_POINT('Ctrl Pts',(1.17721055979432,54.4366943226388,0.0588045053487816));
#42612=CARTESIAN_POINT('Ctrl Pts',(1.17302526479399,54.4335185834894,0.105388759623576));
#42613=CARTESIAN_POINT('Ctrl Pts',(1.17174668055132,54.4325484129195,0.119619989075107));
#42614=CARTESIAN_POINT('Ctrl Pts',(1.17020988885955,54.4315782423497,0.133818920283906));
#42615=CARTESIAN_POINT('Ctrl Pts',(1.16841700426522,54.4306080717799,0.147975560968334));
#42616=CARTESIAN_POINT('Ctrl Pts',(1.16230512098418,54.4273007929376,0.196235072923688));
#42617=CARTESIAN_POINT('Ctrl Pts',(1.15318394782368,54.4239935140954,0.244228494460377));
#42618=CARTESIAN_POINT('Ctrl Pts',(1.1410926766969,54.4206862352531,0.291551994828893));
#42619=CARTESIAN_POINT('Ctrl Pts',(1.1295027712319,54.4175160930302,0.336913221931717));
#42620=CARTESIAN_POINT('Ctrl Pts',(1.11518439637597,54.4143459508072,0.381658386778636));
#42621=CARTESIAN_POINT('Ctrl Pts',(1.09822467823407,54.4111758085843,0.425438148991927));
#42622=CARTESIAN_POINT('Ctrl Pts',(1.08128198566579,54.4080088488134,0.469173961443887));
#42623=CARTESIAN_POINT('Ctrl Pts',(1.06170339831795,54.4048418890425,0.511945770956285));
#42624=CARTESIAN_POINT('Ctrl Pts',(1.03962571650836,54.4016749292716,0.55341976118899));
#42625=CARTESIAN_POINT('Ctrl Pts',(1.01756044284565,54.3985097494023,0.594870442119264));
#42626=CARTESIAN_POINT('Ctrl Pts',(0.992999118661742,54.3953445695331,0.63502425644045));
#42627=CARTESIAN_POINT('Ctrl Pts',(0.966125343888607,54.3921793896638,0.673570250527828));
#42628=CARTESIAN_POINT('Ctrl Pts',(0.939254799095291,54.38901459022,0.712111611742302));
#42629=CARTESIAN_POINT('Ctrl Pts',(0.910072676264339,54.3858497907761,0.749045079670299));
#42630=CARTESIAN_POINT('Ctrl Pts',(0.878805396448503,54.3826849913323,0.78408936842237));
#42631=CARTESIAN_POINT('Ctrl Pts',(0.847506238811093,54.3795169652914,0.819169385756862));
#42632=CARTESIAN_POINT('Ctrl Pts',(0.814118055742262,54.3763489392505,0.852355964318174));
#42633=CARTESIAN_POINT('Ctrl Pts',(0.778905670317124,54.3731809132097,0.883403089901678));
#42634=CARTESIAN_POINT('Ctrl Pts',(0.743671961449416,54.3700109687182,0.914469016585741));
#42635=CARTESIAN_POINT('Ctrl Pts',(0.70661229246037,54.3668410242268,0.943392568656226));
#42636=CARTESIAN_POINT('Ctrl Pts',(0.668023397274221,54.3636710797353,0.969968970222352));
#42637=CARTESIAN_POINT('Ctrl Pts',(0.629363941700992,54.3604953389518,0.996593967146614));
#42638=CARTESIAN_POINT('Ctrl Pts',(0.589170160888317,54.3573195981681,1.02086296610438));
#42639=CARTESIAN_POINT('Ctrl Pts',(0.547764806441438,54.3541438573845,1.04261631453003));
#42640=CARTESIAN_POINT('Ctrl Pts',(0.535115855754481,54.3531736981116,1.04926176015386));
#42641=CARTESIAN_POINT('Ctrl Pts',(0.522353977954967,54.3522035388387,1.05567277334354));
#42642=CARTESIAN_POINT('Ctrl Pts',(0.509488714157003,54.3512333795657,1.06184571037729));
#42643=CARTESIAN_POINT('Ctrl Pts',(0.46737285401055,54.3480574561722,1.08205350066351));
#42644=CARTESIAN_POINT('Ctrl Pts',(0.423958030108927,54.3448815327787,1.09979725698727));
#42645=CARTESIAN_POINT('Ctrl Pts',(0.379562947566655,54.3417056093853,1.11491122127931));
#42646=CARTESIAN_POINT('Ctrl Pts',(0.335244821753066,54.3385351913014,1.12999898624514));
#42647=CARTESIAN_POINT('Ctrl Pts',(0.289950328535312,54.3353647732175,1.14246581355573));
#42648=CARTESIAN_POINT('Ctrl Pts',(0.244019505938903,54.3321943551337,1.15219336190647));
#42649=CARTESIAN_POINT('Ctrl Pts',(0.225752219673109,54.330933438576,1.15606213455939));
#42650=CARTESIAN_POINT('Ctrl Pts',(0.20738449580817,54.3296725220183,1.15949815763526));
#42651=CARTESIAN_POINT('Ctrl Pts',(0.188938462403164,54.3284116054606,1.16249615910106));
#42652=CARTESIAN_POINT('Ctrl Pts',(0.189250941523835,54.8284605668477,1.16440479426666));
#42653=CARTESIAN_POINT('Ctrl Pts',(0.184506076350226,54.8281342221821,1.16518167980759));
#42654=CARTESIAN_POINT('Ctrl Pts',(-0.205344558386595,54.8013496467784,
1.22634143776596));
#42655=CARTESIAN_POINT('Ctrl Pts',(-0.929401945135899,54.7554070862504,
0.962178865328913));
#42656=CARTESIAN_POINT('Ctrl Pts',(-1.17480714037443,54.7097908703881,0.282712264297831));
#42657=CARTESIAN_POINT('Ctrl Pts',(-1.17726285833084,54.6906328852638,-0.00105158309123631));
#42658=CARTESIAN_POINT('Ctrl Pts',(0.188938369713642,54.9278857931129,1.16249617416573));
#42659=CARTESIAN_POINT('Ctrl Pts',(0.108581669493369,54.9220308511459,1.17555640117773));
#42660=CARTESIAN_POINT('Ctrl Pts',(0.0270620916905724,54.9159800893122,
1.18025324761532));
#42661=CARTESIAN_POINT('Ctrl Pts',(-0.077617854509977,54.9083565733959,
1.17542123889652));
#42662=CARTESIAN_POINT('Ctrl Pts',(-0.100893065296731,54.9066724863899,
1.17365256173212));
#42663=CARTESIAN_POINT('Ctrl Pts',(-0.14005917505716,54.9038719617761,1.16950245545791));
#42664=CARTESIAN_POINT('Ctrl Pts',(-0.155981514105395,54.9027428553921,
1.16748550112007));
#42665=CARTESIAN_POINT('Ctrl Pts',(-0.179072317711987,54.9011236996199,
1.16407960968587));
#42666=CARTESIAN_POINT('Ctrl Pts',(-0.186276257296968,54.9006211569238,
1.16294857823349));
#42667=CARTESIAN_POINT('Ctrl Pts',(-0.19905645408507,54.8997348032224,1.16082025773074));
#42668=CARTESIAN_POINT('Ctrl Pts',(-0.204636607717194,54.8993496028971,
1.15984956150082));
#42669=CARTESIAN_POINT('Ctrl Pts',(-0.217214822377719,54.8984853764831,
1.15756791011367));
#42670=CARTESIAN_POINT('Ctrl Pts',(-0.224208271457074,54.8980076380246,
1.1562337147267));
#42671=CARTESIAN_POINT('Ctrl Pts',(-0.245980185316471,54.8965277735199,
1.15187514313082));
#42672=CARTESIAN_POINT('Ctrl Pts',(-0.260713552500866,54.8955370300955,
1.14863009369191));
#42673=CARTESIAN_POINT('Ctrl Pts',(-0.347820091324163,54.8897212876633,
1.12768217855371));
#42674=CARTESIAN_POINT('Ctrl Pts',(-0.418450900997335,54.8851698085063,
1.10342527070036));
#42675=CARTESIAN_POINT('Ctrl Pts',(-0.527974751455495,54.8777351613088,
1.05376908114118));
#42676=CARTESIAN_POINT('Ctrl Pts',(-0.568489790798299,54.8748949739316,
1.03247545610662));
#42677=CARTESIAN_POINT('Ctrl Pts',(-0.633558495604673,54.8700680564544,
0.99328374925848));
#42678=CARTESIAN_POINT('Ctrl Pts',(-0.658842832371133,54.8681206356811,
0.976695888467234));
#42679=CARTESIAN_POINT('Ctrl Pts',(-0.694201584681734,54.8652725059112,
0.95150049994778));
#42680=CARTESIAN_POINT('Ctrl Pts',(-0.704813837404146,54.8644007708928,
0.943666505115941));
#42681=CARTESIAN_POINT('Ctrl Pts',(-0.723303031717886,54.8628503575778,
0.929531856295309));
#42682=CARTESIAN_POINT('Ctrl Pts',(-0.73123491696054,54.8621746190346,0.923305059502648));
#42683=CARTESIAN_POINT('Ctrl Pts',(-0.747772405007723,54.8607425859896,
0.909975809455529));
#42684=CARTESIAN_POINT('Ctrl Pts',(-0.75635894686126,54.8599854487067,0.902851411910783));
#42685=CARTESIAN_POINT('Ctrl Pts',(-0.779239708303687,54.8579300140871,
0.883311371016615));
#42686=CARTESIAN_POINT('Ctrl Pts',(-0.793337355154101,54.8566226121273,
0.870671734589314));
#42687=CARTESIAN_POINT('Ctrl Pts',(-0.867104472317129,54.8495538179979,
0.801254354402917));
#42688=CARTESIAN_POINT('Ctrl Pts',(-0.920989442588037,54.8435432644789,
0.738683132758252));
#42689=CARTESIAN_POINT('Ctrl Pts',(-1.00312490803696,54.8329487937804,0.620207925566341));
#42690=CARTESIAN_POINT('Ctrl Pts',(-1.03429751970192,54.8284055593831,0.566698794979591));
#42691=CARTESIAN_POINT('Ctrl Pts',(-1.06606476437224,54.823253417583,0.50072999928577));
#42692=CARTESIAN_POINT('Ctrl Pts',(-1.07085436532039,54.8224594372652,0.490403473146365));
#42693=CARTESIAN_POINT('Ctrl Pts',(-1.07809910779166,54.8212325815254,0.474171109776234));
#42694=CARTESIAN_POINT('Ctrl Pts',(-1.08065700117231,54.8207940213225,0.468312265745476));
#42695=CARTESIAN_POINT('Ctrl Pts',(-1.08541558695512,54.8199681200594,0.457166117124832));
#42696=CARTESIAN_POINT('Ctrl Pts',(-1.08762559530859,54.8195802720838,0.451883193769292));
#42697=CARTESIAN_POINT('Ctrl Pts',(-1.09298637632923,54.8186283091335,0.438801310182127));
#42698=CARTESIAN_POINT('Ctrl Pts',(-1.09609237283216,54.8180667946752,0.430984140251647));
#42699=CARTESIAN_POINT('Ctrl Pts',(-1.10700727185474,54.8160542896141,0.402632079139013));
#42700=CARTESIAN_POINT('Ctrl Pts',(-1.11432548104744,54.8146287099396,0.381911711804298));
#42701=CARTESIAN_POINT('Ctrl Pts',(-1.14439677534529,54.8083525859727,0.288526705492827));
#42702=CARTESIAN_POINT('Ctrl Pts',(-1.16065296617681,54.8037277940154,0.21395851718434));
#42703=CARTESIAN_POINT('Ctrl Pts',(-1.17500700128451,54.7961443342316,0.092600222495293));
#42704=CARTESIAN_POINT('Ctrl Pts',(-1.17772883794596,54.7932584919118,0.0465884156002357));
#42705=CARTESIAN_POINT('Ctrl Pts',(-1.17775905422434,54.7890057452512,-0.0195486318965704));
#42706=CARTESIAN_POINT('Ctrl Pts',(-1.1772543585512,54.7877008649724,-0.0396312800953101));
#42707=CARTESIAN_POINT('Ctrl Pts',(-1.17560237447178,54.7855579377134,-0.072184705846541));
#42708=CARTESIAN_POINT('Ctrl Pts',(-1.17476930470118,54.7847295782293,-0.0846677938813687));
#42709=CARTESIAN_POINT('Ctrl Pts',(-1.17291149514694,54.7832267674816,-0.10711679915608));
#42710=CARTESIAN_POINT('Ctrl Pts',(-1.17195814144035,54.7825546175109,-0.117087523376365));
#42711=CARTESIAN_POINT('Ctrl Pts',(-1.16963011200334,54.7810975712469,-0.138543276299966));
#42712=CARTESIAN_POINT('Ctrl Pts',(-1.16821318832554,54.7803114094776,-0.150022558999053));
#42713=CARTESIAN_POINT('Ctrl Pts',(-1.16375058502073,54.7780839065945,-0.182263304119424));
#42714=CARTESIAN_POINT('Ctrl Pts',(-1.16031893835141,54.7766306519293,-0.202966004753446));
#42715=CARTESIAN_POINT('Ctrl Pts',(-1.15122345551503,54.7732739204956,-0.250010230692414));
#42716=CARTESIAN_POINT('Ctrl Pts',(-1.14520520299659,54.7713606084661,-0.276270551289992));
#42717=CARTESIAN_POINT('Ctrl Pts',(-1.1188945800364,54.7639958192158,-0.375341658136661));
#42718=CARTESIAN_POINT('Ctrl Pts',(-1.09251201653423,54.7583975787809,-0.446343184072841));
#42719=CARTESIAN_POINT('Ctrl Pts',(-1.04185166901587,54.7499215403512,-0.550705009782923));
#42720=CARTESIAN_POINT('Ctrl Pts',(-1.02232476271566,54.7469973203523,-0.586160087344906));
#42721=CARTESIAN_POINT('Ctrl Pts',(-0.995716171738834,54.7434572921974,
-0.629082921543322));
#42722=CARTESIAN_POINT('Ctrl Pts',(-0.990312910763654,54.7427586216219,
-0.637554995829922));
#42723=CARTESIAN_POINT('Ctrl Pts',(-0.98145111325753,54.7416458264976,-0.651065352990109));
#42724=CARTESIAN_POINT('Ctrl Pts',(-0.978060773390028,54.7412275500888,
-0.656147475368266));
#42725=CARTESIAN_POINT('Ctrl Pts',(-0.971284256245348,54.7404064328614,
-0.666136241299758));
#42726=CARTESIAN_POINT('Ctrl Pts',(-0.967900093340072,54.7400034950416,
-0.671043970757845));
#42727=CARTESIAN_POINT('Ctrl Pts',(-0.959113326017375,54.7389748023258,
-0.68358181002923));
#42728=CARTESIAN_POINT('Ctrl Pts',(-0.953656732186058,54.7383525660555,
-0.691173866745431));
#42729=CARTESIAN_POINT('Ctrl Pts',(-0.928554737045014,54.7355598758739,
-0.725236325850173));
#42730=CARTESIAN_POINT('Ctrl Pts',(-0.907892009083777,54.7334494814902,
-0.750942172714864));
#42731=CARTESIAN_POINT('Ctrl Pts',(-0.831956102099352,54.7261844494736,
-0.837687424251704));
#42732=CARTESIAN_POINT('Ctrl Pts',(-0.771391268898121,54.72120722517,-0.893771644464102));
#42733=CARTESIAN_POINT('Ctrl Pts',(-0.672745192382404,54.7134752931164,
-0.967563538040086));
#42734=CARTESIAN_POINT('Ctrl Pts',(-0.638770769926838,54.7108721146176,
-0.990321503259062));
#42735=CARTESIAN_POINT('Ctrl Pts',(-0.590897797535063,54.7072321195802,
-1.01889971555601));
#42736=CARTESIAN_POINT('Ctrl Pts',(-0.577967668195078,54.7062517953168,
-1.02628952009828));
#42737=CARTESIAN_POINT('Ctrl Pts',(-0.555906764961072,54.7045818328036,
-1.03834859646736));
#42738=CARTESIAN_POINT('Ctrl Pts',(-0.546848612388174,54.7038968872125,
-1.04314750773779));
#42739=CARTESIAN_POINT('Ctrl Pts',(-0.528349280265607,54.7024988845071,
-1.05264108546199));
#42740=CARTESIAN_POINT('Ctrl Pts',(-0.518905411456307,54.7017856479119,
-1.05732841544101));
#42741=CARTESIAN_POINT('Ctrl Pts',(-0.49507510755737,54.699986338297,-1.06876009004839));
#42742=CARTESIAN_POINT('Ctrl Pts',(-0.480613126983862,54.6988947656863,
-1.07534109525262));
#42743=CARTESIAN_POINT('Ctrl Pts',(-0.414079332678504,54.6938721156605,
-1.10400742266151));
#42744=CARTESIAN_POINT('Ctrl Pts',(-0.360598570169302,54.6898276151714,
-1.12261350612172));
#42745=CARTESIAN_POINT('Ctrl Pts',(-0.236607282692602,54.6804765777453,
-1.15597373823385));
#42746=CARTESIAN_POINT('Ctrl Pts',(-0.165658220731116,54.6751400775437,
-1.16825318048703));
#42747=CARTESIAN_POINT('Ctrl Pts',(-0.0677973196773159,54.6680488363,-1.17609154216601));
#42748=CARTESIAN_POINT('Ctrl Pts',(-0.0414962503687463,54.6661706621978,
-1.17731307788736));
#42749=CARTESIAN_POINT('Ctrl Pts',(-0.00620822457986493,54.6637056175882,
-1.17776777186951));
#42750=CARTESIAN_POINT('Ctrl Pts',(0.00275923744179654,54.6630839576747,
-1.17778090728269));
#42751=CARTESIAN_POINT('Ctrl Pts',(0.0170288891855195,54.6621032106605,
-1.17763882388204));
#42752=CARTESIAN_POINT('Ctrl Pts',(0.0223311839644545,54.6617406504017,
-1.17755021281724));
#42753=CARTESIAN_POINT('Ctrl Pts',(0.0336688795939275,54.6609696451615,
-1.17728413008523));
#42754=CARTESIAN_POINT('Ctrl Pts',(0.0397039171113984,54.6605618117028,
-1.17709605364665));
#42755=CARTESIAN_POINT('Ctrl Pts',(0.0554425579326808,54.6595043162332,
-1.1764843889278));
#42756=CARTESIAN_POINT('Ctrl Pts',(0.0651430615232246,54.658858565791,-1.17598715616429));
#42757=CARTESIAN_POINT('Ctrl Pts',(0.112739746730623,54.6557148767919,-1.17295663925994));
#42758=CARTESIAN_POINT('Ctrl Pts',(0.150507990496832,54.6532972017246,-1.16871103171584));
#42759=CARTESIAN_POINT('Ctrl Pts',(0.236534609546935,54.6478346404813,-1.15479989239462));
#42760=CARTESIAN_POINT('Ctrl Pts',(0.284523181011152,54.6448186888625,-1.14392232147804));
#42761=CARTESIAN_POINT('Ctrl Pts',(0.393870105687706,54.6377672939315,-1.11182753881352));
#42762=CARTESIAN_POINT('Ctrl Pts',(0.45442784818955,54.6337207868725,-1.08847968366745));
#42763=CARTESIAN_POINT('Ctrl Pts',(0.527600976521416,54.6284347459268,-1.05309270401104));
#42764=CARTESIAN_POINT('Ctrl Pts',(0.542294454486342,54.6273525355407,-1.04560208217233));
#42765=CARTESIAN_POINT('Ctrl Pts',(0.566220449129681,54.6255529572428,-1.03276480680303));
#42766=CARTESIAN_POINT('Ctrl Pts',(0.575546495912091,54.6248419195946,-1.02759669205789));
#42767=CARTESIAN_POINT('Ctrl Pts',(0.593728197322663,54.6234360254039,-1.01719598292522));
#42768=CARTESIAN_POINT('Ctrl Pts',(0.60258802423958,54.6227415474659,-1.01197257933475));
#42769=CARTESIAN_POINT('Ctrl Pts',(0.623778198427206,54.6210571287002,-0.999102749447694));
#42770=CARTESIAN_POINT('Ctrl Pts',(0.636037599809329,54.6200631178208,-0.991343373117623));
#42771=CARTESIAN_POINT('Ctrl Pts',(0.681740789331787,54.6162812688511,-0.961219581866173));
#42772=CARTESIAN_POINT('Ctrl Pts',(0.714171268817931,54.6134393373115,-0.937375240573873));
#42773=CARTESIAN_POINT('Ctrl Pts',(0.805441476021531,54.604966194094,-0.862779855198039));
#42774=CARTESIAN_POINT('Ctrl Pts',(0.860557351021353,54.5992073911695,-0.807814554644207));
#42775=CARTESIAN_POINT('Ctrl Pts',(0.933963449342101,54.5907728932945,-0.718504433795098));
#42776=CARTESIAN_POINT('Ctrl Pts',(0.956639811387714,54.5880335490278,-0.688024117740916));
#42777=CARTESIAN_POINT('Ctrl Pts',(0.983350729976969,54.5846755841962,-0.64824019699935));
#42778=CARTESIAN_POINT('Ctrl Pts',(0.988790913662792,54.5839840689516,-0.639911366386337));
#42779=CARTESIAN_POINT('Ctrl Pts',(0.997389461945781,54.5828798356126,-0.626375594541597));
#42780=CARTESIAN_POINT('Ctrl Pts',(1.00061398592784,54.5824630742235,-0.621211541796408));
#42781=CARTESIAN_POINT('Ctrl Pts',(1.00692590964027,54.5816422844805,-0.610926368321388));
#42782=CARTESIAN_POINT('Ctrl Pts',(1.01001462078615,54.5812381885914,-0.605806309022732));
#42783=CARTESIAN_POINT('Ctrl Pts',(1.01787711737896,54.5802025548088,-0.592545601026591));
#42784=CARTESIAN_POINT('Ctrl Pts',(1.02259241760102,54.579574629722,-0.584370496326));
#42785=CARTESIAN_POINT('Ctrl Pts',(1.04387846456012,54.5767036294536,-0.546419218456751));
#42786=CARTESIAN_POINT('Ctrl Pts',(1.05925180605185,54.5745248492067,-0.515986704178548));
#42787=CARTESIAN_POINT('Ctrl Pts',(1.11047992812902,54.566694263782,-0.40260403237415));
#42788=CARTESIAN_POINT('Ctrl Pts',(1.13808041660133,54.5612500644246,-0.316274726700439));
#42789=CARTESIAN_POINT('Ctrl Pts',(1.16204987914672,54.5534084638769,-0.194599410206666));
#42790=CARTESIAN_POINT('Ctrl Pts',(1.16713771155286,54.551249007355,-0.161301271577753));
#42791=CARTESIAN_POINT('Ctrl Pts',(1.1723121967252,54.548129177481,-0.113909414185334));
#42792=CARTESIAN_POINT('Ctrl Pts',(1.17358389329953,54.547205354255,-0.0999602868893795));
#42793=CARTESIAN_POINT('Ctrl Pts',(1.17535126702935,54.5455952498521,-0.0758189479226175));
#42794=CARTESIAN_POINT('Ctrl Pts',(1.17596383084177,54.5449126934121,-0.0656366597614956));
#42795=CARTESIAN_POINT('Ctrl Pts',(1.17695327134181,54.5434977355447,-0.0446436200955752));
#42796=CARTESIAN_POINT('Ctrl Pts',(1.17731362158029,54.5427648827179,-0.0338330981236268));
#42797=CARTESIAN_POINT('Ctrl Pts',(1.17786231659242,54.5408505364274,-0.00576544268209311));
#42798=CARTESIAN_POINT('Ctrl Pts',(1.17782033085533,54.5396620020008,0.0114930477235766));
#42799=CARTESIAN_POINT('Ctrl Pts',(1.17689309380546,54.5370198203333,0.0494746363727649));
#42800=CARTESIAN_POINT('Ctrl Pts',(1.17583957954222,54.5355615004583,0.0701875126270989));
#42801=CARTESIAN_POINT('Ctrl Pts',(1.17075091672426,54.5308759401054,0.13595091066353));
#42802=CARTESIAN_POINT('Ctrl Pts',(1.16466799213186,54.527595840425,0.180798628272209));
#42803=CARTESIAN_POINT('Ctrl Pts',(1.14205207629161,54.5189339489643,0.296902610729511));
#42804=CARTESIAN_POINT('Ctrl Pts',(1.12143712644088,54.5135130500848,0.367169973399234));
#42805=CARTESIAN_POINT('Ctrl Pts',(1.08889429953316,54.5072422613434,0.449032090634663));
#42806=CARTESIAN_POINT('Ctrl Pts',(1.08307956631484,54.5061834682992,0.46288153659903));
#42807=CARTESIAN_POINT('Ctrl Pts',(1.07407486069448,54.5046348216219,0.483229289108244));
#42808=CARTESIAN_POINT('Ctrl Pts',(1.07108759180195,54.5041346880911,0.489814995240465));
#42809=CARTESIAN_POINT('Ctrl Pts',(1.06561034432849,54.5032422018361,0.50160032275441));
#42810=CARTESIAN_POINT('Ctrl Pts',(1.06314249258167,54.5028485846098,0.506809960468223));
#42811=CARTESIAN_POINT('Ctrl Pts',(1.05789437667232,54.5020293351275,0.517681690848827));
#42812=CARTESIAN_POINT('Ctrl Pts',(1.05510672374399,54.5016041534072,0.523339900446246));
#42813=CARTESIAN_POINT('Ctrl Pts',(1.04734369320552,54.5004462676145,0.538782640181988));
#42814=CARTESIAN_POINT('Ctrl Pts',(1.04227663931822,54.4997189388052,0.54852071399552));
#42815=CARTESIAN_POINT('Ctrl Pts',(1.00717831862028,54.4948579261839,0.613731042242867));
#42816=CARTESIAN_POINT('Ctrl Pts',(0.972864593137731,54.4909461546723,0.666791207534335));
#42817=CARTESIAN_POINT('Ctrl Pts',(0.884724827568501,54.4819959243063,0.781686773891485));
#42818=CARTESIAN_POINT('Ctrl Pts',(0.82838195215865,54.4769783437578,0.84116225721547));
#42819=CARTESIAN_POINT('Ctrl Pts',(0.751927443845804,54.4704648228739,0.90667547904812));
#42820=CARTESIAN_POINT('Ctrl Pts',(0.737219192660802,54.4692245407684,0.918674643985659));
#42821=CARTESIAN_POINT('Ctrl Pts',(0.713407547253337,54.4672320583351,0.937160298928722));
#42822=CARTESIAN_POINT('Ctrl Pts',(0.704490340064837,54.4664892138377,0.943881931515761));
#42823=CARTESIAN_POINT('Ctrl Pts',(0.68734329257481,54.4650662011728,0.956428718205439));
#42824=CARTESIAN_POINT('Ctrl Pts',(0.679131552459769,54.4643870157674,0.962276996676362));
#42825=CARTESIAN_POINT('Ctrl Pts',(0.660020805452485,54.4628110531842,0.975520918261391));
#42826=CARTESIAN_POINT('Ctrl Pts',(0.649070973082307,54.4619114963118,0.982840461512534));
#42827=CARTESIAN_POINT('Ctrl Pts',(0.612695893329041,54.4589330231006,1.00628282084194));
#42828=CARTESIAN_POINT('Ctrl Pts',(0.586776890231113,54.4568258196721,1.02161341641516));
#42829=CARTESIAN_POINT('Ctrl Pts',(0.520339466511532,54.4514596410861,1.0575471570204));
#42830=CARTESIAN_POINT('Ctrl Pts',(0.479164326107252,54.4481638963685,1.07682868089076));
#42831=CARTESIAN_POINT('Ctrl Pts',(0.368592864083023,54.4394435625942,1.12100762906506));
#42832=CARTESIAN_POINT('Ctrl Pts',(0.297789053653392,54.4339796611412,1.14185877667398));
#42833=CARTESIAN_POINT('Ctrl Pts',(0.21334758840768,54.4278627005996,1.15833118914294));
#42834=CARTESIAN_POINT('Ctrl Pts',(0.201159235894327,54.4269895694131,1.16050993821474));
#42835=CARTESIAN_POINT('Ctrl Pts',(0.188938462297913,54.4261253209981,1.16249615911817));
#42836=CARTESIAN_POINT('Origin',(0.,56.5393671147362,0.));
#42837=CARTESIAN_POINT('',(0.188938462962337,53.8275149312419,1.16249615901018));
#42838=CARTESIAN_POINT('',(0.188938426235786,53.9273245270844,1.16249616497928));
#42839=CARTESIAN_POINT('',(0.188938462403162,56.5393671147362,1.16249615910107));
#42840=CARTESIAN_POINT('',(-1.17774998792321,54.1906328852639,0.000168662017078135));
#42841=CARTESIAN_POINT('Ctrl Pts',(0.188938462962337,53.8275149312419,1.16249615901018));
#42842=CARTESIAN_POINT('Ctrl Pts',(0.189897639249771,53.8275777423717,1.16234026576955));
#42843=CARTESIAN_POINT('Ctrl Pts',(0.190856653239826,53.8276405882925,1.16218318042302));
#42844=CARTESIAN_POINT('Ctrl Pts',(0.210455175505641,53.828925852409,1.15894805147591));
#42845=CARTESIAN_POINT('Ctrl Pts',(0.229017209989778,53.8301605467417,1.15542330758652));
#42846=CARTESIAN_POINT('Ctrl Pts',(0.258387312155716,53.8321463248688,1.14911069794213));
#42847=CARTESIAN_POINT('Ctrl Pts',(0.269254828374231,53.8328881692897,1.14661293477084));
#42848=CARTESIAN_POINT('Ctrl Pts',(0.289884212587121,53.8343107124266,1.14156208239429));
#42849=CARTESIAN_POINT('Ctrl Pts',(0.299651983091371,53.8349904484463,1.13903710330027));
#42850=CARTESIAN_POINT('Ctrl Pts',(0.322133920444049,53.836569853095,1.13291630709004));
#42851=CARTESIAN_POINT('Ctrl Pts',(0.334822206125474,53.837472338609,1.12923145851975));
#42852=CARTESIAN_POINT('Ctrl Pts',(0.3764559888895,53.8404717192991,1.11637708415354));
#42853=CARTESIAN_POINT('Ctrl Pts',(0.405106892572755,53.8425974539408,1.10630241004607));
#42854=CARTESIAN_POINT('Ctrl Pts',(0.476148948615423,53.8480272187007,1.07819169208433));
#42855=CARTESIAN_POINT('Ctrl Pts',(0.51792920499476,53.8513692073833,1.0587557666041));
#42856=CARTESIAN_POINT('Ctrl Pts',(0.624846357842988,53.8602658250449,1.00117299845565));
#42857=CARTESIAN_POINT('Ctrl Pts',(0.687647566758462,53.8658603700334,0.959125839624569));
#42858=CARTESIAN_POINT('Ctrl Pts',(0.756981068135981,53.8722076462129,0.902372484951482));
#42859=CARTESIAN_POINT('Ctrl Pts',(0.767799334606846,53.8732030540073,0.89318568358655));
#42860=CARTESIAN_POINT('Ctrl Pts',(0.783668183433016,53.8746675084701,0.879208510087267));
#42861=CARTESIAN_POINT('Ctrl Pts',(0.788846230534145,53.8751460712782,0.874565638840407));
#42862=CARTESIAN_POINT('Ctrl Pts',(0.79775202792912,53.8759699302324,0.866436844092695));
#42863=CARTESIAN_POINT('Ctrl Pts',(0.801498575625582,53.8763167242912,0.862972269783275));
#42864=CARTESIAN_POINT('Ctrl Pts',(0.810441151674094,53.8771450615838,0.854594252444472));
#42865=CARTESIAN_POINT('Ctrl Pts',(0.815615113787397,53.8776248520316,0.849657689516876));
#42866=CARTESIAN_POINT('Ctrl Pts',(0.831685292066203,53.8791180043831,0.834042790325199));
#42867=CARTESIAN_POINT('Ctrl Pts',(0.842419658972177,53.880119689121,0.823199230203634));
#42868=CARTESIAN_POINT('Ctrl Pts',(0.867930019453822,53.8825201866217,0.7964075761164));
#42869=CARTESIAN_POINT('Ctrl Pts',(0.882481348775273,53.8839065432435,0.780252730743327));
#42870=CARTESIAN_POINT('Ctrl Pts',(0.946069181071393,53.8900931502315,0.705601441695176));
#42871=CARTESIAN_POINT('Ctrl Pts',(0.98979692783405,53.8947207961409,0.642824522778941));
#42872=CARTESIAN_POINT('Ctrl Pts',(1.04983483772091,53.902384688117,0.535810188895795));
#42873=CARTESIAN_POINT('Ctrl Pts',(1.07011476638204,53.9053231991769,0.494064195936099));
#42874=CARTESIAN_POINT('Ctrl Pts',(1.0938613077573,53.9093623800676,0.436813734239895));
#42875=CARTESIAN_POINT('Ctrl Pts',(1.09955522464394,53.9103885928817,0.422276058150287));
#42876=CARTESIAN_POINT('Ctrl Pts',(1.10822674474456,53.9120510285451,0.398770263743154));
#42877=CARTESIAN_POINT('Ctrl Pts',(1.11138844363077,53.9126810824535,0.389871721903961));
#42878=CARTESIAN_POINT('Ctrl Pts',(1.11775903401152,53.9140026823846,0.371234334629821));
#42879=CARTESIAN_POINT('Ctrl Pts',(1.12094842104168,53.914694809176,0.361489716459661));
#42880=CARTESIAN_POINT('Ctrl Pts',(1.12828375179494,53.9163631632894,0.338046812101474));
#42881=CARTESIAN_POINT('Ctrl Pts',(1.13230793958074,53.9173432638144,0.324312457399663));
#42882=CARTESIAN_POINT('Ctrl Pts',(1.14623074235185,53.9209898976618,0.273372088435909));
#42883=CARTESIAN_POINT('Ctrl Pts',(1.15455269352216,53.9237055268266,0.235764122619588));
#42884=CARTESIAN_POINT('Ctrl Pts',(1.17284800863217,53.9315212581504,0.128387594307932));
#42885=CARTESIAN_POINT('Ctrl Pts',(1.17842512749248,53.9367233397907,0.0580386173100602));
#42886=CARTESIAN_POINT('Ctrl Pts',(1.17719406156194,53.9453055518037,-0.0590789737077564));
#42887=CARTESIAN_POINT('Ctrl Pts',(1.17392578973604,53.9486985923327,-0.105713439042868));
#42888=CARTESIAN_POINT('Ctrl Pts',(1.16656638533144,53.9526978841541,-0.162246666670006));
#42889=CARTESIAN_POINT('Ctrl Pts',(1.16510308156413,53.9534144184061,-0.172441119994811));
#42890=CARTESIAN_POINT('Ctrl Pts',(1.16255042512915,53.9545487457405,-0.188704972689162));
#42891=CARTESIAN_POINT('Ctrl Pts',(1.16154684606806,53.954970962947,-0.194787028516905));
#42892=CARTESIAN_POINT('Ctrl Pts',(1.15948547955847,53.9557934887811,-0.206696784265587));
#42893=CARTESIAN_POINT('Ctrl Pts',(1.15843140720323,53.9561939650385,-0.212524857710682));
#42894=CARTESIAN_POINT('Ctrl Pts',(1.15563649841637,53.9572073230373,-0.22733922774901));
#42895=CARTESIAN_POINT('Ctrl Pts',(1.1538347394827,53.9578168939249,-0.236313875792791));
#42896=CARTESIAN_POINT('Ctrl Pts',(1.14554327633093,53.9604466462181,-0.275255822113258));
#42897=CARTESIAN_POINT('Ctrl Pts',(1.13798883547569,53.9624150798674,-0.304986758619145));
#42898=CARTESIAN_POINT('Ctrl Pts',(1.10968073766334,53.968715581962,-0.400586741195724));
#42899=CARTESIAN_POINT('Ctrl Pts',(1.08429662152824,53.9729174156476,-0.464933195086711));
#42900=CARTESIAN_POINT('Ctrl Pts',(1.02914757691913,53.9805815446967,-0.575235967531483));
#42901=CARTESIAN_POINT('Ctrl Pts',(1.0015503143283,53.9839992066261,-0.622042691239074));
#42902=CARTESIAN_POINT('Ctrl Pts',(0.961733264705776,53.9885776501915,-0.680016297896189));
#42903=CARTESIAN_POINT('Ctrl Pts',(0.952370572936345,53.9896324951966,-0.693068026083361));
#42904=CARTESIAN_POINT('Ctrl Pts',(0.936403532666097,53.9913990266495,-0.714391627175366));
#42905=CARTESIAN_POINT('Ctrl Pts',(0.929949172021173,53.9921048629762,-0.722773476273312));
#42906=CARTESIAN_POINT('Ctrl Pts',(0.916959915571681,53.9935100108338,-0.73917971222927));
#42907=CARTESIAN_POINT('Ctrl Pts',(0.910430427055062,53.9942090658191,-0.747207172953837));
#42908=CARTESIAN_POINT('Ctrl Pts',(0.894276147606383,53.9959217233004,-0.766541381636501));
#42909=CARTESIAN_POINT('Ctrl Pts',(0.884541892172662,53.9969397356197,-0.77775389653972));
#42910=CARTESIAN_POINT('Ctrl Pts',(0.845521438562907,54.0009686764683,-0.82101980216904));
#42911=CARTESIAN_POINT('Ctrl Pts',(0.814687195453629,54.0040435141677,-0.851624325514253));
#42912=CARTESIAN_POINT('Ctrl Pts',(0.710896694080237,54.0140539845682,-0.943836736078548));
#42913=CARTESIAN_POINT('Ctrl Pts',(0.632124065275281,54.0211944805238,-0.998308210793504));
#42914=CARTESIAN_POINT('Ctrl Pts',(0.529841482324578,54.029471477815,-1.05203021150768));
#42915=CARTESIAN_POINT('Ctrl Pts',(0.511797970141039,54.0308959709475,-1.06092531016591));
#42916=CARTESIAN_POINT('Ctrl Pts',(0.486152891062619,54.0328626275226,-1.07276116602866));
#42917=CARTESIAN_POINT('Ctrl Pts',(0.478736169437238,54.0334247295666,-1.07609146561457));
#42918=CARTESIAN_POINT('Ctrl Pts',(0.466023960516743,54.0343761194926,-1.08164212659122));
#42919=CARTESIAN_POINT('Ctrl Pts',(0.460745751650601,54.0347676208057,-1.08390100101109));
#42920=CARTESIAN_POINT('Ctrl Pts',(0.449413118188616,54.0356004802199,-1.08865319410042));
#42921=CARTESIAN_POINT('Ctrl Pts',(0.443354135738027,54.0360411598537,-1.09113475029357));
#42922=CARTESIAN_POINT('Ctrl Pts',(0.426018833533182,54.0372897611191,-1.09806646646584));
#42923=CARTESIAN_POINT('Ctrl Pts',(0.414693713260905,54.0380908266133,-1.10239337977651));
#42924=CARTESIAN_POINT('Ctrl Pts',(0.388371010323977,54.0399235558791,-1.11198723577751));
#42925=CARTESIAN_POINT('Ctrl Pts',(0.373329373250857,54.0409492750934,-1.11712706667121));
#42926=CARTESIAN_POINT('Ctrl Pts',(0.319456235713969,54.04456211242,-1.13432613821075));
#42927=CARTESIAN_POINT('Ctrl Pts',(0.280107927518546,54.0470902970624,-1.14467814619456));
#42928=CARTESIAN_POINT('Ctrl Pts',(0.154906839829029,54.055003386667,-1.17077231023223));
#42929=CARTESIAN_POINT('Ctrl Pts',(0.0678091864489637,54.0603401839508,
-1.17902679397471));
#42930=CARTESIAN_POINT('Ctrl Pts',(-0.0378399366511146,54.0671831874009,
-1.17728645156745));
#42931=CARTESIAN_POINT('Ctrl Pts',(-0.0562710430862497,54.0683894806049,
-1.17654951407345));
#42932=CARTESIAN_POINT('Ctrl Pts',(-0.0857139400172132,54.0703405302249,
-1.17467889257891));
#42933=CARTESIAN_POINT('Ctrl Pts',(-0.0967406618192752,54.0710766219033,
-1.17382222267476));
#42934=CARTESIAN_POINT('Ctrl Pts',(-0.117824370854995,54.0724952218331,
-1.17188513142322));
#42935=CARTESIAN_POINT('Ctrl Pts',(-0.1278827478363,54.0731768677523,-1.17083019064873));
#42936=CARTESIAN_POINT('Ctrl Pts',(-0.151236721471257,54.0747714773031,
-1.16807626244645));
#42937=CARTESIAN_POINT('Ctrl Pts',(-0.16451914798825,54.07568743791,-1.16627960829197));
#42938=CARTESIAN_POINT('Ctrl Pts',(-0.20903954864328,54.0787893445294,-1.15948189565702));
#42939=CARTESIAN_POINT('Ctrl Pts',(-0.240103667940637,54.0810069530017,
-1.15344948000309));
#42940=CARTESIAN_POINT('Ctrl Pts',(-0.318762068102926,54.0867605798492,
-1.13485948723233));
#42941=CARTESIAN_POINT('Ctrl Pts',(-0.365878828505685,54.0903410072869,
-1.12055663477398));
#42942=CARTESIAN_POINT('Ctrl Pts',(-0.481249871133808,54.0993759852731,
-1.07748044935363));
#42943=CARTESIAN_POINT('Ctrl Pts',(-0.547953889721088,54.1048529763452,
-1.04513810374041));
#42944=CARTESIAN_POINT('Ctrl Pts',(-0.621361526312065,54.1109060948869,
-1.00057313229331));
#42945=CARTESIAN_POINT('Ctrl Pts',(-0.631442418895626,54.1117376620866,
-0.994242042129243));
#42946=CARTESIAN_POINT('Ctrl Pts',(-0.646937649859022,54.1130143064882,
-0.984179824575021));
#42947=CARTESIAN_POINT('Ctrl Pts',(-0.652419349300206,54.1134656328785,
-0.980554561363219));
#42948=CARTESIAN_POINT('Ctrl Pts',(-0.662626985096187,54.11430505645,-0.973680350341557));
#42949=CARTESIAN_POINT('Ctrl Pts',(-0.667359744904649,54.114693791915,-0.970442640431005));
#42950=CARTESIAN_POINT('Ctrl Pts',(-0.678705322247402,54.1156249069678,
-0.962558806067729));
#42951=CARTESIAN_POINT('Ctrl Pts',(-0.685294277562477,54.1161650456547,
-0.957878975610734));
#42952=CARTESIAN_POINT('Ctrl Pts',(-0.70893767622444,54.1181031128308,-0.940717309300394));
#42953=CARTESIAN_POINT('Ctrl Pts',(-0.725704601582507,54.119477274236,-0.927844084599255));
#42954=CARTESIAN_POINT('Ctrl Pts',(-0.76936795765327,54.12308220813,-0.892412247099435));
#42955=CARTESIAN_POINT('Ctrl Pts',(-0.795618617882556,54.125277781174,-0.869090335595293));
#42956=CARTESIAN_POINT('Ctrl Pts',(-0.886613703514892,54.1331534953056,
-0.780663561580546));
#42957=CARTESIAN_POINT('Ctrl Pts',(-0.944729291851585,54.1387334805242,
-0.709228374402788));
#42958=CARTESIAN_POINT('Ctrl Pts',(-1.00481623244013,54.145959319556,-0.61469414260531));
#42959=CARTESIAN_POINT('Ctrl Pts',(-1.01522867198601,54.1472785103206,-0.597340116843526));
#42960=CARTESIAN_POINT('Ctrl Pts',(-1.03086601720554,54.1493748299363,-0.569687069983775));
#42961=CARTESIAN_POINT('Ctrl Pts',(-1.03639561436579,54.1501410202253,-0.559564310671721));
#42962=CARTESIAN_POINT('Ctrl Pts',(-1.04645097994152,54.151583007999,-0.540495958099178));
#42963=CARTESIAN_POINT('Ctrl Pts',(-1.05101296456143,54.15225744378,-0.531570570760875));
#42964=CARTESIAN_POINT('Ctrl Pts',(-1.06103623641148,54.153786547287,-0.511326783209443));
#42965=CARTESIAN_POINT('Ctrl Pts',(-1.06643132925464,54.1546434279743,-0.499977172202175));
#42966=CARTESIAN_POINT('Ctrl Pts',(-1.08258753978806,54.1573189034295,-0.464537769734686));
#42967=CARTESIAN_POINT('Ctrl Pts',(-1.09272091758728,54.1591583261945,-0.440172608069373));
#42968=CARTESIAN_POINT('Ctrl Pts',(-1.11514324121102,54.1636503044806,-0.380700552506169));
#42969=CARTESIAN_POINT('Ctrl Pts',(-1.12660365050337,54.1663254443192,-0.345313111725471));
#42970=CARTESIAN_POINT('Ctrl Pts',(-1.16059464478777,54.1757412837487,-0.220488715912945));
#42971=CARTESIAN_POINT('Ctrl Pts',(-1.17428946966783,54.1826340072538,-0.128996109111037));
#42972=CARTESIAN_POINT('Ctrl Pts',(-1.17741520442044,54.1896916024278,-0.0291228858599911));
#42973=CARTESIAN_POINT('Ctrl Pts',(-1.17758086629596,54.1902340427651,-0.0214013192409408));
#42974=CARTESIAN_POINT('Ctrl Pts',(-1.17772387952764,54.1910933528807,-0.00908834702228301));
#42975=CARTESIAN_POINT('Ctrl Pts',(-1.1777503576629,54.1914124590411,-0.00449788311559384));
#42976=CARTESIAN_POINT('Ctrl Pts',(-1.17774999635204,54.1917302397619,9.26971843876522E-5));
#42977=CARTESIAN_POINT('Ctrl Pts',(0.188938462403164,54.3284116054606,1.16249615910106));
#42978=CARTESIAN_POINT('Ctrl Pts',(0.142620439045754,54.3252454416958,1.17002414622273));
#42979=CARTESIAN_POINT('Ctrl Pts',(0.0958081067186543,54.3220792779311,
1.17478673301896));
#42980=CARTESIAN_POINT('Ctrl Pts',(0.0488592103140385,54.3189131141663,
1.17673609618618));
#42981=CARTESIAN_POINT('Ctrl Pts',(0.00192930161990609,54.3157482309045,
1.17868467096547));
#42982=CARTESIAN_POINT('Ctrl Pts',(-0.045136504388877,54.3125833476426,
1.17782225392417));
#42983=CARTESIAN_POINT('Ctrl Pts',(-0.0919770848434641,54.3094184643808,
1.17415300466494));
#42984=CARTESIAN_POINT('Ctrl Pts',(-0.138855738355257,54.3062510086321,
1.17048077295896));
#42985=CARTESIAN_POINT('Ctrl Pts',(-0.185508242064195,54.3030835528833,
1.16399718778063));
#42986=CARTESIAN_POINT('Ctrl Pts',(-0.231577150488323,54.2999160971346,
1.15475845347489));
#42987=CARTESIAN_POINT('Ctrl Pts',(-0.277662214602198,54.2967475306056,
1.14551647928067));
#42988=CARTESIAN_POINT('Ctrl Pts',(-0.323162732754152,54.2935789640766,
1.13351756687537));
#42989=CARTESIAN_POINT('Ctrl Pts',(-0.367733709969507,54.2904103975476,
1.11886861652835));
#42990=CARTESIAN_POINT('Ctrl Pts',(-0.41239551487649,54.2872353740459,1.10418981423668));
#42991=CARTESIAN_POINT('Ctrl Pts',(-0.456123470704711,54.2840603505442,
1.08685038516034));
#42992=CARTESIAN_POINT('Ctrl Pts',(-0.498591310827326,54.2808853270425,
1.06700598277024));
#42993=CARTESIAN_POINT('Ctrl Pts',(-0.538836880772404,54.2778764471455,
1.04820000436156));
#42994=CARTESIAN_POINT('Ctrl Pts',(-0.577950596968587,54.2748675672485,
1.02714495758135));
#42995=CARTESIAN_POINT('Ctrl Pts',(-0.615678010633159,54.2718586873515,
1.00400978567083));
#42996=CARTESIAN_POINT('Ctrl Pts',(-0.657146956306185,54.2685514085093,
0.978580234744731));
#42997=CARTESIAN_POINT('Ctrl Pts',(-0.697135041118901,54.265244129667,0.950517495602211));
#42998=CARTESIAN_POINT('Ctrl Pts',(-0.735290338731114,54.2619368508247,
0.920023467238028));
#42999=CARTESIAN_POINT('Ctrl Pts',(-0.771863516366453,54.2587667092151,
0.890793882200711));
#43000=CARTESIAN_POINT('Ctrl Pts',(-0.806752426714082,54.2555965676055,
0.859331067332825));
#43001=CARTESIAN_POINT('Ctrl Pts',(-0.839674531761361,54.2524264259959,
0.825858185895944));
#43002=CARTESIAN_POINT('Ctrl Pts',(-0.872563586789607,54.249259466845,0.792418907394446));
#43003=CARTESIAN_POINT('Ctrl Pts',(-0.903489354314715,54.2460925076942,
0.756973952151734));
#43004=CARTESIAN_POINT('Ctrl Pts',(-0.932203886321935,54.2429255485433,
0.719785368583081));
#43005=CARTESIAN_POINT('Ctrl Pts',(-0.960902280072749,54.2397603692995,
0.682617685891267));
#43006=CARTESIAN_POINT('Ctrl Pts',(-0.987391559186291,54.2365951900557,
0.643708757115702));
#43007=CARTESIAN_POINT('Ctrl Pts',(-1.01146387124962,54.2334300108119,0.603353875977221));
#43008=CARTESIAN_POINT('Ctrl Pts',(-1.03553329001047,54.2302652119977,0.56300384517789));
#43009=CARTESIAN_POINT('Ctrl Pts',(-1.05718603420786,54.2271004131836,0.521208687330514));
#43010=CARTESIAN_POINT('Ctrl Pts',(-1.07625891199395,54.2239356143694,0.478290515119833));
#43011=CARTESIAN_POINT('Ctrl Pts',(-1.09535123507961,54.2207675889598,0.435328586705968));
#43012=CARTESIAN_POINT('Ctrl Pts',(-1.11185821763891,54.2175995635501,0.391241871058178));
#43013=CARTESIAN_POINT('Ctrl Pts',(-1.12566461737596,54.2144315381405,0.34637296616197));
#43014=CARTESIAN_POINT('Ctrl Pts',(-1.13947937780136,54.2112615942819,0.301476890175686));
#43015=CARTESIAN_POINT('Ctrl Pts',(-1.15059016927694,54.2080916504233,0.255798225177934));
#43016=CARTESIAN_POINT('Ctrl Pts',(-1.15893246591963,54.2049217065648,0.209691683043087));
#43017=CARTESIAN_POINT('Ctrl Pts',(-1.16729001659346,54.20174596641,0.163500834312681));
#43018=CARTESIAN_POINT('Ctrl Pts',(-1.17286891050182,54.1985702262552,0.116881101938893));
#43019=CARTESIAN_POINT('Ctrl Pts',(-1.17565645391774,54.1953944861004,0.0701923419010722));
#43020=CARTESIAN_POINT('Ctrl Pts',(-1.17650802651979,54.1944243224461,0.0559292927071424));
#43021=CARTESIAN_POINT('Ctrl Pts',(-1.17709946320061,54.1934541587918,0.0416597915932341));
#43022=CARTESIAN_POINT('Ctrl Pts',(-1.17743136929669,54.1924839951374,0.0273940339511899));
#43023=CARTESIAN_POINT('Ctrl Pts',(-1.17764246586402,54.1918669585129,0.0183208276915143));
#43024=CARTESIAN_POINT('Ctrl Pts',(-1.17774868810365,54.1912499218884,0.00924517196348502));
#43025=CARTESIAN_POINT('Ctrl Pts',(-1.17774998792321,54.1906328852639,0.000168662017078135));
#43026=CARTESIAN_POINT('',(-1.17774941770936,54.2897919344015,-0.00103887450448897));
#43027=CARTESIAN_POINT('Ctrl Pts',(0.188938462297913,54.4261253209981,1.16249615911817));
#43028=CARTESIAN_POINT('Ctrl Pts',(0.185376180620387,54.425873397806,1.16307513051274));
#43029=CARTESIAN_POINT('Ctrl Pts',(0.181811144134491,54.425622229853,1.16363774305742));
#43030=CARTESIAN_POINT('Ctrl Pts',(0.171047631672032,54.4248668821963,1.16528570060094));
#43031=CARTESIAN_POINT('Ctrl Pts',(0.163841499062352,54.4243651883774,1.16632072195973));
#43032=CARTESIAN_POINT('Ctrl Pts',(0.15101447896241,54.423479828719,1.16804184246133));
#43033=CARTESIAN_POINT('Ctrl Pts',(0.145397663283163,54.4230947836953,1.16875431203914));
#43034=CARTESIAN_POINT('Ctrl Pts',(0.132700621743155,54.4222303119995,1.17027192436718));
#43035=CARTESIAN_POINT('Ctrl Pts',(0.125617954789526,54.4217521811564,1.17105335826282));
#43036=CARTESIAN_POINT('Ctrl Pts',(0.103484336285499,54.4202695266035,1.1732922459694));
#43037=CARTESIAN_POINT('Ctrl Pts',(0.0884114918252079,54.419276450186,1.17452422811808));
#43038=CARTESIAN_POINT('Ctrl Pts',(0.0518891585044232,54.4169012084991,
1.1768022649539));
#43039=CARTESIAN_POINT('Ctrl Pts',(0.0304262537657303,54.4155311560299,
1.17755271824888));
#43040=CARTESIAN_POINT('Ctrl Pts',(-0.0650964392275349,54.4095016859618,
1.17827893604401));
#43041=CARTESIAN_POINT('Ctrl Pts',(-0.139037098298981,54.4050066306922,
1.17185685984141));
#43042=CARTESIAN_POINT('Ctrl Pts',(-0.260121184046763,54.3973314172581,
1.14971140316739));
#43043=CARTESIAN_POINT('Ctrl Pts',(-0.307751589403153,54.3942302627828,
1.1378872943589));
#43044=CARTESIAN_POINT('Ctrl Pts',(-0.369425438285785,54.3900159468323,
1.1184206564918));
#43045=CARTESIAN_POINT('Ctrl Pts',(-0.38425168999655,54.3889874537364,1.11341390332088));
#43046=CARTESIAN_POINT('Ctrl Pts',(-0.407862428420751,54.3873224371346,
1.10491292101191));
#43047=CARTESIAN_POINT('Ctrl Pts',(-0.416712554673629,54.3866921232087,
1.10160562882828));
#43048=CARTESIAN_POINT('Ctrl Pts',(-0.435074383660631,54.3853708587132,
1.09449088486819));
#43049=CARTESIAN_POINT('Ctrl Pts',(-0.444578073351309,54.3846793375231,
1.09066509136458));
#43050=CARTESIAN_POINT('Ctrl Pts',(-0.467201290406765,54.3830141593227,
1.081213101225));
#43051=CARTESIAN_POINT('Ctrl Pts',(-0.480270527937359,54.3820366636617,
1.07547152662546));
#43052=CARTESIAN_POINT('Ctrl Pts',(-0.527927316456104,54.3784130333616,
1.05349306064364));
#43053=CARTESIAN_POINT('Ctrl Pts',(-0.561820055704959,54.3757186155543,
1.03581491958072));
#43054=CARTESIAN_POINT('Ctrl Pts',(-0.654628921373838,54.3680053718203,
0.981510318193043));
#43055=CARTESIAN_POINT('Ctrl Pts',(-0.711254551174165,54.3628881865809,
0.94128473991522));
#43056=CARTESIAN_POINT('Ctrl Pts',(-0.800625837446264,54.354279080706,0.865105996390099));
#43057=CARTESIAN_POINT('Ctrl Pts',(-0.835300330812887,54.3507797944047,
0.831675681964896));
#43058=CARTESIAN_POINT('Ctrl Pts',(-0.874820721918252,54.3466785023147,
0.788600366502111));
#43059=CARTESIAN_POINT('Ctrl Pts',(-0.881706122671819,54.3459594715222,
0.780894464870655));
#43060=CARTESIAN_POINT('Ctrl Pts',(-0.8925398794021,54.3448222253155,0.768443686994296));
#43061=CARTESIAN_POINT('Ctrl Pts',(-0.896553730750785,54.3443995462266,
0.76375686490986));
#43062=CARTESIAN_POINT('Ctrl Pts',(-0.904342679677277,54.3435770595897,
0.754515980927527));
#43063=CARTESIAN_POINT('Ctrl Pts',(-0.908120615428342,54.3431770737615,
0.749964664452561));
#43064=CARTESIAN_POINT('Ctrl Pts',(-0.917636548614925,54.3421663367944,
0.738323380282736));
#43065=CARTESIAN_POINT('Ctrl Pts',(-0.923326923162854,54.3415588634717,
0.731194676570492));
#43066=CARTESIAN_POINT('Ctrl Pts',(-0.947539097564128,54.3389570901951,
0.700129061481728));
#43067=CARTESIAN_POINT('Ctrl Pts',(-0.965218758468685,54.3370131589482,
0.675547280251889));
#43068=CARTESIAN_POINT('Ctrl Pts',(-1.0189961486538,54.3308555319913,0.594346247301076));
#43069=CARTESIAN_POINT('Ctrl Pts',(-1.05120880700349,54.3267656687287,0.535314481664691));
#43070=CARTESIAN_POINT('Ctrl Pts',(-1.10103455299137,54.319077839153,0.421940641612684));
#43071=CARTESIAN_POINT('Ctrl Pts',(-1.12006903322628,54.3155129273234,0.368449771993778));
#43072=CARTESIAN_POINT('Ctrl Pts',(-1.13944798249799,54.3107777752394,0.298346159102283));
#43073=CARTESIAN_POINT('Ctrl Pts',(-1.14340375145628,54.3097247232611,0.282807277058497));
#43074=CARTESIAN_POINT('Ctrl Pts',(-1.14943919471797,54.3079605003848,0.25689754720494));
#43075=CARTESIAN_POINT('Ctrl Pts',(-1.15169865576376,54.3072551504005,0.246570488969655));
#43076=CARTESIAN_POINT('Ctrl Pts',(-1.15589418702773,54.3058504427375,0.226076918112123));
#43077=CARTESIAN_POINT('Ctrl Pts',(-1.15783587598494,54.3051513347103,0.215912521342131));
#43078=CARTESIAN_POINT('Ctrl Pts',(-1.16144923896333,54.3037451184607,0.195544409158177));
#43079=CARTESIAN_POINT('Ctrl Pts',(-1.16312098032593,54.3030380800881,0.185341640790745));
#43080=CARTESIAN_POINT('Ctrl Pts',(-1.16791037441324,54.3008219676272,0.153488878645139));
#43081=CARTESIAN_POINT('Ctrl Pts',(-1.17055923453074,54.2992985452284,0.131774227760274));
#43082=CARTESIAN_POINT('Ctrl Pts',(-1.17606481781418,54.2951455311782,0.0730844106249806));
#43083=CARTESIAN_POINT('Ctrl Pts',(-1.17778227202827,54.2924850287514,0.0360301381678281));
#43084=CARTESIAN_POINT('Ctrl Pts',(-1.17774954090924,54.2897920753539,-0.00103989810314145));
#43085=CARTESIAN_POINT('Ctrl Pts',(-1.17774954179877,54.2897921485752,-0.00103889017059593));
#43086=CARTESIAN_POINT('Ctrl Pts',(-1.17766684091552,54.2829813318646,-0.0947936778329939));
#43087=CARTESIAN_POINT('Ctrl Pts',(-1.1663900290375,54.2759661228186,-0.188203459049912));
#43088=CARTESIAN_POINT('Ctrl Pts',(-1.14237450165133,54.2687959593206,-0.286586760639395));
#43089=CARTESIAN_POINT('Ctrl Pts',(-1.14052361246705,54.2682669717101,-0.293866243541163));
#43090=CARTESIAN_POINT('Ctrl Pts',(-1.13614211928704,54.2670673336474,-0.310433240325928));
#43091=CARTESIAN_POINT('Ctrl Pts',(-1.13356699041024,54.2663987622565,-0.319708625680141));
#43092=CARTESIAN_POINT('Ctrl Pts',(-1.12919717017598,54.2653220718467,-0.334731299165248));
#43093=CARTESIAN_POINT('Ctrl Pts',(-1.12747167895214,54.2649102485041,-0.340498031226404));
#43094=CARTESIAN_POINT('Ctrl Pts',(-1.1241393656601,54.2641397040794,-0.35133175256226));
#43095=CARTESIAN_POINT('Ctrl Pts',(-1.12254231801381,54.2637804142805,-0.356401544458406));
#43096=CARTESIAN_POINT('Ctrl Pts',(-1.11813723377616,54.262815385421,-0.370061979057247));
#43097=CARTESIAN_POINT('Ctrl Pts',(-1.11526448272629,54.2622132850362,-0.378631599320267));
#43098=CARTESIAN_POINT('Ctrl Pts',(-1.10342494296863,54.2598334486448,-0.412645394256968));
#43099=CARTESIAN_POINT('Ctrl Pts',(-1.09368310167419,54.2580948566247,-0.437813139174948));
#43100=CARTESIAN_POINT('Ctrl Pts',(-1.05510173312101,54.2518609394231,-0.528138544164643));
#43101=CARTESIAN_POINT('Ctrl Pts',(-1.02123117189314,54.2475273420223,-0.590980661936369));
#43102=CARTESIAN_POINT('Ctrl Pts',(-0.961055019743536,54.2407605611066,
-0.681829436866348));
#43103=CARTESIAN_POINT('Ctrl Pts',(-0.938725412642028,54.2383983666429,
-0.712258684004632));
#43104=CARTESIAN_POINT('Ctrl Pts',(-0.898199303641413,54.2342880710835,
-0.762261748981371));
#43105=CARTESIAN_POINT('Ctrl Pts',(-0.880726642250142,54.2325647806703,
-0.782384417056916));
#43106=CARTESIAN_POINT('Ctrl Pts',(-0.854002632016679,54.2299852158688,
-0.811131032601916));
#43107=CARTESIAN_POINT('Ctrl Pts',(-0.845270117624524,54.2291505713396,
-0.820227075453378));
#43108=CARTESIAN_POINT('Ctrl Pts',(-0.829400471246059,54.2276470829838,
-0.836234764193481));
#43109=CARTESIAN_POINT('Ctrl Pts',(-0.822318654173583,54.2269807031806,
-0.84319970536502));
#43110=CARTESIAN_POINT('Ctrl Pts',(-0.806874662474305,54.225536579457,-0.858009198911631));
#43111=CARTESIAN_POINT('Ctrl Pts',(-0.798484392739496,54.2247575953504,
-0.865822825192788));
#43112=CARTESIAN_POINT('Ctrl Pts',(-0.775211877175748,54.2226110936378,
-0.886869874276522));
#43113=CARTESIAN_POINT('Ctrl Pts',(-0.760106546535356,54.2212332743819,
-0.899849755267083));
#43114=CARTESIAN_POINT('Ctrl Pts',(-0.667105256393696,54.212836440318,-0.975751988598445));
#43115=CARTESIAN_POINT('Ctrl Pts',(-0.581783021004237,54.2054364599915,
-1.02890370264148));
#43116=CARTESIAN_POINT('Ctrl Pts',(-0.463442687413733,54.1959077763105,
-1.08315332096214));
#43117=CARTESIAN_POINT('Ctrl Pts',(-0.435621230752485,54.1937197578759,
-1.09463902671949));
#43118=CARTESIAN_POINT('Ctrl Pts',(-0.394944545698714,54.1906203665715,
-1.10963497540972));
#43119=CARTESIAN_POINT('Ctrl Pts',(-0.382422978309536,54.189679564969,-1.11401241925848));
#43120=CARTESIAN_POINT('Ctrl Pts',(-0.359791593604102,54.1880060280508,
-1.12149759494009));
#43121=CARTESIAN_POINT('Ctrl Pts',(-0.349708896500555,54.1872698815079,
-1.12468242348174));
#43122=CARTESIAN_POINT('Ctrl Pts',(-0.333626868984732,54.1861121242617,
-1.12952506973644));
#43123=CARTESIAN_POINT('Ctrl Pts',(-0.327655197976916,54.1856857809238,
-1.13127178282946));
#43124=CARTESIAN_POINT('Ctrl Pts',(-0.31607999346285,54.1848666231083,-1.13455818043361));
#43125=CARTESIAN_POINT('Ctrl Pts',(-0.310478467253568,54.1844735047832,
-1.13610384661864));
#43126=CARTESIAN_POINT('Ctrl Pts',(-0.296283030140477,54.183485060024,-1.13990805761707));
#43127=CARTESIAN_POINT('Ctrl Pts',(-0.287674346371837,54.1828928142294,
-1.14211098242077));
#43128=CARTESIAN_POINT('Ctrl Pts',(-0.25415706300348,54.1806118060129,-1.15028487721212));
#43129=CARTESIAN_POINT('Ctrl Pts',(-0.229079475087171,54.1789581570558,
-1.15554053134203));
#43130=CARTESIAN_POINT('Ctrl Pts',(-0.13964001280887,54.1731830561818,-1.17125820342098));
#43131=CARTESIAN_POINT('Ctrl Pts',(-0.0746014270614816,54.1692011175891,
-1.17719194484021));
#43132=CARTESIAN_POINT('Ctrl Pts',(0.0539657533508229,54.1612410239696,
-1.17821837426728));
#43133=CARTESIAN_POINT('Ctrl Pts',(0.117263823350239,54.1572777906625,-1.17360923435909));
#43134=CARTESIAN_POINT('Ctrl Pts',(0.195924385368334,54.1520983672329,-1.16145266021968));
#43135=CARTESIAN_POINT('Ctrl Pts',(0.211915515601254,54.1510324683352,-1.15864162656984));
#43136=CARTESIAN_POINT('Ctrl Pts',(0.238253429830621,54.1492526834866,-1.15344829117014));
#43137=CARTESIAN_POINT('Ctrl Pts',(0.248635523393368,54.1485448410872,-1.15125497662715));
#43138=CARTESIAN_POINT('Ctrl Pts',(0.268937176917575,54.1471476578462,-1.1466786424988));
#43139=CARTESIAN_POINT('Ctrl Pts',(0.278858226687779,54.1464587199321,-1.14430642412277));
#43140=CARTESIAN_POINT('Ctrl Pts',(0.30067598604148,54.1449294797133,-1.13878901308675));
#43141=CARTESIAN_POINT('Ctrl Pts',(0.31255660328995,54.1440873680379,-1.13558567026202));
#43142=CARTESIAN_POINT('Ctrl Pts',(0.353973788409239,54.1411176660096,-1.12371927867764));
#43143=CARTESIAN_POINT('Ctrl Pts',(0.383216833466279,54.1389594169493,-1.11408573264574));
#43144=CARTESIAN_POINT('Ctrl Pts',(0.499769225508402,54.1301042297346,-1.07055792370054));
#43145=CARTESIAN_POINT('Ctrl Pts',(0.583265935471028,54.1231377960992,-1.02745337010706));
#43146=CARTESIAN_POINT('Ctrl Pts',(0.689305087021913,54.1138175285663,-0.955584866996923));
#43147=CARTESIAN_POINT('Ctrl Pts',(0.71698698016554,54.1113384961397,-0.934994154527784));
#43148=CARTESIAN_POINT('Ctrl Pts',(0.751068920691356,54.1082630616596,-0.907237663355813));
#43149=CARTESIAN_POINT('Ctrl Pts',(0.758338092624326,54.1076057253709,-0.90117037967133));
#43150=CARTESIAN_POINT('Ctrl Pts',(0.770082427739315,54.1065425021058,-0.891125101673072));
#43151=CARTESIAN_POINT('Ctrl Pts',(0.774601685184035,54.1061330725899,-0.887199597852913));
#43152=CARTESIAN_POINT('Ctrl Pts',(0.783650995858205,54.1053129763408,-0.879217352055635));
#43153=CARTESIAN_POINT('Ctrl Pts',(0.788179936488669,54.1049023953061,-0.875159658234565));
#43154=CARTESIAN_POINT('Ctrl Pts',(0.800009067356065,54.1038289723818,-0.864395061591423));
#43155=CARTESIAN_POINT('Ctrl Pts',(0.807256534274497,54.103170262677,-0.857630593220265));
#43156=CARTESIAN_POINT('Ctrl Pts',(0.841554027662472,54.1000428784993,-0.824798772921333));
#43157=CARTESIAN_POINT('Ctrl Pts',(0.867434589949899,54.0976519162422,-0.797536212529927));
#43158=CARTESIAN_POINT('Ctrl Pts',(0.9429108036744,54.0904066028501,-0.709999835004306));
#43159=CARTESIAN_POINT('Ctrl Pts',(0.987856007182956,54.0856772664437,-0.646004340862252));
#43160=CARTESIAN_POINT('Ctrl Pts',(1.04592810268671,54.0782430386011,-0.542912814058478));
#43161=CARTESIAN_POINT('Ctrl Pts',(1.06389392214581,54.0756722397325,-0.506802858592426));
#43162=CARTESIAN_POINT('Ctrl Pts',(1.08576355994835,54.0720897232812,-0.456533998775625));
#43163=CARTESIAN_POINT('Ctrl Pts',(1.09130798818531,54.0711333354787,-0.443116964730434));
#43164=CARTESIAN_POINT('Ctrl Pts',(1.10035491472776,54.0694849719163,-0.420023729354373));
#43165=CARTESIAN_POINT('Ctrl Pts',(1.10398126968591,54.0687972263755,-0.41039763192229));
#43166=CARTESIAN_POINT('Ctrl Pts',(1.11110790112933,54.0673880949221,-0.390701834518759));
#43167=CARTESIAN_POINT('Ctrl Pts',(1.11459846428922,54.0666664613536,-0.380629664893257));
#43168=CARTESIAN_POINT('Ctrl Pts',(1.12313604720909,54.0648175466932,-0.354869065656975));
#43169=CARTESIAN_POINT('Ctrl Pts',(1.12799123046387,54.0636841156419,-0.339119993665832));
#43170=CARTESIAN_POINT('Ctrl Pts',(1.1502918907072,54.0580437115446,-0.260995113513728));
#43171=CARTESIAN_POINT('Ctrl Pts',(1.16289920877347,54.0533851067073,-0.197364897798639));
#43172=CARTESIAN_POINT('Ctrl Pts',(1.17699257633227,54.0442578329297,-0.0733914807488738));
#43173=CARTESIAN_POINT('Ctrl Pts',(1.1792033450439,54.0398149814453,-0.0133214262186355));
#43174=CARTESIAN_POINT('Ctrl Pts',(1.17568826191117,54.0333922515329,0.0753414138674756));
#43175=CARTESIAN_POINT('Ctrl Pts',(1.17350244581044,54.0313397903894,0.103978449477455));
#43176=CARTESIAN_POINT('Ctrl Pts',(1.1692629829283,54.0287078179411,0.141419778756764));
#43177=CARTESIAN_POINT('Ctrl Pts',(1.16815228031532,54.0280861143389,0.150318792941377));
#43178=CARTESIAN_POINT('Ctrl Pts',(1.16614455091309,54.0270653480333,0.165035075587939));
#43179=CARTESIAN_POINT('Ctrl Pts',(1.16530538651811,54.026663247275,0.170859742831504));
#43180=CARTESIAN_POINT('Ctrl Pts',(1.16349015208585,54.0258416113948,0.182823305420444));
#43181=CARTESIAN_POINT('Ctrl Pts',(1.16250908525541,54.0254223507497,0.188961176377939));
#43182=CARTESIAN_POINT('Ctrl Pts',(1.15973282558278,54.0242987772188,0.205489697610148));
#43183=CARTESIAN_POINT('Ctrl Pts',(1.15784656610734,54.0235993191851,0.215864751958692));
#43184=CARTESIAN_POINT('Ctrl Pts',(1.14450010534135,54.0190319640173,0.284057500630192));
#43185=CARTESIAN_POINT('Ctrl Pts',(1.12885120561852,54.015359904426,0.340977859062479));
#43186=CARTESIAN_POINT('Ctrl Pts',(1.08881848858547,54.0080013848744,0.452950587783391));
#43187=CARTESIAN_POINT('Ctrl Pts',(1.06435286590403,54.004324796566,0.507782009041369));
#43188=CARTESIAN_POINT('Ctrl Pts',(1.02390986872504,53.9989663945658,0.58252028165588));
#43189=CARTESIAN_POINT('Ctrl Pts',(1.01130238315197,53.9973725703271,0.604142920148731));
#43190=CARTESIAN_POINT('Ctrl Pts',(0.987464309694042,53.9944731696427,0.642187080362546));
#43191=CARTESIAN_POINT('Ctrl Pts',(0.976488242108731,53.9931762966754,0.658756895579183));
#43192=CARTESIAN_POINT('Ctrl Pts',(0.958595343158618,53.9911146143098,0.684338201931109));
#43193=CARTESIAN_POINT('Ctrl Pts',(0.951958122199495,53.9903603577457,0.693541292910036));
#43194=CARTESIAN_POINT('Ctrl Pts',(0.939196171379517,53.9889286171827,0.710708463925178));
#43195=CARTESIAN_POINT('Ctrl Pts',(0.933100454427328,53.9882523063521,0.718692910865464));
#43196=CARTESIAN_POINT('Ctrl Pts',(0.918978696362175,53.9867018720004,0.73670769146736));
#43197=CARTESIAN_POINT('Ctrl Pts',(0.910889307869518,53.9858252731211,0.746686489040031));
#43198=CARTESIAN_POINT('Ctrl Pts',(0.884614915766755,53.9830128911505,0.778035226371346));
#43199=CARTESIAN_POINT('Ctrl Pts',(0.865829942521421,53.9810530534614,0.798887128126904));
#43200=CARTESIAN_POINT('Ctrl Pts',(0.780107538218032,53.9723202302185,0.887463923732712));
#43201=CARTESIAN_POINT('Ctrl Pts',(0.705848335542372,53.9652484666891,0.947593454916767));
#43202=CARTESIAN_POINT('Ctrl Pts',(0.603676655810445,53.9564581320075,1.01158955078941));
#43203=CARTESIAN_POINT('Ctrl Pts',(0.581741326487007,53.9546221720533,1.0243613155366));
#43204=CARTESIAN_POINT('Ctrl Pts',(0.54443428749037,53.9516021305551,1.04449794274336));
#43205=CARTESIAN_POINT('Ctrl Pts',(0.529284876625989,53.9504029155016,1.05225578555052));
#43206=CARTESIAN_POINT('Ctrl Pts',(0.507264262148917,53.9487037660767,1.06293631269729));
#43207=CARTESIAN_POINT('Ctrl Pts',(0.500525828748918,53.9481896258823,1.06612594879634));
#43208=CARTESIAN_POINT('Ctrl Pts',(0.489102329775422,53.9473283332711,1.07140107492384));
#43209=CARTESIAN_POINT('Ctrl Pts',(0.484433288588264,53.9469792036017,1.07352025828005));
#43210=CARTESIAN_POINT('Ctrl Pts',(0.473621154818626,53.9461774718036,1.07834275796754));
#43211=CARTESIAN_POINT('Ctrl Pts',(0.467468596476372,53.9457261818297,1.08102415272247));
#43212=CARTESIAN_POINT('Ctrl Pts',(0.449735310626134,53.9444386031246,1.08857292173314));
#43213=CARTESIAN_POINT('Ctrl Pts',(0.43809880857781,53.9436096895887,1.09330797151054));
#43214=CARTESIAN_POINT('Ctrl Pts',(0.36689497933504,53.9386210636272,1.12096229853187));
#43215=CARTESIAN_POINT('Ctrl Pts',(0.305614416407989,53.9346761907162,1.13919717808827));
#43216=CARTESIAN_POINT('Ctrl Pts',(0.225156811893909,53.9295965595726,1.15617373162336));
#43217=CARTESIAN_POINT('Ctrl Pts',(0.207080778897662,53.9284619713002,1.15954752079153));
#43218=CARTESIAN_POINT('Ctrl Pts',(0.188938426235786,53.9273245270844,1.16249616497928));
#43219=CARTESIAN_POINT('Origin',(0.,56.5393671147362,0.));
#43220=CARTESIAN_POINT('',(0.188938471457153,53.3292711974063,1.16249615762954));
#43221=CARTESIAN_POINT('',(0.188938462305883,53.4282524383066,1.16249615911688));
#43222=CARTESIAN_POINT('',(0.188938462403162,56.5393671147362,1.16249615910107));
#43223=CARTESIAN_POINT('Ctrl Pts',(0.188938471457153,53.3292711974063,1.16249615762954));
#43224=CARTESIAN_POINT('Ctrl Pts',(0.272122176233244,53.3345992990564,1.14897645528266));
#43225=CARTESIAN_POINT('Ctrl Pts',(0.353630912953478,53.3396895031084,1.12656498632061));
#43226=CARTESIAN_POINT('Ctrl Pts',(0.471501764327728,53.347635044798,1.08008256925056));
#43227=CARTESIAN_POINT('Ctrl Pts',(0.510067277097042,53.3503336029397,1.06241379436842));
#43228=CARTESIAN_POINT('Ctrl Pts',(0.560646753858215,53.3540648695701,1.03585117118685));
#43229=CARTESIAN_POINT('Ctrl Pts',(0.573569293663219,53.3550357150435,1.0287519938264));
#43230=CARTESIAN_POINT('Ctrl Pts',(0.595312332050345,53.3567013656372,1.0162701272162));
#43231=CARTESIAN_POINT('Ctrl Pts',(0.604201671546006,53.3573917132986,1.01101042163278));
#43232=CARTESIAN_POINT('Ctrl Pts',(0.62207509894178,53.3587995423826,1.00011503653056));
#43233=CARTESIAN_POINT('Ctrl Pts',(0.631054520963015,53.3595171898599,0.994473576190354));
#43234=CARTESIAN_POINT('Ctrl Pts',(0.653548625453581,53.3613420287866,0.979913980767344));
#43235=CARTESIAN_POINT('Ctrl Pts',(0.666957465273019,53.3624550487913,0.970837220814244));
#43236=CARTESIAN_POINT('Ctrl Pts',(0.727329550561807,53.3675856572018,0.928128862192147));
#43237=CARTESIAN_POINT('Ctrl Pts',(0.77195987142941,53.3717214396069,0.891351588655386));
#43238=CARTESIAN_POINT('Ctrl Pts',(0.861436492330174,53.380743753696,0.805841687629467));
#43239=CARTESIAN_POINT('Ctrl Pts',(0.905244603161678,53.385638736311,0.756297388110092));
#43240=CARTESIAN_POINT('Ctrl Pts',(0.96261345677392,53.3926013877805,0.679244526714454));
#43241=CARTESIAN_POINT('Ctrl Pts',(0.979629330804129,53.3947524006647,0.65446504434324));
#43242=CARTESIAN_POINT('Ctrl Pts',(1.00053887171359,53.3974880734876,0.621369277726854));
#43243=CARTESIAN_POINT('Ctrl Pts',(1.00530854957296,53.3981189813882,0.613622478583465));
#43244=CARTESIAN_POINT('Ctrl Pts',(1.01302875683458,53.3991507465524,0.600751813210578));
#43245=CARTESIAN_POINT('Ctrl Pts',(1.01603125284886,53.3995547702384,0.595659720032469));
#43246=CARTESIAN_POINT('Ctrl Pts',(1.02209413131163,53.4003759925294,0.585198120890406));
#43247=CARTESIAN_POINT('Ctrl Pts',(1.02515081279963,53.4007929669845,0.579826758073099));
#43248=CARTESIAN_POINT('Ctrl Pts',(1.03322417193726,53.4019029711945,0.56537638825406));
#43249=CARTESIAN_POINT('Ctrl Pts',(1.03816355853133,53.4025913479283,0.556254522659361));
#43250=CARTESIAN_POINT('Ctrl Pts',(1.06691100482759,53.4066615852118,0.501447702315244));
#43251=CARTESIAN_POINT('Ctrl Pts',(1.08782407739506,53.40989443696,0.454300513866112));
#43252=CARTESIAN_POINT('Ctrl Pts',(1.12108297267133,53.4158838622824,0.363717164501314));
#43253=CARTESIAN_POINT('Ctrl Pts',(1.13415164373756,53.4186438147476,0.320651345897277));
#43254=CARTESIAN_POINT('Ctrl Pts',(1.15346907795142,53.4237473418666,0.24080418526473));
#43255=CARTESIAN_POINT('Ctrl Pts',(1.16049551032288,53.4260770541502,0.204272977605751));
#43256=CARTESIAN_POINT('Ctrl Pts',(1.16953393380883,53.4301377455298,0.14135622124496));
#43257=CARTESIAN_POINT('Ctrl Pts',(1.17240682712747,53.4318447750953,0.115122852564769));
#43258=CARTESIAN_POINT('Ctrl Pts',(1.1753439744265,53.4344048898237,0.0762858000488357));
#43259=CARTESIAN_POINT('Ctrl Pts',(1.1760909993527,53.4352368382902,0.0637410578943533));
#43260=CARTESIAN_POINT('Ctrl Pts',(1.17707277358854,53.4367437142993,0.0411730522257568));
#43261=CARTESIAN_POINT('Ctrl Pts',(1.17738054494792,53.4374162907847,0.0311540722878727));
#43262=CARTESIAN_POINT('Ctrl Pts',(1.17776735006515,53.4388715203704,0.00960038712419998));
#43263=CARTESIAN_POINT('Ctrl Pts',(1.17780488269599,53.4396554034839,-0.00193391429791517));
#43264=CARTESIAN_POINT('Ctrl Pts',(1.17744164016669,53.4418292146908,-0.033700084230902));
#43265=CARTESIAN_POINT('Ctrl Pts',(1.17668888010545,53.443229880684,-0.0539231191577857));
#43266=CARTESIAN_POINT('Ctrl Pts',(1.16858936821251,53.4522381478968,-0.18237491709975));
#43267=CARTESIAN_POINT('Ctrl Pts',(1.14683904003785,53.4603011077607,-0.289159778979795));
#43268=CARTESIAN_POINT('Ctrl Pts',(1.09872354760097,53.4708489978935,-0.425701765814891));
#43269=CARTESIAN_POINT('Ctrl Pts',(1.08506600892611,53.4734659236939,-0.459399284786602));
#43270=CARTESIAN_POINT('Ctrl Pts',(1.06585520517816,53.4766822709934,-0.501138687829624));
#43271=CARTESIAN_POINT('Ctrl Pts',(1.06173298685907,53.4773493246654,-0.509814066628288));
#43272=CARTESIAN_POINT('Ctrl Pts',(1.05485688357332,53.4784242687151,-0.523839866541042));
#43273=CARTESIAN_POINT('Ctrl Pts',(1.052167402681,53.4788358407283,-0.529221136903243));
#43274=CARTESIAN_POINT('Ctrl Pts',(1.04668983548114,53.4796561911237,-0.539974142309233));
#43275=CARTESIAN_POINT('Ctrl Pts',(1.04390134555481,53.4800649295153,-0.545345460215639));
#43276=CARTESIAN_POINT('Ctrl Pts',(1.03650166640205,53.4811273296619,-0.559334314833676));
#43277=CARTESIAN_POINT('Ctrl Pts',(1.03182429099254,53.4817770141004,-0.567916568078174));
#43278=CARTESIAN_POINT('Ctrl Pts',(1.0096743839441,53.4847593968217,-0.607380956792485));
#43279=CARTESIAN_POINT('Ctrl Pts',(0.99091719636382,53.4870229795918,-0.63752458781805));
#43280=CARTESIAN_POINT('Ctrl Pts',(0.925610335424598,53.4942689665555,-0.73261108350359));
#43281=CARTESIAN_POINT('Ctrl Pts',(0.873815855190618,53.4991052731634,-0.793675052818285));
#43282=CARTESIAN_POINT('Ctrl Pts',(0.786891554988415,53.5066783845719,-0.877242265770893));
#43283=CARTESIAN_POINT('Ctrl Pts',(0.756104247766958,53.5092737191256,-0.903912695655278));
#43284=CARTESIAN_POINT('Ctrl Pts',(0.712513635568641,53.5128849694348,-0.937886706854698));
#43285=CARTESIAN_POINT('Ctrl Pts',(0.700862312965438,53.5138443341537,-0.94662513335947));
#43286=CARTESIAN_POINT('Ctrl Pts',(0.680701840180331,53.515496366166,-0.961169126168438));
#43287=CARTESIAN_POINT('Ctrl Pts',(0.67227290828531,53.5161847580772,-0.96708335193797));
#43288=CARTESIAN_POINT('Ctrl Pts',(0.654969256897275,53.5175939318682,-0.978889055636462));
#43289=CARTESIAN_POINT('Ctrl Pts',(0.646090009504519,53.5183149456928,-0.984772155028817));
#43290=CARTESIAN_POINT('Ctrl Pts',(0.623316896738008,53.5201595687942,-0.99942030549462));
#43291=CARTESIAN_POINT('Ctrl Pts',(0.609317595911858,53.5212892674594,-1.00801632941558));
#43292=CARTESIAN_POINT('Ctrl Pts',(0.5395935567445,53.5268980044687,-1.04884595934508));
#43293=CARTESIAN_POINT('Ctrl Pts',(0.481478766636501,53.5315267741778,-1.07676129089872));
#43294=CARTESIAN_POINT('Ctrl Pts',(0.376051356931989,53.5397840076527,-1.1171558187886));
#43295=CARTESIAN_POINT('Ctrl Pts',(0.329689186797785,53.5433686889202,-1.13170524134979));
#43296=CARTESIAN_POINT('Ctrl Pts',(0.24467416959669,53.5497605181276,-1.15271538035918));
#43297=CARTESIAN_POINT('Ctrl Pts',(0.206340645603524,53.5525778105362,-1.16019065214295));
#43298=CARTESIAN_POINT('Ctrl Pts',(0.15802321779594,53.5559967426003,-1.16714153640258));
#43299=CARTESIAN_POINT('Ctrl Pts',(0.148325879528012,53.5566763002715,-1.16841351955232));
#43300=CARTESIAN_POINT('Ctrl Pts',(0.132602410435525,53.5577662551786,-1.17027701981836));
#43301=CARTESIAN_POINT('Ctrl Pts',(0.126585816008528,53.5581805167005,-1.17094309756986));
#43302=CARTESIAN_POINT('Ctrl Pts',(0.115296954872432,53.5589521921319,-1.17210482133907));
#43303=CARTESIAN_POINT('Ctrl Pts',(0.110026010116141,53.5593102126632,-1.17261135065402));
#43304=CARTESIAN_POINT('Ctrl Pts',(0.095869211128407,53.5602660900925,-1.17387549796522));
#43305=CARTESIAN_POINT('Ctrl Pts',(0.0869776545308116,53.5608604349539,
-1.17456778861695));
#43306=CARTESIAN_POINT('Ctrl Pts',(0.0522594913214459,53.5631606741977,
-1.17687449856718));
#43307=CARTESIAN_POINT('Ctrl Pts',(0.026388534705586,53.5648306990101,-1.17773872525583));
#43308=CARTESIAN_POINT('Ctrl Pts',(-0.08856760774046,53.5721384901364,-1.17778831877234));
#43309=CARTESIAN_POINT('Ctrl Pts',(-0.177364091779214,53.5775029464724,
-1.16772154689559));
#43310=CARTESIAN_POINT('Ctrl Pts',(-0.305542190075641,53.5857506853485,
-1.13821807438996));
#43311=CARTESIAN_POINT('Ctrl Pts',(-0.346354223354358,53.5884522341009,
-1.12646996967279));
#43312=CARTESIAN_POINT('Ctrl Pts',(-0.400372419152107,53.5921869724843,
-1.10770686869929));
#43313=CARTESIAN_POINT('Ctrl Pts',(-0.414211732449651,53.5931581412674,
-1.10260654343474));
#43314=CARTESIAN_POINT('Ctrl Pts',(-0.437574669955535,53.5948241761321,
-1.09349447698427));
#43315=CARTESIAN_POINT('Ctrl Pts',(-0.447148141338848,53.5955145796003,
-1.0896147443303));
#43316=CARTESIAN_POINT('Ctrl Pts',(-0.466442657689451,53.5969223750086,
-1.08149837502614));
#43317=CARTESIAN_POINT('Ctrl Pts',(-0.476159970997694,53.5976399311828,
-1.07725538163962));
#43318=CARTESIAN_POINT('Ctrl Pts',(-0.50056202684096,53.5994642321416,-1.066205733092));
#43319=CARTESIAN_POINT('Ctrl Pts',(-0.515165788622925,53.600576798437,-1.05922668609973));
#43320=CARTESIAN_POINT('Ctrl Pts',(-0.581017556140803,53.6056917609705,
-1.0260725713299));
#43321=CARTESIAN_POINT('Ctrl Pts',(-0.630441515002507,53.6098113730722,
-0.996467799001293));
#43322=CARTESIAN_POINT('Ctrl Pts',(-0.731652650436643,53.6188302216918,
-0.925290514198592));
#43323=CARTESIAN_POINT('Ctrl Pts',(-0.782497914598962,53.6237391554934,
-0.882708906811734));
#43324=CARTESIAN_POINT('Ctrl Pts',(-0.8508525149281,53.6307182917934,-0.81489270746091));
#43325=CARTESIAN_POINT('Ctrl Pts',(-0.871391574986299,53.6328721658634,
-0.792891655106744));
#43326=CARTESIAN_POINT('Ctrl Pts',(-0.897017799795665,53.6356108355229,
-0.763241079460414));
#43327=CARTESIAN_POINT('Ctrl Pts',(-0.902888706373137,53.6362419993615,
-0.756286900189999));
#43328=CARTESIAN_POINT('Ctrl Pts',(-0.912439620138181,53.6372740687119,
-0.744703935336704));
#43329=CARTESIAN_POINT('Ctrl Pts',(-0.916166347283998,53.6376781442489,
-0.740114343454668));
#43330=CARTESIAN_POINT('Ctrl Pts',(-0.923237464171409,53.6384471775105,
-0.731270759075751));
#43331=CARTESIAN_POINT('Ctrl Pts',(-0.926587341677578,53.6388125543855,
-0.727021484927079));
#43332=CARTESIAN_POINT('Ctrl Pts',(-0.935767166094992,53.6398172312023,
-0.715210483782094));
#43333=CARTESIAN_POINT('Ctrl Pts',(-0.941534777239932,53.6404523451065,
-0.70760052508435));
#43334=CARTESIAN_POINT('Ctrl Pts',(-0.966000327698649,53.6431675248616,
-0.674491072278882));
#43335=CARTESIAN_POINT('Ctrl Pts',(-0.983761316385715,53.6451933027415,
-0.648312334826286));
#43336=CARTESIAN_POINT('Ctrl Pts',(-1.04440787179169,53.6524430780907,-0.550679476528287));
#43337=CARTESIAN_POINT('Ctrl Pts',(-1.08073537181196,53.6574775114207,-0.47544496596454));
#43338=CARTESIAN_POINT('Ctrl Pts',(-1.12277739658354,53.6653057222121,-0.35802275616099));
#43339=CARTESIAN_POINT('Ctrl Pts',(-1.1346676590225,53.6679436807481,-0.318336520049744));
#43340=CARTESIAN_POINT('Ctrl Pts',(-1.14789995659898,53.6716045335986,-0.26388454087882));
#43341=CARTESIAN_POINT('Ctrl Pts',(-1.15109109409832,53.6725687152649,-0.249596921014044));
#43342=CARTESIAN_POINT('Ctrl Pts',(-1.15607440516219,53.6742264546652,-0.22515179072733));
#43343=CARTESIAN_POINT('Ctrl Pts',(-1.15800102013634,53.6749156608476,-0.215023219551279));
#43344=CARTESIAN_POINT('Ctrl Pts',(-1.16142569030614,53.6762399478473,-0.195635826823854));
#43345=CARTESIAN_POINT('Ctrl Pts',(-1.16294661208628,53.6768742437467,-0.186381810790098));
#43346=CARTESIAN_POINT('Ctrl Pts',(-1.16664739840601,53.678548067993,-0.162052212325414));
#43347=CARTESIAN_POINT('Ctrl Pts',(-1.16864553007423,53.6795932306927,-0.146951211712593));
#43348=CARTESIAN_POINT('Ctrl Pts',(-1.17531675937336,53.6837190752358,-0.0877197370874866));
#43349=CARTESIAN_POINT('Ctrl Pts',(-1.17778661101037,53.6868662939408,-0.0433830430605927));
#43350=CARTESIAN_POINT('Ctrl Pts',(-1.1776841270502,53.6957335960238,0.0794332951306981));
#43351=CARTESIAN_POINT('Ctrl Pts',(-1.16978077091275,53.7015631621963,0.157674418825063));
#43352=CARTESIAN_POINT('Ctrl Pts',(-1.14774802337991,53.7096006058311,0.266093840693275));
#43353=CARTESIAN_POINT('Ctrl Pts',(-1.14004540147492,53.7119115416153,0.297369000529171));
#43354=CARTESIAN_POINT('Ctrl Pts',(-1.12841346325165,53.7148319009299,0.337444739062884));
#43355=CARTESIAN_POINT('Ctrl Pts',(-1.12564572725268,53.7154937153235,0.346565444669406));
#43356=CARTESIAN_POINT('Ctrl Pts',(-1.12113455398268,53.7165215974492,0.3608068938321));
#43357=CARTESIAN_POINT('Ctrl Pts',(-1.11946611731128,53.7168917193444,0.365950704260894));
#43358=CARTESIAN_POINT('Ctrl Pts',(-1.11589856054584,53.7176623032736,0.376696765548133));
#43359=CARTESIAN_POINT('Ctrl Pts',(-1.11399255938596,53.7180623108859,0.382296521762411));
#43360=CARTESIAN_POINT('Ctrl Pts',(-1.10904208910941,53.7190727734424,0.396489358477497));
#43361=CARTESIAN_POINT('Ctrl Pts',(-1.10593980886366,53.7196799561819,0.405062117226059));
#43362=CARTESIAN_POINT('Ctrl Pts',(-1.09211305411378,53.7222808620585,0.441927089171468));
#43363=CARTESIAN_POINT('Ctrl Pts',(-1.08039924296611,53.7242242381574,0.46983857451692));
#43364=CARTESIAN_POINT('Ctrl Pts',(-1.03932202460243,53.7303753252218,0.558029961792834));
#43365=CARTESIAN_POINT('Ctrl Pts',(-1.00588533175447,53.7344595544153,0.616265644429291));
#43366=CARTESIAN_POINT('Ctrl Pts',(-0.935425080538271,53.7421327253014,
0.717827124140434));
#43367=CARTESIAN_POINT('Ctrl Pts',(-0.899871982936977,53.7456887324383,
0.761922022555255));
#43368=CARTESIAN_POINT('Ctrl Pts',(-0.850273572398811,53.7504216825328,
0.815101740249983));
#43369=CARTESIAN_POINT('Ctrl Pts',(-0.839014686615012,53.7514823717284,
0.826686342564799));
#43370=CARTESIAN_POINT('Ctrl Pts',(-0.819981260793099,53.7532559802974,
0.845480980680122));
#43371=CARTESIAN_POINT('Ctrl Pts',(-0.812341044367375,53.7539629484292,
0.852824349968331));
#43372=CARTESIAN_POINT('Ctrl Pts',(-0.797056428333644,53.7553682717022,
0.867123350873446));
#43373=CARTESIAN_POINT('Ctrl Pts',(-0.789417494873166,53.7560663439184,
0.874083441382371));
#43374=CARTESIAN_POINT('Ctrl Pts',(-0.77063784216132,53.7577728415555,0.890747232723807));
#43375=CARTESIAN_POINT('Ctrl Pts',(-0.75940446478982,53.7587856015193,0.900343345846582));
#43376=CARTESIAN_POINT('Ctrl Pts',(-0.715023622868079,53.7627580278213,
0.936834146825534));
#43377=CARTESIAN_POINT('Ctrl Pts',(-0.680607802062416,53.7657792736133,
0.962127463860813));
#43378=CARTESIAN_POINT('Ctrl Pts',(-0.569123416102032,53.7753791976557,
1.0350818136319));
#43379=CARTESIAN_POINT('Ctrl Pts',(-0.487889485123113,53.7821391770667,
1.07575919060754));
#43380=CARTESIAN_POINT('Ctrl Pts',(-0.379801043204749,53.7904295904191,
1.11509880772011));
#43381=CARTESIAN_POINT('Ctrl Pts',(-0.356542863596595,53.7921726735827,
1.12275178044642));
#43382=CARTESIAN_POINT('Ctrl Pts',(-0.324670490678888,53.794491858572,1.13214869207535));
#43383=CARTESIAN_POINT('Ctrl Pts',(-0.316252038783791,53.7950979383177,
1.1345290864782));
#43384=CARTESIAN_POINT('Ctrl Pts',(-0.302222408135289,53.7960963698605,
1.13832779066846));
#43385=CARTESIAN_POINT('Ctrl Pts',(-0.296626003080605,53.7964915871873,
1.139798913425));
#43386=CARTESIAN_POINT('Ctrl Pts',(-0.284943559473161,53.7973099550022,
1.14277799153259));
#43387=CARTESIAN_POINT('Ctrl Pts',(-0.278855953412043,53.7977327042798,
1.14427869500515));
#43388=CARTESIAN_POINT('Ctrl Pts',(-0.262256765872946,53.7988761189345,
1.14823035283336));
#43389=CARTESIAN_POINT('Ctrl Pts',(-0.251722726783744,53.7995916331148,
1.15058560904719));
#43390=CARTESIAN_POINT('Ctrl Pts',(-0.180026926831319,53.8044023807367,
1.16558390113029));
#43391=CARTESIAN_POINT('Ctrl Pts',(-0.117967759443314,53.808278849281,1.17349101941963));
#43392=CARTESIAN_POINT('Ctrl Pts',(0.0262064092789694,53.817201464806,1.18030087155895));
#43393=CARTESIAN_POINT('Ctrl Pts',(0.108148751295267,53.8222244615645,1.17562676922961));
#43394=CARTESIAN_POINT('Ctrl Pts',(0.188938462962337,53.8275149312419,1.16249615901018));
#43395=CARTESIAN_POINT('Ctrl Pts',(0.188938426235786,53.9273245270844,1.16249616497928));
#43396=CARTESIAN_POINT('Ctrl Pts',(0.152659231822772,53.9250499841622,1.1683925576763));
#43397=CARTESIAN_POINT('Ctrl Pts',(0.116114877842513,53.9227633969847,1.17258888333654));
#43398=CARTESIAN_POINT('Ctrl Pts',(0.0456482290779684,53.9182954063845,
1.17735185449536));
#43399=CARTESIAN_POINT('Ctrl Pts',(0.0117913650629317,53.916122848071,1.17817731794005));
#43400=CARTESIAN_POINT('Ctrl Pts',(-0.0357656519651533,53.9130075193054,
1.17728671715397));
#43401=CARTESIAN_POINT('Ctrl Pts',(-0.0494734003468065,53.9121022139423,
1.17679036061967));
#43402=CARTESIAN_POINT('Ctrl Pts',(-0.0733099531465983,53.9105135779761,
1.17551003868362));
#43403=CARTESIAN_POINT('Ctrl Pts',(-0.0834432595663409,53.9098336901031,
1.17483420601588));
#43404=CARTESIAN_POINT('Ctrl Pts',(-0.104454583854328,53.9084139273164,
1.1731596695673));
#43405=CARTESIAN_POINT('Ctrl Pts',(-0.115329942010815,53.9076734727027,
1.17214050386461));
#43406=CARTESIAN_POINT('Ctrl Pts',(-0.143867896688091,53.9057150173803,
1.16906512019708));
#43407=CARTESIAN_POINT('Ctrl Pts',(-0.161500244965537,53.9044893522484,
1.16675997423065));
#43408=CARTESIAN_POINT('Ctrl Pts',(-0.281602355997566,53.896029275183,1.14828404677168));
#43409=CARTESIAN_POINT('Ctrl Pts',(-0.381583162984285,53.888370178109,1.11903625172896));
#43410=CARTESIAN_POINT('Ctrl Pts',(-0.50437070093299,53.8785397948054,1.06472513181056));
#43411=CARTESIAN_POINT('Ctrl Pts',(-0.531835045507651,53.8763157614107,
1.05127594635854));
#43412=CARTESIAN_POINT('Ctrl Pts',(-0.570537534118971,53.8731715720721,
1.03041806824942));
#43413=CARTESIAN_POINT('Ctrl Pts',(-0.582219926352531,53.8722211710787,
1.02386252161253));
#43414=CARTESIAN_POINT('Ctrl Pts',(-0.60298785353048,53.8705324401875,1.01173819910354));
#43415=CARTESIAN_POINT('Ctrl Pts',(-0.61211438444692,53.8697906123593,1.00624278158637));
#43416=CARTESIAN_POINT('Ctrl Pts',(-0.62646580242538,53.8686260524972,0.99733373570745));
#43417=CARTESIAN_POINT('Ctrl Pts',(-0.63174004297222,53.8681984972616,0.994001259880188));
#43418=CARTESIAN_POINT('Ctrl Pts',(-0.641866888005468,53.8673787724929,
0.987489549405691));
#43419=CARTESIAN_POINT('Ctrl Pts',(-0.646722868723927,53.8669862782822,
0.984316130595538));
#43420=CARTESIAN_POINT('Ctrl Pts',(-0.658913118589361,53.8660019372149,
0.976220558450205));
#43421=CARTESIAN_POINT('Ctrl Pts',(-0.666216025571102,53.8654131166064,
0.971251407013234));
#43422=CARTESIAN_POINT('Ctrl Pts',(-0.694113894249522,53.8631642702005,
0.951805987794783));
#43423=CARTESIAN_POINT('Ctrl Pts',(-0.714300078526848,53.8615381041934,
0.936752015663351));
#43424=CARTESIAN_POINT('Ctrl Pts',(-0.804229254726047,53.8542202816923,
0.865087853597262));
#43425=CARTESIAN_POINT('Ctrl Pts',(-0.867839083162592,53.8488136827263,
0.801261030261879));
#43426=CARTESIAN_POINT('Ctrl Pts',(-0.94998998012497,53.8405128830896,0.697442273802732));
#43427=CARTESIAN_POINT('Ctrl Pts',(-0.974570109904326,53.8378039305937,
0.662660705222124));
#43428=CARTESIAN_POINT('Ctrl Pts',(-1.00506484963416,53.8340607525191,0.614131522796961));
#43429=CARTESIAN_POINT('Ctrl Pts',(-1.01268135675169,53.8330889425121,0.601489249140145));
#43430=CARTESIAN_POINT('Ctrl Pts',(-1.02522118955754,53.8314222896792,0.579761389482697));
#43431=CARTESIAN_POINT('Ctrl Pts',(-1.03026629340123,53.8307319214265,0.570747850910221));
#43432=CARTESIAN_POINT('Ctrl Pts',(-1.04024550701023,53.8293246223153,0.552355530816141));
#43433=CARTESIAN_POINT('Ctrl Pts',(-1.04517288060168,53.8286075325064,0.542974202069317));
#43434=CARTESIAN_POINT('Ctrl Pts',(-1.0572941351978,53.8267853134336,0.519119802392274));
#43435=CARTESIAN_POINT('Ctrl Pts',(-1.06431772422427,53.8256743863906,0.504563171442096));
#43436=CARTESIAN_POINT('Ctrl Pts',(-1.09469754669775,53.8206073469156,0.438141128454311));
#43437=CARTESIAN_POINT('Ctrl Pts',(-1.1145741661967,53.8165369645876,0.384776696895595));
#43438=CARTESIAN_POINT('Ctrl Pts',(-1.14714400783415,53.8080723856222,0.273263663605702));
#43439=CARTESIAN_POINT('Ctrl Pts',(-1.15944704481569,53.8036836305903,0.215162088572969));
#43440=CARTESIAN_POINT('Ctrl Pts',(-1.17218381204311,53.7966933668929,0.120087803411154));
#43441=CARTESIAN_POINT('Ctrl Pts',(-1.17535118299592,53.7940555075056,0.0835828638502875));
#43442=CARTESIAN_POINT('Ctrl Pts',(-1.17719623458976,53.7908180035941,0.0373720583644565));
#43443=CARTESIAN_POINT('Ctrl Pts',(-1.17746228524513,53.790149678217,0.0277529719767753));
#43444=CARTESIAN_POINT('Ctrl Pts',(-1.17770307870723,53.7890732826708,0.0121136865822064));
#43445=CARTESIAN_POINT('Ctrl Pts',(-1.17774960635718,53.7886615117446,0.00609524966651524));
#43446=CARTESIAN_POINT('Ctrl Pts',(-1.17775039039683,53.7878413875649,-0.0059687622322643));
#43447=CARTESIAN_POINT('Ctrl Pts',(-1.17770423813461,53.7874330672057,-0.0120141515325746));
#43448=CARTESIAN_POINT('Ctrl Pts',(-1.17746206087186,53.7863727301873,-0.0278062407918057));
#43449=CARTESIAN_POINT('Ctrl Pts',(-1.17719156796747,53.7857246642865,-0.037551559094287));
#43450=CARTESIAN_POINT('Ctrl Pts',(-1.17525224431485,53.782541654558,-0.0858083097293891));
#43451=CARTESIAN_POINT('Ctrl Pts',(-1.17181428826531,53.7800894395291,-0.124228835477599));
#43452=CARTESIAN_POINT('Ctrl Pts',(-1.15975156479247,53.7746092401423,-0.210865653479617));
#43453=CARTESIAN_POINT('Ctrl Pts',(-1.14999344817933,53.7716080262934,-0.258850100305046));
#43454=CARTESIAN_POINT('Ctrl Pts',(-1.1205163643538,53.7645892730672,-0.368372445157435));
#43455=CARTESIAN_POINT('Ctrl Pts',(-1.09866772038034,53.7605603460187,-0.429165452501773));
#43456=CARTESIAN_POINT('Ctrl Pts',(-1.0651429988736,53.7552963894138,-0.502827882172949));
#43457=CARTESIAN_POINT('Ctrl Pts',(-1.05801870236843,53.7542171676749,-0.517650334565637));
#43458=CARTESIAN_POINT('Ctrl Pts',(-1.04577188227245,53.7524212187868,-0.541820739238523));
#43459=CARTESIAN_POINT('Ctrl Pts',(-1.04082850731533,53.7517107690503,-0.551257243864777));
#43460=CARTESIAN_POINT('Ctrl Pts',(-1.03085937737525,53.7503050357582,-0.569675264801677));
#43461=CARTESIAN_POINT('Ctrl Pts',(-1.02584254679098,53.7496101179238,-0.578660540151756));
#43462=CARTESIAN_POINT('Ctrl Pts',(-1.01345363031929,53.7479228740344,-0.600181871574193));
#43463=CARTESIAN_POINT('Ctrl Pts',(-1.00596600388983,53.7469264437929,-0.612649088440841));
#43464=CARTESIAN_POINT('Ctrl Pts',(-0.976737521841124,53.7431205765336,
-0.659334750308995));
#43465=CARTESIAN_POINT('Ctrl Pts',(-0.953467991180597,53.7402561317173,
-0.692558033441009));
#43466=CARTESIAN_POINT('Ctrl Pts',(-0.879892091693928,53.7316561838714,
-0.786852811775211));
#43467=CARTESIAN_POINT('Ctrl Pts',(-0.82509672860188,53.7257876664316,-0.844133320142188));
#43468=CARTESIAN_POINT('Ctrl Pts',(-0.737307943179909,53.7173727795443,
-0.919128390621436));
#43469=CARTESIAN_POINT('Ctrl Pts',(-0.70854791604467,53.7147500030779,-0.941477757666481));
#43470=CARTESIAN_POINT('Ctrl Pts',(-0.670769588615357,53.7115117525278,
-0.968121734872099));
#43471=CARTESIAN_POINT('Ctrl Pts',(-0.662672166575706,53.7108291702538,
-0.97368226348867));
#43472=CARTESIAN_POINT('Ctrl Pts',(-0.649466831398828,53.7097356578704,
-0.982509355671043));
#43473=CARTESIAN_POINT('Ctrl Pts',(-0.644401793562308,53.7093208179043,
-0.985838796015544));
#43474=CARTESIAN_POINT('Ctrl Pts',(-0.634269148771241,53.7085003690883,
-0.992387903478384));
#43475=CARTESIAN_POINT('Ctrl Pts',(-0.629202193099903,53.708094730247,-0.995608210032243));
#43476=CARTESIAN_POINT('Ctrl Pts',(-0.616010497566849,53.707050005927,-1.00385126492851));
#43477=CARTESIAN_POINT('Ctrl Pts',(-0.607848688892706,53.7064146569309,
-1.00881429472247));
#43478=CARTESIAN_POINT('Ctrl Pts',(-0.568973502919236,53.7034357402132,
-1.03181037603517));
#43479=CARTESIAN_POINT('Ctrl Pts',(-0.53751000134393,53.701162556173,-1.04854518690345));
#43480=CARTESIAN_POINT('Ctrl Pts',(-0.411021291326211,53.6923638169503,
-1.10862902721096));
#43481=CARTESIAN_POINT('Ctrl Pts',(-0.311174234656337,53.6861006680883,
-1.14068766067955));
#43482=CARTESIAN_POINT('Ctrl Pts',(-0.18566564894933,53.6779159752707,-1.16325284113186));
#43483=CARTESIAN_POINT('Ctrl Pts',(-0.162811149525184,53.6764157686861,
-1.16667104267546));
#43484=CARTESIAN_POINT('Ctrl Pts',(-0.127842054805132,53.6740971291523,
-1.17085364712644));
#43485=CARTESIAN_POINT('Ctrl Pts',(-0.115790953119114,53.6732939332609,
-1.17210677451548));
#43486=CARTESIAN_POINT('Ctrl Pts',(-0.0937625018144055,53.6718171295385,
-1.17405436133281));
#43487=CARTESIAN_POINT('Ctrl Pts',(-0.0837914390509295,53.6711454498308,
-1.1748080839849));
#43488=CARTESIAN_POINT('Ctrl Pts',(-0.0619430650411083,53.6696660844722,
-1.17618006793515));
#43489=CARTESIAN_POINT('Ctrl Pts',(-0.0500636726413079,53.6688568172892,
-1.1767455570374));
#43490=CARTESIAN_POINT('Ctrl Pts',(-0.0155216484095266,53.6664885166175,
-1.17786586539288));
#43491=CARTESIAN_POINT('Ctrl Pts',(0.00714985271567457,53.6649150269079,
-1.17794638019866));
#43492=CARTESIAN_POINT('Ctrl Pts',(0.08368940932996,53.659535548023,-1.17600858175775));
#43493=CARTESIAN_POINT('Ctrl Pts',(0.137406833823505,53.6556435659775,-1.17094755463221));
#43494=CARTESIAN_POINT('Ctrl Pts',(0.258585755937825,53.6466595385097,-1.15107653050602));
#43495=CARTESIAN_POINT('Ctrl Pts',(0.325479484460857,53.6415491111313,-1.13397855320986));
#43496=CARTESIAN_POINT('Ctrl Pts',(0.410329347150613,53.635096902081,-1.10415888854439));
#43497=CARTESIAN_POINT('Ctrl Pts',(0.429974344367729,53.6336060852208,-1.09665820350503));
#43498=CARTESIAN_POINT('Ctrl Pts',(0.457057282400076,53.6315647643212,-1.08547784970786));
#43499=CARTESIAN_POINT('Ctrl Pts',(0.464672026240766,53.6309923923729,-1.08224001015246));
#43500=CARTESIAN_POINT('Ctrl Pts',(0.477530277115895,53.6300293263961,-1.07661185727455));
#43501=CARTESIAN_POINT('Ctrl Pts',(0.482791412411177,53.6296362770106,-1.07426287047756));
#43502=CARTESIAN_POINT('Ctrl Pts',(0.493928313695612,53.6288066227151,-1.06919212905545));
#43503=CARTESIAN_POINT('Ctrl Pts',(0.499799171704392,53.6283706147074,-1.06646039816956));
#43504=CARTESIAN_POINT('Ctrl Pts',(0.51628370097506,53.6271493452826,-1.05862405964244));
#43505=CARTESIAN_POINT('Ctrl Pts',(0.526844090655197,53.6263704786571,-1.05340832055091));
#43506=CARTESIAN_POINT('Ctrl Pts',(0.588258284704693,53.6218512658212,-1.02192140920936));
#43507=CARTESIAN_POINT('Ctrl Pts',(0.63722668266313,53.6182875568741,-0.99212645998877));
#43508=CARTESIAN_POINT('Ctrl Pts',(0.754771189948186,53.6093548498176,-0.908298358852658));
#43509=CARTESIAN_POINT('Ctrl Pts',(0.819864557515042,53.6040241618622,-0.850003470836564));
#43510=CARTESIAN_POINT('Ctrl Pts',(0.890234272667171,53.5971874920884,-0.771309652110807));
#43511=CARTESIAN_POINT('Ctrl Pts',(0.902210230398231,53.5959805301114,-0.757266319892999));
#43512=CARTESIAN_POINT('Ctrl Pts',(0.920827598299305,53.594028795696,-0.734366337528263));
#43513=CARTESIAN_POINT('Ctrl Pts',(0.927682953571771,53.5932927030396,-0.725687058619148));
#43514=CARTESIAN_POINT('Ctrl Pts',(0.940568701858436,53.591874368064,-0.70889194020726));
#43515=CARTESIAN_POINT('Ctrl Pts',(0.946618832718822,53.5911929912547,-0.70079243736782));
#43516=CARTESIAN_POINT('Ctrl Pts',(0.960439230683301,53.589599430457,-0.681785071767931));
#43517=CARTESIAN_POINT('Ctrl Pts',(0.96812906748496,53.5886842582153,-0.670820752986448));
#43518=CARTESIAN_POINT('Ctrl Pts',(0.993315958693978,53.5855874415137,-0.633573457437504));
#43519=CARTESIAN_POINT('Ctrl Pts',(1.00994145730019,53.5833742711981,-0.606720569476476));
#43520=CARTESIAN_POINT('Ctrl Pts',(1.04958723165269,53.5776363383147,-0.536532341734669));
#43521=CARTESIAN_POINT('Ctrl Pts',(1.07101446968706,53.5740674867239,-0.492369270769709));
#43522=CARTESIAN_POINT('Ctrl Pts',(1.11780681112742,53.5650230325015,-0.378307217113263));
#43523=CARTESIAN_POINT('Ctrl Pts',(1.13943069637904,53.5595238562637,-0.307095545735416));
#43524=CARTESIAN_POINT('Ctrl Pts',(1.15656784309077,53.5534528412819,-0.222681107322508));
#43525=CARTESIAN_POINT('Ctrl Pts',(1.15875419629785,53.5526233464698,-0.211008982933579));
#43526=CARTESIAN_POINT('Ctrl Pts',(1.16187461019135,53.5513492573521,-0.192835535692198));
#43527=CARTESIAN_POINT('Ctrl Pts',(1.16293139537067,53.5508984493367,-0.186356455546155));
#43528=CARTESIAN_POINT('Ctrl Pts',(1.16480972565689,53.5500595626198,-0.174201741319826));
#43529=CARTESIAN_POINT('Ctrl Pts',(1.16564403702173,53.5496708519765,-0.168528704012624));
#43530=CARTESIAN_POINT('Ctrl Pts',(1.16755542371879,53.5487392497945,-0.154838071043752));
#43531=CARTESIAN_POINT('Ctrl Pts',(1.16859138766132,53.5481986078473,-0.146815100038312));
#43532=CARTESIAN_POINT('Ctrl Pts',(1.17204271997722,53.5462557133987,-0.117729968719078));
#43533=CARTESIAN_POINT('Ctrl Pts',(1.17397212427653,53.5448773880538,-0.0966129639201676));
#43534=CARTESIAN_POINT('Ctrl Pts',(1.17759007943259,53.5412574067993,-0.040256796115039));
#43535=CARTESIAN_POINT('Ctrl Pts',(1.17826762477489,53.5390513179674,-0.0049735429055084));
#43536=CARTESIAN_POINT('Ctrl Pts',(1.17498144957712,53.5311210256185,0.122763058998919));
#43537=CARTESIAN_POINT('Ctrl Pts',(1.16171698058323,53.5254968070784,0.214626721490528));
#43538=CARTESIAN_POINT('Ctrl Pts',(1.13276132659902,53.5182525368309,0.323008242973149));
#43539=CARTESIAN_POINT('Ctrl Pts',(1.12720476688198,53.5169682128172,0.341894558470876));
#43540=CARTESIAN_POINT('Ctrl Pts',(1.11768198656201,53.5149149956376,0.371500173670461));
#43541=CARTESIAN_POINT('Ctrl Pts',(1.11402842904227,53.5141562892186,0.382316682849085));
#43542=CARTESIAN_POINT('Ctrl Pts',(1.10720427810417,53.5127880798925,0.401590964814957));
#43543=CARTESIAN_POINT('Ctrl Pts',(1.10409250578537,53.512180573141,0.410068710424449));
#43544=CARTESIAN_POINT('Ctrl Pts',(1.09653885311686,53.5107428072886,0.42993848608389));
#43545=CARTESIAN_POINT('Ctrl Pts',(1.09201652441991,53.5099099044167,0.441298593736082));
#43546=CARTESIAN_POINT('Ctrl Pts',(1.07791438922034,53.5073920071606,0.475178373587465));
#43547=CARTESIAN_POINT('Ctrl Pts',(1.06780927616412,53.5056895949642,0.497470715302193));
#43548=CARTESIAN_POINT('Ctrl Pts',(1.01432040096068,53.4971432299624,0.606318121929986));
#43549=CARTESIAN_POINT('Ctrl Pts',(0.961076625213557,53.4899686094203,0.687599897175047));
#43550=CARTESIAN_POINT('Ctrl Pts',(0.8723168884384,53.4799374331565,0.792337745829489));
#43551=CARTESIAN_POINT('Ctrl Pts',(0.844548989662814,53.4770086703715,0.82187196328075));
#43552=CARTESIAN_POINT('Ctrl Pts',(0.808058928259811,53.4734641648204,0.85687620802663));
#43553=CARTESIAN_POINT('Ctrl Pts',(0.800717228437614,53.4727653167395,0.863740704499297));
#43554=CARTESIAN_POINT('Ctrl Pts',(0.788772247053147,53.4716522796479,0.874626054682852));
#43555=CARTESIAN_POINT('Ctrl Pts',(0.7842241556256,53.4712339368155,0.878706362378256));
#43556=CARTESIAN_POINT('Ctrl Pts',(0.775176536320685,53.4704127717297,0.886697204587074));
#43557=CARTESIAN_POINT('Ctrl Pts',(0.770678703017699,53.4700098517953,0.890609305338378));
#43558=CARTESIAN_POINT('Ctrl Pts',(0.759051820776676,53.4689812533735,0.900568028975325));
#43559=CARTESIAN_POINT('Ctrl Pts',(0.751879952810958,53.4683590923172,0.906564389198077));
#43560=CARTESIAN_POINT('Ctrl Pts',(0.719108673922144,53.4655673220435,0.933307821675175));
#43561=CARTESIAN_POINT('Ctrl Pts',(0.692714612460654,53.463457725435,0.953062253515281));
#43562=CARTESIAN_POINT('Ctrl Pts',(0.59767943733474,53.4561987284,1.01815351146247));
#43563=CARTESIAN_POINT('Ctrl Pts',(0.525153308653292,53.4512264342153,1.05738940345974));
#43564=CARTESIAN_POINT('Ctrl Pts',(0.411277463622825,53.4434955467889,1.10436517124263));
#43565=CARTESIAN_POINT('Ctrl Pts',(0.37264122855725,53.440887662107,1.11799355015461));
#43566=CARTESIAN_POINT('Ctrl Pts',(0.319085238406269,53.4372421731406,1.13379967621427));
#43567=CARTESIAN_POINT('Ctrl Pts',(0.304715699979462,53.4362612991878,1.13774575557498));
#43568=CARTESIAN_POINT('Ctrl Pts',(0.280340057740739,53.4345907073707,1.14394476071865));
#43569=CARTESIAN_POINT('Ctrl Pts',(0.270372144584672,53.4339056915133,1.14634159639856));
#43570=CARTESIAN_POINT('Ctrl Pts',(0.250095003439261,53.4325078074733,1.15093816047064));
#43571=CARTESIAN_POINT('Ctrl Pts',(0.239785016805525,53.4317947630238,1.15313021514289));
#43572=CARTESIAN_POINT('Ctrl Pts',(0.215987303652998,53.4301430568098,1.15785701435894));
#43573=CARTESIAN_POINT('Ctrl Pts',(0.202482313003292,53.4292014287768,1.16029490081215));
#43574=CARTESIAN_POINT('Ctrl Pts',(0.188938462305883,53.4282524383066,1.16249615911688));
#43575=CARTESIAN_POINT('Origin',(0.,56.5393671147362,0.));
#43576=CARTESIAN_POINT('',(0.188938518720844,52.8287166258961,1.16249614994785));
#43577=CARTESIAN_POINT('',(0.188938438127302,52.9266130464139,1.16249616304658));
#43578=CARTESIAN_POINT('',(0.188938462403162,56.5393671147362,1.16249615910107));
#43579=CARTESIAN_POINT('',(-1.17774981132563,53.18979291915,-0.000666650161686058));
#43580=CARTESIAN_POINT('Ctrl Pts',(0.188938518720853,52.8287166258961,1.16249614994785));
#43581=CARTESIAN_POINT('Ctrl Pts',(0.2006730995186,52.8295897176874,1.16058894852285));
#43582=CARTESIAN_POINT('Ctrl Pts',(0.212381401918546,52.8304621543522,1.15850364635666));
#43583=CARTESIAN_POINT('Ctrl Pts',(0.267010632734191,52.8345345518635,1.14791744976063));
#43584=CARTESIAN_POINT('Ctrl Pts',(0.309469407987332,52.8377059339504,1.13720649980803));
#43585=CARTESIAN_POINT('Ctrl Pts',(0.360959490409606,52.8414889103456,1.12111866210965));
#43586=CARTESIAN_POINT('Ctrl Pts',(0.370642167423009,52.8421974189029,1.11795492294123));
#43587=CARTESIAN_POINT('Ctrl Pts',(0.386094072421604,52.8433221207186,1.11268330125663));
#43588=CARTESIAN_POINT('Ctrl Pts',(0.391889736438981,52.8437426143387,1.11065530228121));
#43589=CARTESIAN_POINT('Ctrl Pts',(0.403260880691614,52.8445645842728,1.10657625668621));
#43590=CARTESIAN_POINT('Ctrl Pts',(0.408837163538314,52.8449661963987,1.10452819163131));
#43591=CARTESIAN_POINT('Ctrl Pts',(0.423048378346701,52.8459865072165,1.09918630704447));
#43592=CARTESIAN_POINT('Ctrl Pts',(0.431660700320431,52.8466018019491,1.0958327979896));
#43593=CARTESIAN_POINT('Ctrl Pts',(0.46960169037032,52.8493027398839,1.08054241916639));
#43594=CARTESIAN_POINT('Ctrl Pts',(0.498483985424261,52.8513330893003,1.06752600009715));
#43595=CARTESIAN_POINT('Ctrl Pts',(0.593337432878825,52.8580266417731,1.02008765996191));
#43596=CARTESIAN_POINT('Ctrl Pts',(0.656566379223215,52.8625411110672,0.980586433127076));
#43597=CARTESIAN_POINT('Ctrl Pts',(0.754224455601946,52.8702100380247,0.905869552532492));
#43598=CARTESIAN_POINT('Ctrl Pts',(0.790933302753439,52.8732827095672,0.874001086947903));
#43599=CARTESIAN_POINT('Ctrl Pts',(0.836747547604304,52.8774684280752,0.828971854586845));
#43600=CARTESIAN_POINT('Ctrl Pts',(0.847706445816414,52.8784987031842,0.817761907709031));
#43601=CARTESIAN_POINT('Ctrl Pts',(0.864910923710795,52.8801659611316,0.799445773687585));
#43602=CARTESIAN_POINT('Ctrl Pts',(0.871300523789437,52.8807967050165,0.792477027679491));
#43603=CARTESIAN_POINT('Ctrl Pts',(0.884437357022759,52.8821183724084,0.777798543247462));
#43604=CARTESIAN_POINT('Ctrl Pts',(0.8911692497593,52.882809861242,0.770076209935523));
#43605=CARTESIAN_POINT('Ctrl Pts',(0.907028756337303,52.8844740124996,0.751396862259263));
#43606=CARTESIAN_POINT('Ctrl Pts',(0.916059585857138,52.8854504977446,0.740360191567335));
#43607=CARTESIAN_POINT('Ctrl Pts',(0.948456625177196,52.8890634303193,0.699267008691656));
#43608=CARTESIAN_POINT('Ctrl Pts',(0.970559932785211,52.8917477722769,0.668249342853592));
#43609=CARTESIAN_POINT('Ctrl Pts',(1.02828932224789,52.899412415559,0.578316762190948));
#43610=CARTESIAN_POINT('Ctrl Pts',(1.06030967675751,52.9044893720213,0.517272734497527));
#43611=CARTESIAN_POINT('Ctrl Pts',(1.10561411067218,52.9131112608756,0.408769742506601));
#43612=CARTESIAN_POINT('Ctrl Pts',(1.12159847298634,52.9166611620149,0.362619806138691));
#43613=CARTESIAN_POINT('Ctrl Pts',(1.13744784911272,52.9208108259074,0.305637899272518));
#43614=CARTESIAN_POINT('Ctrl Pts',(1.14008935721792,52.9215308952189,0.295632222587381));
#43615=CARTESIAN_POINT('Ctrl Pts',(1.14409604138076,52.9226694610145,0.279602282609837));
#43616=CARTESIAN_POINT('Ctrl Pts',(1.14554623549847,52.9230924365349,0.273600100700102));
#43617=CARTESIAN_POINT('Ctrl Pts',(1.14829307666671,52.9239152281922,0.261826390607417));
#43618=CARTESIAN_POINT('Ctrl Pts',(1.14959356170063,52.9243152258021,0.256056036737968));
#43619=CARTESIAN_POINT('Ctrl Pts',(1.15278759123815,52.9253256263788,0.241368850269724));
#43620=CARTESIAN_POINT('Ctrl Pts',(1.15462124072121,52.9259327579675,0.232439144088306));
#43621=CARTESIAN_POINT('Ctrl Pts',(1.1620907742283,52.9285330512514,0.19379109163921));
#43622=CARTESIAN_POINT('Ctrl Pts',(1.16668480798187,52.9304758954287,0.163880592253115));
#43623=CARTESIAN_POINT('Ctrl Pts',(1.17773365483925,52.9366238649529,0.0672721995210272));
#43624=CARTESIAN_POINT('Ctrl Pts',(1.17965376705203,52.9407056477405,0.000189555242239093));
#43625=CARTESIAN_POINT('Ctrl Pts',(1.17265342603484,52.9483790633043,-0.123228654284533));
#43626=CARTESIAN_POINT('Ctrl Pts',(1.16537447955829,52.9519379905089,-0.179450750498619));
#43627=CARTESIAN_POINT('Ctrl Pts',(1.15085906525947,52.9566741898002,-0.250757771638523));
#43628=CARTESIAN_POINT('Ctrl Pts',(1.14731135900949,52.957734983924,-0.266519515351546));
#43629=CARTESIAN_POINT('Ctrl Pts',(1.14090150898911,52.9595087196088,-0.292491214293996));
#43630=CARTESIAN_POINT('Ctrl Pts',(1.13822361739693,52.9602157081075,-0.30274469106938));
#43631=CARTESIAN_POINT('Ctrl Pts',(1.13266181922262,52.9616210348736,-0.322922674878579));
#43632=CARTESIAN_POINT('Ctrl Pts',(1.12978491752607,52.9623190897455,-0.332848131945473));
#43633=CARTESIAN_POINT('Ctrl Pts',(1.12247906632206,52.9640254783519,-0.356866954416469));
#43634=CARTESIAN_POINT('Ctrl Pts',(1.1179149411176,52.9650381452989,-0.370917008369469));
#43635=CARTESIAN_POINT('Ctrl Pts',(1.0991433750963,52.9690095822471,-0.425205536805777));
#43636=CARTESIAN_POINT('Ctrl Pts',(1.08301904835391,52.9720298913571,-0.464741741315517));
#43637=CARTESIAN_POINT('Ctrl Pts',(1.02612121917154,52.9816230403571,-0.585112510950493));
#43638=CARTESIAN_POINT('Ctrl Pts',(0.978162190955798,52.9883768112269,-0.662176937680276));
#43639=CARTESIAN_POINT('Ctrl Pts',(0.906577877595465,52.9966676415709,-0.752206357595949));
#43640=CARTESIAN_POINT('Ctrl Pts',(0.89069928776084,52.998416204701,-0.770942814697882));
#43641=CARTESIAN_POINT('Ctrl Pts',(0.868377364399699,53.0007413496616,-0.795671104170916));
#43642=CARTESIAN_POINT('Ctrl Pts',(0.862436838404874,53.0013480982001,-0.802106267539213));
#43643=CARTESIAN_POINT('Ctrl Pts',(0.852451686046485,53.00234731473,-0.812683632040403));
#43644=CARTESIAN_POINT('Ctrl Pts',(0.848447385578473,53.0027426575487,-0.816863270375048));
#43645=CARTESIAN_POINT('Ctrl Pts',(0.840043934300118,53.0035609405267,-0.825506219450236));
#43646=CARTESIAN_POINT('Ctrl Pts',(0.835639711988269,53.0039834835219,-0.829964219847369));
#43647=CARTESIAN_POINT('Ctrl Pts',(0.823564169564346,53.0051257024392,-0.841993638963694));
#43648=CARTESIAN_POINT('Ctrl Pts',(0.815823954686229,53.0058402453446,-0.849495453100467));
#43649=CARTESIAN_POINT('Ctrl Pts',(0.762786259511501,53.0106282156251,-0.899505913155628));
#43650=CARTESIAN_POINT('Ctrl Pts',(0.714284081766245,53.0144851746573,-0.938484965679031));
#43651=CARTESIAN_POINT('Ctrl Pts',(0.594101508627504,53.0234745825206,-1.02032949163686));
#43652=CARTESIAN_POINT('Ctrl Pts',(0.520506789082438,53.0285823425829,-1.05976408288123));
#43653=CARTESIAN_POINT('Ctrl Pts',(0.425904987512413,53.0351900187235,-1.09820557622742));
#43654=CARTESIAN_POINT('Ctrl Pts',(0.408270675972368,53.0364223260745,-1.10488258960758));
#43655=CARTESIAN_POINT('Ctrl Pts',(0.379971739242383,53.0384051851033,-1.11482765773376));
#43656=CARTESIAN_POINT('Ctrl Pts',(0.369407428586212,53.0391465462902,-1.11837264200398));
#43657=CARTESIAN_POINT('Ctrl Pts',(0.349183728680285,53.0405687466225,-1.12484114737185));
#43658=CARTESIAN_POINT('Ctrl Pts',(0.339533910166088,53.0412486313885,-1.12779146832828));
#43659=CARTESIAN_POINT('Ctrl Pts',(0.31714955400953,53.0428292538764,-1.13432190655528));
#43660=CARTESIAN_POINT('Ctrl Pts',(0.30439044762799,53.0437328229255,-1.13781213636515));
#43661=CARTESIAN_POINT('Ctrl Pts',(0.262061611743417,53.0467403208364,-1.14862819548066));
#43662=CARTESIAN_POINT('Ctrl Pts',(0.232268586942874,53.0488733075452,-1.15502122571214));
#43663=CARTESIAN_POINT('Ctrl Pts',(0.156664191535607,53.0543281790943,-1.16820112986629));
#43664=CARTESIAN_POINT('Ctrl Pts',(0.110640043253869,53.0576885005965,-1.17345456225868));
#43665=CARTESIAN_POINT('Ctrl Pts',(-0.0115765761533891,53.0666567579805,
-1.18015058576851));
#43666=CARTESIAN_POINT('Ctrl Pts',(-0.0878115283503732,53.0723048533969,
-1.17693664445345));
#43667=CARTESIAN_POINT('Ctrl Pts',(-0.17656862787715,53.0786439264146,-1.16451733757324));
#43668=CARTESIAN_POINT('Ctrl Pts',(-0.1898985530457,53.0795891535347,-1.16241803501005));
#43669=CARTESIAN_POINT('Ctrl Pts',(-0.209908532292049,53.0809949450734,
-1.15891328062842));
#43670=CARTESIAN_POINT('Ctrl Pts',(-0.216616784493539,53.0814639956263,
-1.15767817567493));
#43671=CARTESIAN_POINT('Ctrl Pts',(-0.228896554039207,53.0823180467502,
-1.15530677987873));
#43672=CARTESIAN_POINT('Ctrl Pts',(-0.234470901157486,53.0827039544629,
-1.15418836709251));
#43673=CARTESIAN_POINT('Ctrl Pts',(-0.247540556601461,53.0836047773406,
-1.15146753059295));
#43674=CARTESIAN_POINT('Ctrl Pts',(-0.255028633944232,53.084117861702,-1.14983225079936));
#43675=CARTESIAN_POINT('Ctrl Pts',(-0.280343802733076,53.0858438361369,
-1.14404433593328));
#43676=CARTESIAN_POINT('Ctrl Pts',(-0.298090792901531,53.0870392746276,
-1.13954905867998));
#43677=CARTESIAN_POINT('Ctrl Pts',(-0.342906325355392,53.09003773247,-1.12707862822197));
#43678=CARTESIAN_POINT('Ctrl Pts',(-0.369806996218645,53.0918185551398,
-1.11854099995123));
#43679=CARTESIAN_POINT('Ctrl Pts',(-0.477661504512481,53.0989750930174,
-1.07999341288384));
#43680=CARTESIAN_POINT('Ctrl Pts',(-0.555503955156738,53.1041992107036,
-1.042094911211));
#43681=CARTESIAN_POINT('Ctrl Pts',(-0.654109799791452,53.1116010380592,
-0.979873452017202));
#43682=CARTESIAN_POINT('Ctrl Pts',(-0.679078846822568,53.1135490442023,
-0.962737397082373));
#43683=CARTESIAN_POINT('Ctrl Pts',(-0.713168118897791,53.1163337658918,
-0.937355785675274));
#43684=CARTESIAN_POINT('Ctrl Pts',(-0.72286296091537,53.1171406375484,-0.929899863447548));
#43685=CARTESIAN_POINT('Ctrl Pts',(-0.74041546657779,53.118630322848,-0.915960551827862));
#43686=CARTESIAN_POINT('Ctrl Pts',(-0.748308565487754,53.1193112601898,
-0.909523543029886));
#43687=CARTESIAN_POINT('Ctrl Pts',(-0.764276655294852,53.1207122720172,
-0.896152621115338));
#43688=CARTESIAN_POINT('Ctrl Pts',(-0.772343099562601,53.1214326633869,
-0.889210014410118));
#43689=CARTESIAN_POINT('Ctrl Pts',(-0.792585551049317,53.1232736352252,
-0.871304550059492));
#43690=CARTESIAN_POINT('Ctrl Pts',(-0.804628573098222,53.1244002566837,
-0.860195493290082));
#43691=CARTESIAN_POINT('Ctrl Pts',(-0.864896613328724,53.1302042905662,
-0.802228145526444));
#43692=CARTESIAN_POINT('Ctrl Pts',(-0.909269337253967,53.1350466833101,
-0.751560206045921));
#43693=CARTESIAN_POINT('Ctrl Pts',(-0.991809042942691,53.1452522320054,
-0.639233015411393));
#43694=CARTESIAN_POINT('Ctrl Pts',(-1.02911039010068,53.1506063499974,-0.577266524132677));
#43695=CARTESIAN_POINT('Ctrl Pts',(-1.06796373237299,53.1569762139058,-0.496832538305492));
#43696=CARTESIAN_POINT('Ctrl Pts',(-1.0750846390581,53.1581860170101,-0.481229880008048));
#43697=CARTESIAN_POINT('Ctrl Pts',(-1.08461638336148,53.1598624496257,-0.459076146974757));
#43698=CARTESIAN_POINT('Ctrl Pts',(-1.08731332925585,53.1603438158904,-0.452651452877882));
#43699=CARTESIAN_POINT('Ctrl Pts',(-1.09213634622688,53.1612172835387,-0.440870127773195));
#43700=CARTESIAN_POINT('Ctrl Pts',(-1.09428041212785,53.1616103971149,-0.43552112916146));
#43701=CARTESIAN_POINT('Ctrl Pts',(-1.09875157952514,53.1624403755978,-0.424124987647527));
#43702=CARTESIAN_POINT('Ctrl Pts',(-1.10106816727896,53.1628766409014,-0.418074077964121));
#43703=CARTESIAN_POINT('Ctrl Pts',(-1.10745939798681,53.1640990626195,-0.400958554817809));
#43704=CARTESIAN_POINT('Ctrl Pts',(-1.11141811817988,53.1648788071173,-0.389851091641765));
#43705=CARTESIAN_POINT('Ctrl Pts',(-1.14123400628228,53.1709506699302,-0.302044825141836));
#43706=CARTESIAN_POINT('Ctrl Pts',(-1.15929234383037,53.1758839538206,-0.222914798662539));
#43707=CARTESIAN_POINT('Ctrl Pts',(-1.17483202358449,53.1838233515734,-0.0954687539975504));
#43708=CARTESIAN_POINT('Ctrl Pts',(-1.17772296884976,53.1867715638193,-0.0480884055395803));
#43709=CARTESIAN_POINT('Ctrl Pts',(-1.17774981132563,53.18979291915,-0.000666650161686058));
#43710=CARTESIAN_POINT('Ctrl Pts',(-1.17774981213881,53.1897930107793,-0.000665211992267972));
#43711=CARTESIAN_POINT('Ctrl Pts',(-1.17775881074562,53.1908080729105,0.0152667128767563));
#43712=CARTESIAN_POINT('Ctrl Pts',(-1.17744453218618,53.1918307404128,0.0311967694603609));
#43713=CARTESIAN_POINT('Ctrl Pts',(-1.17628672381245,53.1937050423063,0.0601156220613494));
#43714=CARTESIAN_POINT('Ctrl Pts',(-1.1755508580111,53.1945535166369,0.073106114269657));
#43715=CARTESIAN_POINT('Ctrl Pts',(-1.17385945964058,53.19607422811,0.0961856340810697));
#43716=CARTESIAN_POINT('Ctrl Pts',(-1.17298863166316,53.196743851152,0.106279662253863));
#43717=CARTESIAN_POINT('Ctrl Pts',(-1.17105087815903,53.1980480573628,0.125796719961337));
#43718=CARTESIAN_POINT('Ctrl Pts',(-1.17000015236007,53.1986820889182,0.135220591887283));
#43719=CARTESIAN_POINT('Ctrl Pts',(-1.16753584597819,53.2000315893319,0.15513595615592));
#43720=CARTESIAN_POINT('Ctrl Pts',(-1.16609437843298,53.2007478837948,0.165623079140138));
#43721=CARTESIAN_POINT('Ctrl Pts',(-1.16210522261643,53.202564742239,0.192004156347377));
#43722=CARTESIAN_POINT('Ctrl Pts',(-1.15937275888079,53.2036710305287,0.207867519135568));
#43723=CARTESIAN_POINT('Ctrl Pts',(-1.14528736706233,53.208815527063,0.280685607510413));
#43724=CARTESIAN_POINT('Ctrl Pts',(-1.13005828750316,53.212973566722,0.336799700416078));
#43725=CARTESIAN_POINT('Ctrl Pts',(-1.09101171867704,53.2215357586388,0.447566318194352));
#43726=CARTESIAN_POINT('Ctrl Pts',(-1.06705928347146,53.2259311043804,0.502002469110884));
#43727=CARTESIAN_POINT('Ctrl Pts',(-1.02233577947957,53.23284979792,0.58582719210843));
#43728=CARTESIAN_POINT('Ctrl Pts',(-1.00414890491117,53.2354135532736,0.616481481327817));
#43729=CARTESIAN_POINT('Ctrl Pts',(-0.979356217176713,53.2385757476547,
0.654253570115244));
#43730=CARTESIAN_POINT('Ctrl Pts',(-0.974016657234918,53.2392391980329,
0.662176638376606));
#43731=CARTESIAN_POINT('Ctrl Pts',(-0.965164783229106,53.2403098210482,
0.674972638822706));
#43732=CARTESIAN_POINT('Ctrl Pts',(-0.961710676379634,53.2407206233373,
0.679885064873146));
#43733=CARTESIAN_POINT('Ctrl Pts',(-0.954693800564389,53.241540951109,0.689703973520671));
#43734=CARTESIAN_POINT('Ctrl Pts',(-0.951130422153745,53.2419504194311,
0.69460978122075));
#43735=CARTESIAN_POINT('Ctrl Pts',(-0.941693056909727,53.2430170464234,
0.707393673738016));
#43736=CARTESIAN_POINT('Ctrl Pts',(-0.9357579461752,53.2436701693493,0.715226331351325));
#43737=CARTESIAN_POINT('Ctrl Pts',(-0.907347060874671,53.2467196147501,
0.751761460492516));
#43738=CARTESIAN_POINT('Ctrl Pts',(-0.883642479901959,53.2490428235216,
0.779487324018403));
#43739=CARTESIAN_POINT('Ctrl Pts',(-0.80460934965297,53.2562894596543,0.863679333028259));
#43740=CARTESIAN_POINT('Ctrl Pts',(-0.744871180500709,53.2610766954214,
0.915699608718587));
#43741=CARTESIAN_POINT('Ctrl Pts',(-0.647290672665594,53.268586224422,0.984760080301541));
#43742=CARTESIAN_POINT('Ctrl Pts',(-0.613025492960796,53.271170467429,1.00644764598841));
#43743=CARTESIAN_POINT('Ctrl Pts',(-0.565039602314749,53.2747687997538,
1.03345867041337));
#43744=CARTESIAN_POINT('Ctrl Pts',(-0.552235426345082,53.2757268932295,
1.04035694774618));
#43745=CARTESIAN_POINT('Ctrl Pts',(-0.530156632796453,53.2773774206417,
1.05172950752944));
#43746=CARTESIAN_POINT('Ctrl Pts',(-0.520944877503815,53.2780655992446,
1.05632260006367));
#43747=CARTESIAN_POINT('Ctrl Pts',(-0.502075982933415,53.2794749404054,
1.06542401572055));
#43748=CARTESIAN_POINT('Ctrl Pts',(-0.4924155095044,53.2801963423577,1.06992316493672));
#43749=CARTESIAN_POINT('Ctrl Pts',(-0.467687136289251,53.2820432407385,
1.08103401140068));
#43750=CARTESIAN_POINT('Ctrl Pts',(-0.452539724155098,53.2831748567747,
1.0874619723675));
#43751=CARTESIAN_POINT('Ctrl Pts',(-0.37729648407676,53.2888003301564,1.11754792797804));
#43752=CARTESIAN_POINT('Ctrl Pts',(-0.315468594688774,53.2934449294353,
1.13654880284632));
#43753=CARTESIAN_POINT('Ctrl Pts',(-0.204528913663951,53.3017526016701,
1.16088991129994));
#43754=CARTESIAN_POINT('Ctrl Pts',(-0.156044862621687,53.3053722508415,
1.16839524138436));
#43755=CARTESIAN_POINT('Ctrl Pts',(-0.0690196570407146,53.3117479978521,
1.17635195597477));
#43756=CARTESIAN_POINT('Ctrl Pts',(-0.030652948524172,53.314516585301,1.17797649572207));
#43757=CARTESIAN_POINT('Ctrl Pts',(0.017466945641632,53.317886483501,1.17766073989571));
#43758=CARTESIAN_POINT('Ctrl Pts',(0.0272050718706771,53.318563152773,1.17747603466719));
#43759=CARTESIAN_POINT('Ctrl Pts',(0.0429816306332634,53.319649639649,1.17698095863901));
#43760=CARTESIAN_POINT('Ctrl Pts',(0.0490217064016686,53.3200632789158,
1.17674486361693));
#43761=CARTESIAN_POINT('Ctrl Pts',(0.0603547529825577,53.3208346982353,
1.17621446323108));
#43762=CARTESIAN_POINT('Ctrl Pts',(0.0656480315593585,53.3211930751927,
1.17593090713628));
#43763=CARTESIAN_POINT('Ctrl Pts',(0.0798730920925098,53.3221514251488,
1.17507253145257));
#43764=CARTESIAN_POINT('Ctrl Pts',(0.0888007484543166,53.3227478522903,
1.17443160902997));
#43765=CARTESIAN_POINT('Ctrl Pts',(0.123789388982842,53.3250686265806,1.1715184779065));
#43766=CARTESIAN_POINT('Ctrl Pts',(0.149780866389999,53.3267562775609,1.16847989940207));
#43767=CARTESIAN_POINT('Ctrl Pts',(0.180085150454982,53.3287037036864,1.16390914793015));
#43768=CARTESIAN_POINT('Ctrl Pts',(0.184514178616128,53.3289878115911,1.16321523022274));
#43769=CARTESIAN_POINT('Ctrl Pts',(0.188938471457153,53.3292711974063,1.16249615762954));
#43770=CARTESIAN_POINT('',(-1.17774959099604,53.2897949711755,0.000981533826876358));
#43771=CARTESIAN_POINT('Ctrl Pts',(0.188938462305883,53.4282524383066,1.16249615911688));
#43772=CARTESIAN_POINT('Ctrl Pts',(0.186813409162065,53.4281035400925,1.16284154027806));
#43773=CARTESIAN_POINT('Ctrl Pts',(0.18468739932223,53.4279544610923,1.1631810960855));
#43774=CARTESIAN_POINT('Ctrl Pts',(0.12687570163315,53.4238975029053,1.17225199893712));
#43775=CARTESIAN_POINT('Ctrl Pts',(0.070643708420418,53.4198673902119,1.17697918612135));
#43776=CARTESIAN_POINT('Ctrl Pts',(-0.0568402614405747,53.4105834797223,
1.17852680582014));
#43777=CARTESIAN_POINT('Ctrl Pts',(-0.127906998503584,53.405301100624,1.17294324984981));
#43778=CARTESIAN_POINT('Ctrl Pts',(-0.224735460402383,53.3982000323451,
1.15642669540633));
#43779=CARTESIAN_POINT('Ctrl Pts',(-0.251273366197439,53.3962655679825,
1.15095207204492));
#43780=CARTESIAN_POINT('Ctrl Pts',(-0.286395110472615,53.393740482604,1.14243371371532));
#43781=CARTESIAN_POINT('Ctrl Pts',(-0.29516476711775,53.3931129610262,1.14019942227426));
#43782=CARTESIAN_POINT('Ctrl Pts',(-0.3090453074787,53.3921253875346,1.13649211767734));
#43783=CARTESIAN_POINT('Ctrl Pts',(-0.314173259945425,53.3917617790438,
1.13508523962241));
#43784=CARTESIAN_POINT('Ctrl Pts',(-0.325082545142064,53.3909911283218,
1.1320126307487));
#43785=CARTESIAN_POINT('Ctrl Pts',(-0.330861025279416,53.3905846727771,
1.13033722540397));
#43786=CARTESIAN_POINT('Ctrl Pts',(-0.345837456957529,53.3895351682323,
1.12587028734485));
#43787=CARTESIAN_POINT('Ctrl Pts',(-0.35501474216169,53.3888959211898,1.12301023961493));
#43788=CARTESIAN_POINT('Ctrl Pts',(-0.398840073619962,53.3858572439161,
1.10876137297469));
#43789=CARTESIAN_POINT('Ctrl Pts',(-0.432984949879753,53.383531699539,1.09587853487723));
#43790=CARTESIAN_POINT('Ctrl Pts',(-0.554763663171177,53.3752058229106,
1.04334872328381));
#43791=CARTESIAN_POINT('Ctrl Pts',(-0.638050306622606,53.369419163093,0.994601349775795));
#43792=CARTESIAN_POINT('Ctrl Pts',(-0.736859786128382,53.361498645237,0.919197887893779));
#43793=CARTESIAN_POINT('Ctrl Pts',(-0.758611969887773,53.3596815343996,
0.90132945413712));
#43794=CARTESIAN_POINT('Ctrl Pts',(-0.789339855014467,53.3569892355088,
0.874187059736822));
#43795=CARTESIAN_POINT('Ctrl Pts',(-0.798837184083047,53.3561386211128,
0.865516928651321));
#43796=CARTESIAN_POINT('Ctrl Pts',(-0.815498224929902,53.3546116929156,
0.849799177300278));
#43797=CARTESIAN_POINT('Ctrl Pts',(-0.822717386727143,53.3539380070507,
0.8428120119045));
#43798=CARTESIAN_POINT('Ctrl Pts',(-0.837891726661008,53.3524953546382,
0.827744569677094));
#43799=CARTESIAN_POINT('Ctrl Pts',(-0.845821322760341,53.3517253538657,
0.819640099343704));
#43800=CARTESIAN_POINT('Ctrl Pts',(-0.867295829766628,53.3495943180387,
0.797048499563651));
#43801=CARTESIAN_POINT('Ctrl Pts',(-0.880593201602652,53.3482229853186,
0.782332344309234));
#43802=CARTESIAN_POINT('Ctrl Pts',(-0.90976972827318,53.3450922524266,0.748356093704944));
#43803=CARTESIAN_POINT('Ctrl Pts',(-0.925420523200168,53.3433248736112,
0.728913236267799));
#43804=CARTESIAN_POINT('Ctrl Pts',(-0.978867727163318,53.3369668465686,
0.658018005155726));
#43805=CARTESIAN_POINT('Ctrl Pts',(-1.01308388236413,53.3322713101378,0.6040111058606));
#43806=CARTESIAN_POINT('Ctrl Pts',(-1.06651438653906,53.3238301417344,0.502249629217621));
#43807=CARTESIAN_POINT('Ctrl Pts',(-1.08730657253335,53.3200925602846,0.45549202904627));
#43808=CARTESIAN_POINT('Ctrl Pts',(-1.10940960067704,53.3155805326032,0.395560476715898));
#43809=CARTESIAN_POINT('Ctrl Pts',(-1.11362864851105,53.3146878691113,0.383521862535381));
#43810=CARTESIAN_POINT('Ctrl Pts',(-1.11978074298935,53.3133384110953,0.365009228423059));
#43811=CARTESIAN_POINT('Ctrl Pts',(-1.12185492541622,53.3128742580437,0.358583576275452));
#43812=CARTESIAN_POINT('Ctrl Pts',(-1.12556000521974,53.3120282967825,0.346758622549607));
#43813=CARTESIAN_POINT('Ctrl Pts',(-1.12720747915799,53.3116456076217,0.341365154175699));
#43814=CARTESIAN_POINT('Ctrl Pts',(-1.1310201093161,53.3107438968264,0.328554811595778));
#43815=CARTESIAN_POINT('Ctrl Pts',(-1.1331511215039,53.3102268081991,0.321128161097478));
#43816=CARTESIAN_POINT('Ctrl Pts',(-1.14019184177094,53.308470333215,0.295647838116286));
#43817=CARTESIAN_POINT('Ctrl Pts',(-1.14474465707906,53.3072492474254,0.277497465428001));
#43818=CARTESIAN_POINT('Ctrl Pts',(-1.16798841165331,53.3004482943822,0.174491110350817));
#43819=CARTESIAN_POINT('Ctrl Pts',(-1.17767717262205,53.295202567577,0.0878768684682339));
#43820=CARTESIAN_POINT('Ctrl Pts',(-1.17774959099604,53.2897949711755,0.000981533826876358));
#43821=CARTESIAN_POINT('Ctrl Pts',(-1.17774959188343,53.2897949048769,0.000980468466004801));
#43822=CARTESIAN_POINT('Ctrl Pts',(-1.17778032745941,53.2874973357847,-0.0359394461675392));
#43823=CARTESIAN_POINT('Ctrl Pts',(-1.1760750282772,53.2851776679351,-0.0728387245586704));
#43824=CARTESIAN_POINT('Ctrl Pts',(-1.17060466416177,53.2814102869727,-0.131369816716317));
#43825=CARTESIAN_POINT('Ctrl Pts',(-1.1679637027389,53.2799935590884,-0.153081687179469));
#43826=CARTESIAN_POINT('Ctrl Pts',(-1.16318664187066,53.2778800540219,-0.184929044750261));
#43827=CARTESIAN_POINT('Ctrl Pts',(-1.16151878914946,53.2771976563521,-0.195130742575383));
#43828=CARTESIAN_POINT('Ctrl Pts',(-1.15791318200115,53.2758237458455,-0.215497533749276));
#43829=CARTESIAN_POINT('Ctrl Pts',(-1.15597531406087,53.2751322861124,-0.225661662040095));
#43830=CARTESIAN_POINT('Ctrl Pts',(-1.15178709897825,53.2737255845958,-0.246157101937808));
#43831=CARTESIAN_POINT('Ctrl Pts',(-1.14953104667879,53.2730102186906,-0.25648625732619));
#43832=CARTESIAN_POINT('Ctrl Pts',(-1.14350288650903,53.2711981769024,-0.282406620401633));
#43833=CARTESIAN_POINT('Ctrl Pts',(-1.13955084495826,53.2700958358667,-0.297953315096262));
#43834=CARTESIAN_POINT('Ctrl Pts',(-1.12014624288904,53.2650386230242,-0.368242845669103));
#43835=CARTESIAN_POINT('Ctrl Pts',(-1.10105997143721,53.2609692160256,-0.421895301867576));
#43836=CARTESIAN_POINT('Ctrl Pts',(-1.05122151251319,53.2519467010786,-0.535270825702235));
#43837=CARTESIAN_POINT('Ctrl Pts',(-1.01908590543671,53.2469792789337,-0.5941761177014));
#43838=CARTESIAN_POINT('Ctrl Pts',(-0.965430522304102,53.2399318930273,
-0.675243022136471));
#43839=CARTESIAN_POINT('Ctrl Pts',(-0.947776629563363,53.237766860554,-0.699806418748032));
#43840=CARTESIAN_POINT('Ctrl Pts',(-0.923592901813035,53.2350162446476,
-0.730858637897702));
#43841=CARTESIAN_POINT('Ctrl Pts',(-0.917906923567276,53.2343838347964,
-0.737987187947478));
#43842=CARTESIAN_POINT('Ctrl Pts',(-0.908397208115924,53.2333503610177,
-0.749629609715714));
#43843=CARTESIAN_POINT('Ctrl Pts',(-0.904621315083805,53.2329461087124,
-0.754181888744853));
#43844=CARTESIAN_POINT('Ctrl Pts',(-0.896835625858463,53.2321252310991,
-0.763425835864132));
#43845=CARTESIAN_POINT('Ctrl Pts',(-0.892822966764624,53.2317088204095,
-0.76811477077353));
#43846=CARTESIAN_POINT('Ctrl Pts',(-0.881991063398176,53.2306017174844,
-0.780572659862728));
#43847=CARTESIAN_POINT('Ctrl Pts',(-0.875105914172077,53.2299156378716,
-0.78828394022504));
#43848=CARTESIAN_POINT('Ctrl Pts',(-0.835482877495063,53.2260590857437,
-0.831502153501267));
#43849=CARTESIAN_POINT('Ctrl Pts',(-0.800683154047731,53.2230189597548,
-0.865063612500677));
#43850=CARTESIAN_POINT('Ctrl Pts',(-0.711260232793834,53.2157138714024,
-0.941270608347812));
#43851=CARTESIAN_POINT('Ctrl Pts',(-0.654753547313782,53.2114958125317,
-0.981416918827469));
#43852=CARTESIAN_POINT('Ctrl Pts',(-0.562110701056196,53.2047365256981,
-1.03565608545356));
#43853=CARTESIAN_POINT('Ctrl Pts',(-0.528256256625591,53.202297334268,-1.05332656653601));
#43854=CARTESIAN_POINT('Ctrl Pts',(-0.480650104918661,53.1988685050152,
-1.0753018943789));
#43855=CARTESIAN_POINT('Ctrl Pts',(-0.46758698415141,53.1979278791769,-1.08104628508205));
#43856=CARTESIAN_POINT('Ctrl Pts',(-0.444972459158287,53.196298099099,-1.09050424646045));
#43857=CARTESIAN_POINT('Ctrl Pts',(-0.435470844720434,53.1956129286696,
-1.09433319103701));
#43858=CARTESIAN_POINT('Ctrl Pts',(-0.417111462799178,53.1942876460043,
-1.10145466080406));
#43859=CARTESIAN_POINT('Ctrl Pts',(-0.408261611474434,53.1936482116722,
-1.10476549082157));
#43860=CARTESIAN_POINT('Ctrl Pts',(-0.384646999409304,53.1919398817379,
-1.11327749566626));
#43861=CARTESIAN_POINT('Ctrl Pts',(-0.369817191693778,53.1908648946645,
-1.11829124107762));
#43862=CARTESIAN_POINT('Ctrl Pts',(-0.308777666326095,53.1864292751039,
-1.13758092825293));
#43863=CARTESIAN_POINT('Ctrl Pts',(-0.261814987612224,53.1829884726797,
-1.14929798181298));
#43864=CARTESIAN_POINT('Ctrl Pts',(-0.14091030334436,53.1740806924452,-1.17166773033841));
#43865=CARTESIAN_POINT('Ctrl Pts',(-0.0664311877587063,53.1685395185662,
-1.17823896993833));
#43866=CARTESIAN_POINT('Ctrl Pts',(0.0297017437705045,53.1615610568858,
-1.1775723544185));
#43867=CARTESIAN_POINT('Ctrl Pts',(0.0512299188434735,53.1600106316708,
-1.17683237720296));
#43868=CARTESIAN_POINT('Ctrl Pts',(0.0878515010458165,53.1574061502739,
-1.17456664668707));
#43869=CARTESIAN_POINT('Ctrl Pts',(0.102957599117281,53.1563414324886,-1.17333903019491));
#43870=CARTESIAN_POINT('Ctrl Pts',(0.125131928046243,53.1547965974966,-1.17110542523557));
#43871=CARTESIAN_POINT('Ctrl Pts',(0.132220811276758,53.1543054591375,-1.17032627077795));
#43872=CARTESIAN_POINT('Ctrl Pts',(0.144367128060274,53.1534691061801,-1.16887946777974));
#43873=CARTESIAN_POINT('Ctrl Pts',(0.149427832740566,53.1531222193662,-1.16824329807423));
#43874=CARTESIAN_POINT('Ctrl Pts',(0.161392314151985,53.1523058263058,-1.16666024865569));
#43875=CARTESIAN_POINT('Ctrl Pts',(0.168292033439669,53.1518378957449,-1.16568495419912));
#43876=CARTESIAN_POINT('Ctrl Pts',(0.189293012154789,53.1504212694848,-1.16252605034281));
#43877=CARTESIAN_POINT('Ctrl Pts',(0.203364156772529,53.1494826115159,-1.16014728645598));
#43878=CARTESIAN_POINT('Ctrl Pts',(0.291410655436076,53.143655627514,-1.1436115184159));
#43879=CARTESIAN_POINT('Ctrl Pts',(0.363936869121167,53.1390543099286,-1.12263982019768));
#43880=CARTESIAN_POINT('Ctrl Pts',(0.476750192251949,53.1315526342403,-1.07792485768823));
#43881=CARTESIAN_POINT('Ctrl Pts',(0.518497810757143,53.1286955641166,-1.05847643193722));
#43882=CARTESIAN_POINT('Ctrl Pts',(0.585712065282108,53.1238437760148,-1.02223165794898));
#43883=CARTESIAN_POINT('Ctrl Pts',(0.611856906900606,53.1218889494526,-1.00680041283312));
#43884=CARTESIAN_POINT('Ctrl Pts',(0.648481910469745,53.1190320043405,-0.983229743739168));
#43885=CARTESIAN_POINT('Ctrl Pts',(0.659467292674132,53.1181591236908,-0.975895682785428));
#43886=CARTESIAN_POINT('Ctrl Pts',(0.678619516190133,53.1166074435277,-0.962638218147491));
#43887=CARTESIAN_POINT('Ctrl Pts',(0.686838067156415,53.1159316011766,-0.956791641590141));
#43888=CARTESIAN_POINT('Ctrl Pts',(0.703980063034734,53.1145001403933,-0.944262357361838));
#43889=CARTESIAN_POINT('Ctrl Pts',(0.71288569648386,53.1137436892311,-0.937557090245571));
#43890=CARTESIAN_POINT('Ctrl Pts',(0.736619521453132,53.1116921727298,-0.919153649580152));
#43891=CARTESIAN_POINT('Ctrl Pts',(0.751263156528585,53.1103880622523,-0.907223979191796));
#43892=CARTESIAN_POINT('Ctrl Pts',(0.828598280208299,53.1032864833245,-0.841065082488195));
#43893=CARTESIAN_POINT('Ctrl Pts',(0.885709253569833,53.0972361118865,-0.780692154252102));
#43894=CARTESIAN_POINT('Ctrl Pts',(0.973902033390121,53.0865578640274,-0.665213463795146));
#43895=CARTESIAN_POINT('Ctrl Pts',(1.00779882087184,53.0819706078462,-0.612647676529148));
#43896=CARTESIAN_POINT('Ctrl Pts',(1.04247410570068,53.0768258807859,-0.548141430908158));
#43897=CARTESIAN_POINT('Ctrl Pts',(1.04744819706604,53.076074875009,-0.538575514287927));
#43898=CARTESIAN_POINT('Ctrl Pts',(1.05510452984942,53.0748993309761,-0.523343820823535));
#43899=CARTESIAN_POINT('Ctrl Pts',(1.05787397426443,53.0744698218832,-0.517722882322851));
#43900=CARTESIAN_POINT('Ctrl Pts',(1.06311409926472,53.0736491281615,-0.506869755202702));
#43901=CARTESIAN_POINT('Ctrl Pts',(1.06559128397986,53.0732575856574,-0.501641060866144));
#43902=CARTESIAN_POINT('Ctrl Pts',(1.07171797719502,53.0722796003028,-0.4884590152888));
#43903=CARTESIAN_POINT('Ctrl Pts',(1.07531766192179,53.071696099644,-0.480482642433942));
#43904=CARTESIAN_POINT('Ctrl Pts',(1.08865981614971,53.0694959533515,-0.450017223286487));
#43905=CARTESIAN_POINT('Ctrl Pts',(1.09778906223907,53.0679113171205,-0.427264627363491));
#43906=CARTESIAN_POINT('Ctrl Pts',(1.13727080674822,53.0605835154434,-0.319223409920281));
#43907=CARTESIAN_POINT('Ctrl Pts',(1.15843641609231,53.0551368375165,-0.230902366762911));
#43908=CARTESIAN_POINT('Ctrl Pts',(1.17438664714476,53.046785609058,-0.0986529972555718));
#43909=CARTESIAN_POINT('Ctrl Pts',(1.17718957778006,53.044069675923,-0.0560404025092714));
#43910=CARTESIAN_POINT('Ctrl Pts',(1.17784178715581,53.0403183970712,0.00139670291630801));
#43911=CARTESIAN_POINT('Ctrl Pts',(1.17773163731984,53.0393458375014,0.0161673935100462));
#43912=CARTESIAN_POINT('Ctrl Pts',(1.17707241148053,53.0376782933447,0.041259400569131));
#43913=CARTESIAN_POINT('Ctrl Pts',(1.17666519944823,53.0369877952924,0.0515829117962025));
#43914=CARTESIAN_POINT('Ctrl Pts',(1.17556546999635,53.0355805719014,0.072478350259879));
#43915=CARTESIAN_POINT('Ctrl Pts',(1.17486601220825,53.0348636918126,0.0830489376975468));
#43916=CARTESIAN_POINT('Ctrl Pts',(1.17274072100554,53.0330427092746,0.109704068902194));
#43917=CARTESIAN_POINT('Ctrl Pts',(1.17112655396628,53.0319328252079,0.125770945256003));
#43918=CARTESIAN_POINT('Ctrl Pts',(1.16238712106749,53.026897320322,0.197830703730188));
#43919=CARTESIAN_POINT('Ctrl Pts',(1.15157353640139,53.0228593505094,0.253293394710134));
#43920=CARTESIAN_POINT('Ctrl Pts',(1.11928052088419,53.0138572407522,0.372579690749307));
#43921=CARTESIAN_POINT('Ctrl Pts',(1.0962217995729,53.0088769090276,0.435777560097039));
#43922=CARTESIAN_POINT('Ctrl Pts',(1.05513475364238,53.0018136740027,0.52412074150068));
#43923=CARTESIAN_POINT('Ctrl Pts',(1.04131049376399,52.9996454164127,0.551075936517293));
#43924=CARTESIAN_POINT('Ctrl Pts',(1.02199122941377,52.9968917990483,0.585416181385997));
#43925=CARTESIAN_POINT('Ctrl Pts',(1.01742882674944,52.9962594612066,0.593310015051768));
#43926=CARTESIAN_POINT('Ctrl Pts',(1.0097564379765,52.9952260730573,0.606235905446079));
#43927=CARTESIAN_POINT('Ctrl Pts',(1.0066994570074,52.9948218353864,0.61129881881871));
#43928=CARTESIAN_POINT('Ctrl Pts',(1.000374666013,52.9940009535977,0.62159768162832));
#43929=CARTESIAN_POINT('Ctrl Pts',(0.997103612170494,52.9935845244912,0.626831349880083));
#43930=CARTESIAN_POINT('Ctrl Pts',(0.988243481445447,52.9924773151794,0.640762641157766));
#43931=CARTESIAN_POINT('Ctrl Pts',(0.982580631230541,52.9917911491458,0.649413013617887));
#43932=CARTESIAN_POINT('Ctrl Pts',(0.949785162033687,52.9879300941138,0.698098939005781));
#43933=CARTESIAN_POINT('Ctrl Pts',(0.920317624316057,52.98488592719,0.736512426138912));
#43934=CARTESIAN_POINT('Ctrl Pts',(0.843193583304655,52.9775801738212,0.825165955665399));
#43935=CARTESIAN_POINT('Ctrl Pts',(0.79331644543358,52.9733651438873,0.873225736831357));
#43936=CARTESIAN_POINT('Ctrl Pts',(0.709816123139314,52.9666099155097,0.940591292442827));
#43937=CARTESIAN_POINT('Ctrl Pts',(0.678975900981495,52.9641715790578,0.963089920640685));
#43938=CARTESIAN_POINT('Ctrl Pts',(0.635178970055762,52.9607437503787,0.991890274192237));
#43939=CARTESIAN_POINT('Ctrl Pts',(0.623116489623485,52.9598032304498,0.999512106595802));
#43940=CARTESIAN_POINT('Ctrl Pts',(0.602161159445122,52.9581735748295,1.012226226339));
#43941=CARTESIAN_POINT('Ctrl Pts',(0.593334671854942,52.9574884213037,1.01742515747232));
#43942=CARTESIAN_POINT('Ctrl Pts',(0.576238083428325,52.9561631298216,1.02719716718026));
#43943=CARTESIAN_POINT('Ctrl Pts',(0.567978524389655,52.9555236692693,1.03178715624679));
#43944=CARTESIAN_POINT('Ctrl Pts',(0.545889771404482,52.9538151683903,1.04371668524398));
#43945=CARTESIAN_POINT('Ctrl Pts',(0.531968352329282,52.952740034318,1.05088048431595));
#43946=CARTESIAN_POINT('Ctrl Pts',(0.475855384023323,52.9484108869342,1.07835484750512));
#43947=CARTESIAN_POINT('Ctrl Pts',(0.432616738387698,52.945082408327,1.09641657199658));
#43948=CARTESIAN_POINT('Ctrl Pts',(0.323517113591594,52.9367187336731,1.13453012528846));
#43949=CARTESIAN_POINT('Ctrl Pts',(0.256767693375939,52.9316259251028,1.15147199457756));
#43950=CARTESIAN_POINT('Ctrl Pts',(0.188938438127302,52.9266130464139,1.16249616304658));
#43951=CARTESIAN_POINT('Origin',(0.,56.5393671147362,0.));
#43952=CARTESIAN_POINT('',(0.188938462485257,52.327342596858,1.16249615908772));
#43953=CARTESIAN_POINT('',(0.188938431190144,52.4266410775339,1.16249616417406));
#43954=CARTESIAN_POINT('',(0.188938462403162,56.5393671147362,1.16249615910107));
#43955=CARTESIAN_POINT('Ctrl Pts',(0.188938462485257,52.327342596858,1.16249615908772));
#43956=CARTESIAN_POINT('Ctrl Pts',(0.196171651122745,52.3278387177455,1.16132056162071));
#43957=CARTESIAN_POINT('Ctrl Pts',(0.203393645764959,52.3283369745778,1.16007749164273));
#43958=CARTESIAN_POINT('Ctrl Pts',(0.228868425715194,52.3301050656455,1.1554475034012));
#43959=CARTESIAN_POINT('Ctrl Pts',(0.247051330677571,52.3313863019024,1.15169668786707));
#43960=CARTESIAN_POINT('Ctrl Pts',(0.3491060353982,52.3386904527072,1.12811667111043));
#43961=CARTESIAN_POINT('Ctrl Pts',(0.430678164409059,52.3449905913468,1.09956063034604));
#43962=CARTESIAN_POINT('Ctrl Pts',(0.560634907475863,52.3555772552927,1.03737076530023));
#43963=CARTESIAN_POINT('Ctrl Pts',(0.610968992825355,52.3598250712863,1.00854734780391));
#43964=CARTESIAN_POINT('Ctrl Pts',(0.668774236404321,52.364738285421,0.969523432267412));
#43965=CARTESIAN_POINT('Ctrl Pts',(0.678467391372795,52.3655632611532,0.962765127460925));
#43966=CARTESIAN_POINT('Ctrl Pts',(0.693320079048421,52.3668270924489,0.952073722462365));
#43967=CARTESIAN_POINT('Ctrl Pts',(0.698551296394552,52.3672721687913,0.948242161252259));
#43968=CARTESIAN_POINT('Ctrl Pts',(0.708370144731885,52.3681070512215,0.94092507111451));
#43969=CARTESIAN_POINT('Ctrl Pts',(0.712964035420163,52.3684973974311,0.937448951655603));
#43970=CARTESIAN_POINT('Ctrl Pts',(0.723051080066843,52.3693542625305,0.929699214297603));
#43971=CARTESIAN_POINT('Ctrl Pts',(0.728532135178738,52.3698197255308,0.92541041023103));
#43972=CARTESIAN_POINT('Ctrl Pts',(0.747346858309635,52.3714183059802,0.910417532805911));
#43973=CARTESIAN_POINT('Ctrl Pts',(0.760485903516109,52.3725360578737,0.899471329851401));
#43974=CARTESIAN_POINT('Ctrl Pts',(0.834631596224866,52.3788829986527,0.834913493652379));
#43975=CARTESIAN_POINT('Ctrl Pts',(0.890206588434308,52.3838095042527,0.775387303015026));
#43976=CARTESIAN_POINT('Ctrl Pts',(0.967823979591012,52.3917876779878,0.672799921650939));
#43977=CARTESIAN_POINT('Ctrl Pts',(0.994119215925472,52.3947557683597,0.633300387030666));
#43978=CARTESIAN_POINT('Ctrl Pts',(1.0291944075396,52.3992398862333,0.573020779696434));
#43979=CARTESIAN_POINT('Ctrl Pts',(1.03987558456847,52.4006923591232,0.553400946470502));
#43980=CARTESIAN_POINT('Ctrl Pts',(1.05535124954253,52.4029440772238,0.522942426461188));
#43981=CARTESIAN_POINT('Ctrl Pts',(1.06055109112651,52.4037291572135,0.51231475416677));
#43982=CARTESIAN_POINT('Ctrl Pts',(1.06985050906475,52.4051883993447,0.492559670103494));
#43983=CARTESIAN_POINT('Ctrl Pts',(1.07399561434788,52.4058609078884,0.483454806609093));
#43984=CARTESIAN_POINT('Ctrl Pts',(1.08293351437436,52.407361897769,0.463140021270697));
#43985=CARTESIAN_POINT('Ctrl Pts',(1.08766919054945,52.4081922407333,0.451906393173391));
#43986=CARTESIAN_POINT('Ctrl Pts',(1.10101235331791,52.4106390897167,0.418829358223343));
#43987=CARTESIAN_POINT('Ctrl Pts',(1.10914166328743,52.4122711928743,0.396800790904513));
#43988=CARTESIAN_POINT('Ctrl Pts',(1.14453211356754,52.4201043493812,0.291293618111428));
#43989=CARTESIAN_POINT('Ctrl Pts',(1.16305550722178,52.4265728159333,0.205190366441568));
#43990=CARTESIAN_POINT('Ctrl Pts',(1.175252874049,52.4355145986921,0.0839022907124738));
#43991=CARTESIAN_POINT('Ctrl Pts',(1.17719019495639,52.4380047301848,0.0498239371205162));
#43992=CARTESIAN_POINT('Ctrl Pts',(1.1779220454132,52.4419377297626,-0.00504432905393951));
#43993=CARTESIAN_POINT('Ctrl Pts',(1.17765028208433,52.4434079698568,-0.0258017071985731));
#43994=CARTESIAN_POINT('Ctrl Pts',(1.17651273787595,52.4454114526971,-0.0545645959089164));
#43995=CARTESIAN_POINT('Ctrl Pts',(1.17611344113166,52.4459663595309,-0.0625835461111537));
#43996=CARTESIAN_POINT('Ctrl Pts',(1.17528887092577,52.4469095800765,-0.0763146766143366));
#43997=CARTESIAN_POINT('Ctrl Pts',(1.17490388281053,52.4473000085032,-0.0820288478219724));
#43998=CARTESIAN_POINT('Ctrl Pts',(1.17398555018848,52.4481352398934,-0.0943214911849874));
#43999=CARTESIAN_POINT('Ctrl Pts',(1.1734385775851,52.4485793051564,-0.100898590910782));
#44000=CARTESIAN_POINT('Ctrl Pts',(1.17173841001515,52.4498249320783,-0.119452613416765));
#44001=CARTESIAN_POINT('Ctrl Pts',(1.17045689428382,52.4506198415272,-0.131417329850327));
#44002=CARTESIAN_POINT('Ctrl Pts',(1.16017889629268,52.4561425502463,-0.215226109403612));
#44003=CARTESIAN_POINT('Ctrl Pts',(1.14475617797452,52.4605871775781,-0.286135244885433));
#44004=CARTESIAN_POINT('Ctrl Pts',(1.10334909461352,52.4690676938359,-0.417043149141915));
#44005=CARTESIAN_POINT('Ctrl Pts',(1.07870747384763,52.4730843344662,-0.477172188258911));
#44006=CARTESIAN_POINT('Ctrl Pts',(1.03920859046764,52.4786778104778,-0.554642684940989));
#44007=CARTESIAN_POINT('Ctrl Pts',(1.02862395967766,52.4801147490685,-0.574034538726406));
#44008=CARTESIAN_POINT('Ctrl Pts',(1.01156639609088,52.4823475467567,-0.603297068882315));
#44009=CARTESIAN_POINT('Ctrl Pts',(1.00547964633855,52.4831296231111,-0.61338779816486));
#44010=CARTESIAN_POINT('Ctrl Pts',(0.993946682882943,52.4845860254056,-0.631874328570208));
#44011=CARTESIAN_POINT('Ctrl Pts',(0.988542856639564,52.4852587434929,-0.640295389185344));
#44012=CARTESIAN_POINT('Ctrl Pts',(0.976288643407263,52.4867637231263,-0.658866818977799));
#44013=CARTESIAN_POINT('Ctrl Pts',(0.969386004522352,52.4875978972066,-0.668981131851096));
#44014=CARTESIAN_POINT('Ctrl Pts',(0.948168023238092,52.490123254163,-0.699053400857583));
#44015=CARTESIAN_POINT('Ctrl Pts',(0.933385642879342,52.491832004635,-0.718671930163635));
#44016=CARTESIAN_POINT('Ctrl Pts',(0.863560842143729,52.4996874354691,-0.805549366790932));
#44017=CARTESIAN_POINT('Ctrl Pts',(0.801796519832233,52.5060910787434,-0.867043910169488));
#44018=CARTESIAN_POINT('Ctrl Pts',(0.707340262809247,52.5149487474114,-0.942291441033023));
#44019=CARTESIAN_POINT('Ctrl Pts',(0.679934832277706,52.5174217608351,-0.962253758450003));
#44020=CARTESIAN_POINT('Ctrl Pts',(0.634492614857426,52.5213314889796,-0.99244204340386));
#44021=CARTESIAN_POINT('Ctrl Pts',(0.616980787317879,52.5227952258801,-1.0034226024663));
#44022=CARTESIAN_POINT('Ctrl Pts',(0.592286973951487,52.5247915053365,-1.01801544976755));
#44023=CARTESIAN_POINT('Ctrl Pts',(0.58534439071844,52.5253455169918,-1.02202312539194));
#44024=CARTESIAN_POINT('Ctrl Pts',(0.573373841981408,52.5262877256026,-1.02877124668342));
#44025=CARTESIAN_POINT('Ctrl Pts',(0.56836594126289,52.52667802499,-1.03154641349479));
#44026=CARTESIAN_POINT('Ctrl Pts',(0.55753616427182,52.5275135722115,-1.03744500119894));
#44027=CARTESIAN_POINT('Ctrl Pts',(0.55170798364647,52.5279580747668,-1.04055610662811));
#44028=CARTESIAN_POINT('Ctrl Pts',(0.535164285505931,52.5292062029695,-1.04920911849396));
#44029=CARTESIAN_POINT('Ctrl Pts',(0.524389030219952,52.5300031343864,-1.05463584217562));
#44030=CARTESIAN_POINT('Ctrl Pts',(0.448812932927772,52.5354954558795,-1.09125331918974));
#44031=CARTESIAN_POINT('Ctrl Pts',(0.381349316825964,52.5399118333018,-1.11662090376679));
#44032=CARTESIAN_POINT('Ctrl Pts',(0.263441740643995,52.5474641277285,-1.14901166935567));
#44033=CARTESIAN_POINT('Ctrl Pts',(0.214095313704058,52.5505774124116,-1.15922048032076));
#44034=CARTESIAN_POINT('Ctrl Pts',(0.132483319142417,52.5558023539137,-1.17071446300197));
#44035=CARTESIAN_POINT('Ctrl Pts',(0.10054981340637,52.5578648138136,-1.17388825711982));
#44036=CARTESIAN_POINT('Ctrl Pts',(0.055083368844715,52.5608499163235,-1.17653825810153));
#44037=CARTESIAN_POINT('Ctrl Pts',(0.0416261873327244,52.5617393886215,
-1.17709119701653));
#44038=CARTESIAN_POINT('Ctrl Pts',(0.0180435346432932,52.5633100204654,
-1.17765527810999));
#44039=CARTESIAN_POINT('Ctrl Pts',(0.00792172329658865,52.5639879773732,
-1.17776685235916));
#44040=CARTESIAN_POINT('Ctrl Pts',(-0.0132305930733779,52.5654133613249,
-1.17772734036032));
#44041=CARTESIAN_POINT('Ctrl Pts',(-0.024260006717177,52.566161488916,-1.17755177143525));
#44042=CARTESIAN_POINT('Ctrl Pts',(-0.0535777682185026,52.5681638703773,
-1.17667302636727));
#44043=CARTESIAN_POINT('Ctrl Pts',(-0.0718543076942338,52.5694264254686,
-1.17569846514909));
#44044=CARTESIAN_POINT('Ctrl Pts',(-0.178276029554224,52.5768654550174,
-1.16753309495685));
#44045=CARTESIAN_POINT('Ctrl Pts',(-0.265395278060826,52.583336703185,-1.15085874104335));
#44046=CARTESIAN_POINT('Ctrl Pts',(-0.388022558047356,52.5927722468262,
-1.11271513719296));
#44047=CARTESIAN_POINT('Ctrl Pts',(-0.425605811203037,52.5957062176172,
-1.09888876059694));
#44048=CARTESIAN_POINT('Ctrl Pts',(-0.483506222500621,52.6002324317384,
-1.07417073193855));
#44049=CARTESIAN_POINT('Ctrl Pts',(-0.50433272120519,52.6018615488285,-1.06455140660277));
#44050=CARTESIAN_POINT('Ctrl Pts',(-0.532314880737407,52.604039659617,-1.05062131969466));
#44051=CARTESIAN_POINT('Ctrl Pts',(-0.539724026125907,52.6046153205837,
-1.04683440685455));
#44052=CARTESIAN_POINT('Ctrl Pts',(-0.552202372741598,52.6055822602989,
-1.04028885171864));
#44053=CARTESIAN_POINT('Ctrl Pts',(-0.557292465125318,52.6059759386204,
-1.03757094688395));
#44054=CARTESIAN_POINT('Ctrl Pts',(-0.568036310353754,52.6068050611806,
-1.03173228578991));
#44055=CARTESIAN_POINT('Ctrl Pts',(-0.573684666523248,52.6072399311722,
-1.02860228843668));
#44056=CARTESIAN_POINT('Ctrl Pts',(-0.589482160810121,52.6084541221585,
-1.01967760498855));
#44057=CARTESIAN_POINT('Ctrl Pts',(-0.59957151791268,52.609227168136,-1.01377791281077));
#44058=CARTESIAN_POINT('Ctrl Pts',(-0.6756449725309,52.6150505490144,-0.967761326719216));
#44059=CARTESIAN_POINT('Ctrl Pts',(-0.737636419225367,52.6197734007477,
-0.921386932537127));
#44060=CARTESIAN_POINT('Ctrl Pts',(-0.829699530287199,52.6274810253954,
-0.837227105559554));
#44061=CARTESIAN_POINT('Ctrl Pts',(-0.862780206981749,52.6304255373881,
-0.803094284217346));
#44062=CARTESIAN_POINT('Ctrl Pts',(-0.913869488520139,52.6354055286484,
-0.743569677874498));
#44063=CARTESIAN_POINT('Ctrl Pts',(-0.933095162374441,52.6373980600136,
-0.719295817203522));
#44064=CARTESIAN_POINT('Ctrl Pts',(-0.959183015201604,52.6403000565938,
-0.683549523304943));
#44065=CARTESIAN_POINT('Ctrl Pts',(-0.966841827787528,52.6411789369416,
-0.67267292470351));
#44066=CARTESIAN_POINT('Ctrl Pts',(-0.979988850585412,52.6427375424247,
-0.653313804693735));
#44067=CARTESIAN_POINT('Ctrl Pts',(-0.985555296836889,52.6434142230881,
-0.64488589737217));
#44068=CARTESIAN_POINT('Ctrl Pts',(-0.997013933526051,52.6448436619321,
-0.627041974460064));
#44069=CARTESIAN_POINT('Ctrl Pts',(-1.00288266274385,52.6455972053521,-0.617612152854169));
#44070=CARTESIAN_POINT('Ctrl Pts',(-1.01825954509646,52.6476311130092,-0.592107534069492));
#44071=CARTESIAN_POINT('Ctrl Pts',(-1.02751982289569,52.6489202504077,-0.575887816198061));
#44072=CARTESIAN_POINT('Ctrl Pts',(-1.07683240714013,52.6561610300914,-0.484536371018312));
#44073=CARTESIAN_POINT('Ctrl Pts',(-1.10902523012598,52.6623820201597,-0.40546485929945));
#44074=CARTESIAN_POINT('Ctrl Pts',(-1.14891734725186,52.6730502323373,-0.265879183905796));
#44075=CARTESIAN_POINT('Ctrl Pts',(-1.16098181726994,52.6774576454823,-0.206943067781209));
#44076=CARTESIAN_POINT('Ctrl Pts',(-1.16988231714256,52.6824596230565,-0.136356027284769));
#44077=CARTESIAN_POINT('Ctrl Pts',(-1.1711123190639,52.6832312701991,-0.125353742089219));
#44078=CARTESIAN_POINT('Ctrl Pts',(-1.17280139608191,52.6844315634296,-0.108036999848024));
#44079=CARTESIAN_POINT('Ctrl Pts',(-1.17336497576778,52.6848655176651,-0.101733703162982));
#44080=CARTESIAN_POINT('Ctrl Pts',(-1.17434421353911,52.6856888119471,-0.0896876613545392));
#44081=CARTESIAN_POINT('Ctrl Pts',(-1.17476860849671,52.6860785819563,-0.0839459731359289));
#44082=CARTESIAN_POINT('Ctrl Pts',(-1.17562870439996,52.6869504316642,-0.0710210924314333));
#44083=CARTESIAN_POINT('Ctrl Pts',(-1.17604071466418,52.6874312374448,-0.0638364323985576));
#44084=CARTESIAN_POINT('Ctrl Pts',(-1.17728569655548,52.6891490811008,-0.0379824828622398));
#44085=CARTESIAN_POINT('Ctrl Pts',(-1.17774021203685,52.690367539285,-0.0192967495721671));
#44086=CARTESIAN_POINT('Ctrl Pts',(-1.177765383676,52.6935106954921,0.0295479765876257));
#44087=CARTESIAN_POINT('Ctrl Pts',(-1.17662279298064,52.6954090192095,0.0596943640464959));
#44088=CARTESIAN_POINT('Ctrl Pts',(-1.16665160274001,52.7035653177381,0.190138925176396));
#44089=CARTESIAN_POINT('Ctrl Pts',(-1.14614359440823,52.7096447395677,0.289107353461203));
#44090=CARTESIAN_POINT('Ctrl Pts',(-1.1069223761335,52.7174095186163,0.402740667361204));
#44091=CARTESIAN_POINT('Ctrl Pts',(-1.10008570165631,52.7186852023949,0.421056492495837));
#44092=CARTESIAN_POINT('Ctrl Pts',(-1.08854936552971,52.720727897612,0.449761124136841));
#44093=CARTESIAN_POINT('Ctrl Pts',(-1.08414906377245,52.7214849071075,0.460266859746315));
#44094=CARTESIAN_POINT('Ctrl Pts',(-1.07598536042091,52.7228518873122,0.478990853052281));
#44095=CARTESIAN_POINT('Ctrl Pts',(-1.0722783664773,52.7234598907621,0.487232829396527));
#44096=CARTESIAN_POINT('Ctrl Pts',(-1.06331458279389,52.724901311142,0.506564671582463));
#44097=CARTESIAN_POINT('Ctrl Pts',(-1.05797866462153,52.7257374110049,0.517616454231129));
#44098=CARTESIAN_POINT('Ctrl Pts',(-1.04138067273157,52.7282752519403,0.550665049211453));
#44099=CARTESIAN_POINT('Ctrl Pts',(-1.0295986908514,52.7299948211154,0.572391543384777));
#44100=CARTESIAN_POINT('Ctrl Pts',(-1.00009407038046,52.7341206444383,0.622937094852221));
#44101=CARTESIAN_POINT('Ctrl Pts',(-0.981796545910135,52.7365447117542,
0.651393873575988));
#44102=CARTESIAN_POINT('Ctrl Pts',(-0.9357858472675,52.742332496937,0.716599655269995));
#44103=CARTESIAN_POINT('Ctrl Pts',(-0.907092886474679,52.745716412,0.752590439792059));
#44104=CARTESIAN_POINT('Ctrl Pts',(-0.841681774006431,52.7529082628366,
0.82544716812205));
#44105=CARTESIAN_POINT('Ctrl Pts',(-0.804472417794417,52.7567072643138,
0.861751898845221));
#44106=CARTESIAN_POINT('Ctrl Pts',(-0.75525251976073,52.761280319611,0.90379895186724));
#44107=CARTESIAN_POINT('Ctrl Pts',(-0.745384484517787,52.7621762430078,
0.911954449290143));
#44108=CARTESIAN_POINT('Ctrl Pts',(-0.730102805533488,52.763529651934,0.924170268881754));
#44109=CARTESIAN_POINT('Ctrl Pts',(-0.724784220297454,52.7639945563068,
0.928347258420498));
#44110=CARTESIAN_POINT('Ctrl Pts',(-0.714964456120256,52.7648412920009,
0.935923446115648));
#44111=CARTESIAN_POINT('Ctrl Pts',(-0.710474597256807,52.7652240139641,
0.939336318406548));
#44112=CARTESIAN_POINT('Ctrl Pts',(-0.6997845538992,52.7661250549968,0.947341630503309));
#44113=CARTESIAN_POINT('Ctrl Pts',(-0.693563506578452,52.7666414525874,
0.951905592581376));
#44114=CARTESIAN_POINT('Ctrl Pts',(-0.672167972268608,52.7683921727246,
0.9672809354685));
#44115=CARTESIAN_POINT('Ctrl Pts',(-0.656781211079435,52.7696083594457,
0.97779380433841));
#44116=CARTESIAN_POINT('Ctrl Pts',(-0.616856105134819,52.7726742557191,
1.00370434311688));
#44117=CARTESIAN_POINT('Ctrl Pts',(-0.591986822373387,52.7745004791876,
1.01857040900352));
#44118=CARTESIAN_POINT('Ctrl Pts',(-0.486247786169047,52.7820300819112,
1.07659531867141));
#44119=CARTESIAN_POINT('Ctrl Pts',(-0.401034484189394,52.78757098048,1.11115510814235));
#44120=CARTESIAN_POINT('Ctrl Pts',(-0.287138849598926,52.795116869945,1.14251823880059));
#44121=CARTESIAN_POINT('Ctrl Pts',(-0.261373673642282,52.7968303492206,
1.14868632871186));
#44122=CARTESIAN_POINT('Ctrl Pts',(-0.223093649708061,52.7993982344904,
1.15649584918497));
#44123=CARTESIAN_POINT('Ctrl Pts',(-0.21072427367824,52.8002313096336,1.1588134819001));
#44124=CARTESIAN_POINT('Ctrl Pts',(-0.188438782848915,52.8017393902313,
1.16262048236914));
#44125=CARTESIAN_POINT('Ctrl Pts',(-0.178536166173565,52.8024120280386,
1.16418228278888));
#44126=CARTESIAN_POINT('Ctrl Pts',(-0.157212049413898,52.8038664527557,
1.16726697203663));
#44127=CARTESIAN_POINT('Ctrl Pts',(-0.145785800531673,52.804649457314,1.16874903051094));
#44128=CARTESIAN_POINT('Ctrl Pts',(-0.113731958332498,52.80685710428,1.17242927023569));
#44129=CARTESIAN_POINT('Ctrl Pts',(-0.0930662321954791,52.808293312736,
1.17425037081808));
#44130=CARTESIAN_POINT('Ctrl Pts',(-0.0458985163730122,52.8116024769584,
1.17715397474442));
#44131=CARTESIAN_POINT('Ctrl Pts',(-0.0193870819109981,52.8134848556146,
1.17788883912925));
#44132=CARTESIAN_POINT('Ctrl Pts',(0.0680534839491707,52.8197631486888,
1.1773598461867));
#44133=CARTESIAN_POINT('Ctrl Pts',(0.128840879173521,52.8242451618814,1.17226371691588));
#44134=CARTESIAN_POINT('Ctrl Pts',(0.188938518720853,52.8287166258961,1.16249614994785));
#44135=CARTESIAN_POINT('Ctrl Pts',(0.188938438127302,52.9266130464139,1.16249616304658));
#44136=CARTESIAN_POINT('Ctrl Pts',(0.181906598859068,52.9260933627305,1.16363903540241));
#44137=CARTESIAN_POINT('Ctrl Pts',(0.17486314581592,52.9255746504092,1.1647183075498));
#44138=CARTESIAN_POINT('Ctrl Pts',(0.13621166039432,52.9227394587882,1.17028224020324));
#44139=CARTESIAN_POINT('Ctrl Pts',(0.10443945363839,52.9204498064909,1.1735445955169));
#44140=CARTESIAN_POINT('Ctrl Pts',(0.0633266670875664,52.917569703251,1.17608272809651));
#44141=CARTESIAN_POINT('Ctrl Pts',(0.0540753257050632,52.9169270140479,
1.17654439901917));
#44142=CARTESIAN_POINT('Ctrl Pts',(0.0388801636704436,52.9158812967143,
1.17712306832208));
#44143=CARTESIAN_POINT('Ctrl Pts',(0.0329393436406825,52.9154749349046,
1.17730428947039));
#44144=CARTESIAN_POINT('Ctrl Pts',(0.0216221551707913,52.9147058577791,
1.17756377788745));
#44145=CARTESIAN_POINT('Ctrl Pts',(0.0162462129984789,52.9143426743784,
1.17765021635223));
#44146=CARTESIAN_POINT('Ctrl Pts',(0.00149830396955103,52.9133517724962,
1.17778633407267));
#44147=CARTESIAN_POINT('Ctrl Pts',(-0.00787419318824625,52.9127280487827,
1.17776097090682));
#44148=CARTESIAN_POINT('Ctrl Pts',(-0.0478188541366931,52.9100915902299,
1.17717599981353));
#44149=CARTESIAN_POINT('Ctrl Pts',(-0.0783657939029402,52.9081297142182,
1.17553780081192));
#44150=CARTESIAN_POINT('Ctrl Pts',(-0.19289970007592,52.9008637378609,1.16491010448066));
#44151=CARTESIAN_POINT('Ctrl Pts',(-0.275901630913065,52.8957642627541,
1.14808774296736));
#44152=CARTESIAN_POINT('Ctrl Pts',(-0.396061866709044,52.8878529163917,
1.10993793189134));
#44153=CARTESIAN_POINT('Ctrl Pts',(-0.435030549143859,52.8852017812498,
1.09525115356684));
#44154=CARTESIAN_POINT('Ctrl Pts',(-0.486562206428158,52.8815257603364,
1.07264494802227));
#44155=CARTESIAN_POINT('Ctrl Pts',(-0.499875174370029,52.8805602674396,
1.06650585735951));
#44156=CARTESIAN_POINT('Ctrl Pts',(-0.522351270285795,52.8789011177469,
1.05562803140338));
#44157=CARTESIAN_POINT('Ctrl Pts',(-0.531573265884883,52.8782118350317,
1.05101438700445));
#44158=CARTESIAN_POINT('Ctrl Pts',(-0.549058018298693,52.8768879806953,
1.04197800704493));
#44159=CARTESIAN_POINT('Ctrl Pts',(-0.557330925851231,52.8762542006003,
1.0375765537301));
#44160=CARTESIAN_POINT('Ctrl Pts',(-0.578883214502724,52.8745830974489,
1.02577791508226));
#44161=CARTESIAN_POINT('Ctrl Pts',(-0.592073072739325,52.8735401724103,
1.01822175665989));
#44162=CARTESIAN_POINT('Ctrl Pts',(-0.642883879259474,52.86944096029,0.987792357298786));
#44163=CARTESIAN_POINT('Ctrl Pts',(-0.6793526504809,52.8663192799724,0.963074540591081));
#44164=CARTESIAN_POINT('Ctrl Pts',(-0.777206008517299,52.8574358252869,
0.88842353066654));
#44165=CARTESIAN_POINT('Ctrl Pts',(-0.835069758050751,52.8515600969101,
0.834267775943299));
#44166=CARTESIAN_POINT('Ctrl Pts',(-0.908417975346589,52.843460625658,0.750283320685518));
#44167=CARTESIAN_POINT('Ctrl Pts',(-0.928748479518946,52.8411317482933,
0.724965472104622));
#44168=CARTESIAN_POINT('Ctrl Pts',(-0.953531150504212,52.8382109928372,
0.691346529663212));
#44169=CARTESIAN_POINT('Ctrl Pts',(-0.958964730488236,52.8375651241213,
0.683789688826118));
#44170=CARTESIAN_POINT('Ctrl Pts',(-0.967725769423283,52.8365156122482,
0.671295262164273));
#44171=CARTESIAN_POINT('Ctrl Pts',(-0.971106294035118,52.8361085902616,
0.666395576711511));
#44172=CARTESIAN_POINT('Ctrl Pts',(-0.977887037183352,52.8352882912651,
0.656406476846597));
#44173=CARTESIAN_POINT('Ctrl Pts',(-0.98128499976818,52.8348751575827,0.65131580194277));
#44174=CARTESIAN_POINT('Ctrl Pts',(-0.990184077780535,52.833786982268,0.637755860543223));
#44175=CARTESIAN_POINT('Ctrl Pts',(-0.995616347847002,52.8331162808337,
0.629241726607294));
#44176=CARTESIAN_POINT('Ctrl Pts',(-1.02300423154385,52.8296951949845,0.585073162091319));
#44177=CARTESIAN_POINT('Ctrl Pts',(-1.04315893103414,52.8270421033696,0.54833244859142));
#44178=CARTESIAN_POINT('Ctrl Pts',(-1.09356505759076,52.8197806544029,0.443558471921142));
#44179=CARTESIAN_POINT('Ctrl Pts',(-1.11939110898145,52.8152606228773,0.373620702405441));
#44180=CARTESIAN_POINT('Ctrl Pts',(-1.14530267813639,52.8089004472211,0.275849202589395));
#44181=CARTESIAN_POINT('Ctrl Pts',(-1.15127349530915,52.807200868551,0.249760295454077));
#44182=CARTESIAN_POINT('Ctrl Pts',(-1.16031292406317,52.8041302438282,0.202990156727357));
#44183=CARTESIAN_POINT('Ctrl Pts',(-1.16372922625291,52.8027696076362,0.182387739896717));
#44184=CARTESIAN_POINT('Ctrl Pts',(-1.16818135313701,52.8006300127655,0.150268824493119));
#44185=CARTESIAN_POINT('Ctrl Pts',(-1.169598416476,52.7998630300252,0.138808939472798));
#44186=CARTESIAN_POINT('Ctrl Pts',(-1.17192991205189,52.7984205694787,0.117370038574803));
#44187=CARTESIAN_POINT('Ctrl Pts',(-1.17288593598726,52.7977464684418,0.10739653220063));
#44188=CARTESIAN_POINT('Ctrl Pts',(-1.17475178551673,52.7962195123387,0.0849150313132307));
#44189=CARTESIAN_POINT('Ctrl Pts',(-1.17558929322518,52.7953644665255,0.0724024339286911));
#44190=CARTESIAN_POINT('Ctrl Pts',(-1.17725342309204,52.7931162398901,0.0397134172702676));
#44191=CARTESIAN_POINT('Ctrl Pts',(-1.17776119790702,52.7917134245488,0.0195256588717659));
#44192=CARTESIAN_POINT('Ctrl Pts',(-1.17772228042435,52.7868666274024,-0.0494890055778496));
#44193=CARTESIAN_POINT('Ctrl Pts',(-1.1746586924823,52.7833516387715,-0.098259350422583));
#44194=CARTESIAN_POINT('Ctrl Pts',(-1.15759350849066,52.7733518789253,-0.234202272227691));
#44195=CARTESIAN_POINT('Ctrl Pts',(-1.13681386911742,52.7667721350037,-0.320201156339612));
#44196=CARTESIAN_POINT('Ctrl Pts',(-1.10255237704474,52.7597157197357,-0.414264533395263));
#44197=CARTESIAN_POINT('Ctrl Pts',(-1.09830753023619,52.7588838258475,-0.425390930887397));
#44198=CARTESIAN_POINT('Ctrl Pts',(-1.09145915320445,52.7576068648468,-0.44255526823521));
#44199=CARTESIAN_POINT('Ctrl Pts',(-1.08897272250366,52.7571555419762,-0.448638678052654));
#44200=CARTESIAN_POINT('Ctrl Pts',(-1.08422234434106,52.7563162664717,-0.459988944599663));
#44201=CARTESIAN_POINT('Ctrl Pts',(-1.08197077739439,52.7559276738912,-0.465260313648089));
#44202=CARTESIAN_POINT('Ctrl Pts',(-1.07645466363868,52.7549971134014,-0.477918011817304));
#44203=CARTESIAN_POINT('Ctrl Pts',(-1.07315249237172,52.7544573812662,-0.485287549991492));
#44204=CARTESIAN_POINT('Ctrl Pts',(-1.06094994788232,52.7525220392577,-0.511786471750085));
#44205=CARTESIAN_POINT('Ctrl Pts',(-1.05161123212238,52.7511501130849,-0.530710966313526));
#44206=CARTESIAN_POINT('Ctrl Pts',(-1.02544017024571,52.7475529811635,-0.580338550912572));
#44207=CARTESIAN_POINT('Ctrl Pts',(-1.00773850964026,52.7453627920869,-0.610560229967278));
#44208=CARTESIAN_POINT('Ctrl Pts',(-0.939049798397481,52.7375157395071,
-0.716683504310696));
#44209=CARTESIAN_POINT('Ctrl Pts',(-0.880624762888923,52.7319590957658,
-0.787368210049975));
#44210=CARTESIAN_POINT('Ctrl Pts',(-0.79978879547614,52.7247427456121,-0.864785772890295));
#44211=CARTESIAN_POINT('Ctrl Pts',(-0.784593666891378,52.7234049457621,
-0.878595041350704));
#44212=CARTESIAN_POINT('Ctrl Pts',(-0.760265293487885,52.7212858331393,
-0.899569986643057));
#44213=CARTESIAN_POINT('Ctrl Pts',(-0.751373440706584,52.7205158724955,
-0.90701015090022));
#44214=CARTESIAN_POINT('Ctrl Pts',(-0.734598769735623,52.7190707807433,
-0.920630221515992));
#44215=CARTESIAN_POINT('Ctrl Pts',(-0.726744094783247,52.7183970730516,
-0.926843226888218));
#44216=CARTESIAN_POINT('Ctrl Pts',(-0.708928539050146,52.7168749934932,
-0.940569528396011));
#44217=CARTESIAN_POINT('Ctrl Pts',(-0.698925713276865,52.7160244908762,
-0.948026127034976));
#44218=CARTESIAN_POINT('Ctrl Pts',(-0.667820044868065,52.7133910495522,
-0.970453944445982));
#44219=CARTESIAN_POINT('Ctrl Pts',(-0.646342065953354,52.7115882187465,
-0.984888939333304));
#44220=CARTESIAN_POINT('Ctrl Pts',(-0.593767799108988,52.7072093180907,
-1.01776259932172));
#44221=CARTESIAN_POINT('Ctrl Pts',(-0.562265037543508,52.7046122034898,
-1.03549917241062));
#44222=CARTESIAN_POINT('Ctrl Pts',(-0.491542845406176,52.6988542375696,
-1.07113730572529));
#44223=CARTESIAN_POINT('Ctrl Pts',(-0.452053674883491,52.6956845642826,
-1.08839180976296));
#44224=CARTESIAN_POINT('Ctrl Pts',(-0.364074766241985,52.6887883924813,
-1.12121792668024));
#44225=CARTESIAN_POINT('Ctrl Pts',(-0.315334080498396,52.6850712455849,
-1.13588970763363));
#44226=CARTESIAN_POINT('Ctrl Pts',(-0.253380478849017,52.6805793668379,
-1.15024160693782));
#44227=CARTESIAN_POINT('Ctrl Pts',(-0.240920698487838,52.67968763602,-1.1529157260412));
#44228=CARTESIAN_POINT('Ctrl Pts',(-0.221798439052521,52.6783392869666,
-1.15669618521147));
#44229=CARTESIAN_POINT('Ctrl Pts',(-0.215166182252834,52.6778753276757,
-1.15794824241359));
#44230=CARTESIAN_POINT('Ctrl Pts',(-0.202972377554019,52.6770295320652,
-1.16014183902186));
#44231=CARTESIAN_POINT('Ctrl Pts',(-0.197414530335856,52.676646817697,-1.16110050288303));
#44232=CARTESIAN_POINT('Ctrl Pts',(-0.184222789972167,52.6757448044647,
-1.16327846220754));
#44233=CARTESIAN_POINT('Ctrl Pts',(-0.176583463842287,52.6752274427226,
-1.16446258222668));
#44234=CARTESIAN_POINT('Ctrl Pts',(-0.150390429735297,52.6734689071876,
-1.16825888486413));
#44235=CARTESIAN_POINT('Ctrl Pts',(-0.131785346967884,52.672246091833,-1.17050366044697));
#44236=CARTESIAN_POINT('Ctrl Pts',(-0.0840621937397945,52.6691583607835,
-1.17510919383224));
#44237=CARTESIAN_POINT('Ctrl Pts',(-0.0548947492583419,52.6673173603891,
-1.17683255119244));
#44238=CARTESIAN_POINT('Ctrl Pts',(0.0677091935300681,52.6596638094872,
-1.17950769661));
#44239=CARTESIAN_POINT('Ctrl Pts',(0.161016125991956,52.6540171461394,-1.17042582142129));
#44240=CARTESIAN_POINT('Ctrl Pts',(0.276759310421148,52.6464321961513,-1.14504493454523));
#44241=CARTESIAN_POINT('Ctrl Pts',(0.301069189325804,52.6448075706934,-1.13889455992838));
#44242=CARTESIAN_POINT('Ctrl Pts',(0.337018175520609,52.6423470641,-1.1285680988567));
#44243=CARTESIAN_POINT('Ctrl Pts',(0.348818717861868,52.6415299179226,-1.1249767496357));
#44244=CARTESIAN_POINT('Ctrl Pts',(0.370086596117126,52.6400388299362,-1.1181373390153));
#44245=CARTESIAN_POINT('Ctrl Pts',(0.379573181725984,52.6393670230533,-1.11495263871227));
#44246=CARTESIAN_POINT('Ctrl Pts',(0.400064109053508,52.6379007505945,-1.10778189885467));
#44247=CARTESIAN_POINT('Ctrl Pts',(0.41105183340377,52.6371048860821,-1.10375196475852));
#44248=CARTESIAN_POINT('Ctrl Pts',(0.442218638734939,52.634818956425,-1.09179109261006));
#44249=CARTESIAN_POINT('Ctrl Pts',(0.462240326416332,52.6333159521476,-1.08346614468807));
#44250=CARTESIAN_POINT('Ctrl Pts',(0.50771928533553,52.6298197399259,-1.06306610536183));
#44251=CARTESIAN_POINT('Ctrl Pts',(0.532995152792648,52.6278154460824,-1.05062094735149));
#44252=CARTESIAN_POINT('Ctrl Pts',(0.632455545667665,52.6196863061562,-0.997136088127851));
#44253=CARTESIAN_POINT('Ctrl Pts',(0.702552210371302,52.6133769405874,-0.949051606142162));
#44254=CARTESIAN_POINT('Ctrl Pts',(0.789835286476483,52.6050368306206,-0.87416830964758));
#44255=CARTESIAN_POINT('Ctrl Pts',(0.812027254455015,52.602869659613,-0.853593626583031));
#44256=CARTESIAN_POINT('Ctrl Pts',(0.840006537915129,52.6001002051549,-0.825573370914851));
#44257=CARTESIAN_POINT('Ctrl Pts',(0.84653031502051,52.5994516805885,-0.818882662053815));
#44258=CARTESIAN_POINT('Ctrl Pts',(0.856677758948102,52.5984394976818,-0.808224678025534));
#44259=CARTESIAN_POINT('Ctrl Pts',(0.860354932776254,52.5980719799747,-0.804309210084399));
#44260=CARTESIAN_POINT('Ctrl Pts',(0.868048115189813,52.5973017948987,-0.796004348983089));
#44261=CARTESIAN_POINT('Ctrl Pts',(0.872057897725546,52.5968996309935,-0.791609423695176));
#44262=CARTESIAN_POINT('Ctrl Pts',(0.882243505568154,52.5958755838328,-0.780274158625251));
#44263=CARTESIAN_POINT('Ctrl Pts',(0.888370990041231,52.5952571566659,-0.773290607286997));
#44264=CARTESIAN_POINT('Ctrl Pts',(0.915398026528667,52.5925147233279,-0.741742324743234));
#44265=CARTESIAN_POINT('Ctrl Pts',(0.935367755335194,52.5904481448974,-0.716395687755391));
#44266=CARTESIAN_POINT('Ctrl Pts',(0.999881325762435,52.5835056864066,-0.627206563362836));
#44267=CARTESIAN_POINT('Ctrl Pts',(1.03912921748367,52.5787907983908,-0.55978768652984));
#44268=CARTESIAN_POINT('Ctrl Pts',(1.09023205448077,52.5710944043338,-0.447814112016011));
#44269=CARTESIAN_POINT('Ctrl Pts',(1.1066321696032,52.5682226168149,-0.405595841143059));
#44270=CARTESIAN_POINT('Ctrl Pts',(1.12527327894334,52.5642731892322,-0.347978999651666));
#44271=CARTESIAN_POINT('Ctrl Pts',(1.12970034055336,52.5632664814413,-0.33332632872761));
#44272=CARTESIAN_POINT('Ctrl Pts',(1.13638019880628,52.5616272775998,-0.309553316830945));
#44273=CARTESIAN_POINT('Ctrl Pts',(1.13881171790684,52.5610006195028,-0.300484732831128));
#44274=CARTESIAN_POINT('Ctrl Pts',(1.14368147155595,52.5596794277044,-0.281413807457504));
#44275=CARTESIAN_POINT('Ctrl Pts',(1.14609748590941,52.5589842382201,-0.271406669912734));
#44276=CARTESIAN_POINT('Ctrl Pts',(1.15161387722742,52.5572952549841,-0.247169235243929));
#44277=CARTESIAN_POINT('Ctrl Pts',(1.15458201295071,52.5562973360079,-0.232910916611048));
#44278=CARTESIAN_POINT('Ctrl Pts',(1.16484487403713,52.552476589013,-0.178578995901162));
#44279=CARTESIAN_POINT('Ctrl Pts',(1.17032276321948,52.5495981822774,-0.138195512783588));
#44280=CARTESIAN_POINT('Ctrl Pts',(1.18032627252935,52.5409179343216,-0.0179137724509621));
#44281=CARTESIAN_POINT('Ctrl Pts',(1.17881891960564,52.5349795580874,0.0622509924898277));
#44282=CARTESIAN_POINT('Ctrl Pts',(1.16494913882073,52.5265799410599,0.176747227426));
#44283=CARTESIAN_POINT('Ctrl Pts',(1.15911560859603,52.5240336215335,0.211654354553783));
#44284=CARTESIAN_POINT('Ctrl Pts',(1.1496771754735,52.5208720834665,0.255798387554034));
#44285=CARTESIAN_POINT('Ctrl Pts',(1.14751663792708,52.5201935471815,0.265322453529812));
#44286=CARTESIAN_POINT('Ctrl Pts',(1.14382632806066,52.5191048925738,0.280700878711885));
#44287=CARTESIAN_POINT('Ctrl Pts',(1.14236952194913,52.518690924289,0.286572035587541));
#44288=CARTESIAN_POINT('Ctrl Pts',(1.13937402648438,52.5178705985368,0.298258393139576));
#44289=CARTESIAN_POINT('Ctrl Pts',(1.13783589650262,52.5174642283304,0.304073540059658));
#44290=CARTESIAN_POINT('Ctrl Pts',(1.13372592377178,52.5164152220568,0.319143948115073));
#44291=CARTESIAN_POINT('Ctrl Pts',(1.1310852253008,52.5157763811104,0.328380203120146));
#44292=CARTESIAN_POINT('Ctrl Pts',(1.11790393628216,52.5127440364702,0.372437057665053));
#44293=CARTESIAN_POINT('Ctrl Pts',(1.10586573671166,52.5104240431187,0.406792434895543));
#44294=CARTESIAN_POINT('Ctrl Pts',(1.05329926740777,52.5016009234835,0.53712380592191));
#44295=CARTESIAN_POINT('Ctrl Pts',(1.00170711262517,52.4953503630184,0.628112222109145));
#44296=CARTESIAN_POINT('Ctrl Pts',(0.925094626857716,52.4872015735636,0.729254279172741));
#44297=CARTESIAN_POINT('Ctrl Pts',(0.910847009357528,52.4857247634979,0.746973553409694));
#44298=CARTESIAN_POINT('Ctrl Pts',(0.888281837209385,52.4834347985403,0.773430963462203));
#44299=CARTESIAN_POINT('Ctrl Pts',(0.880327556883455,52.4826362885093,0.782472652677561));
#44300=CARTESIAN_POINT('Ctrl Pts',(0.865517796643294,52.4811641730241,0.798795327606991));
#44301=CARTESIAN_POINT('Ctrl Pts',(0.858705483207773,52.480492425786,0.806114082598959));
#44302=CARTESIAN_POINT('Ctrl Pts',(0.843539836985375,52.4790081181306,0.821996779447248));
#44303=CARTESIAN_POINT('Ctrl Pts',(0.835147626903749,52.4781939095742,0.830521874948095));
#44304=CARTESIAN_POINT('Ctrl Pts',(0.810216809466123,52.4757948151914,0.855087456784489));
#44305=CARTESIAN_POINT('Ctrl Pts',(0.793336485999797,52.4741948854623,0.870771455473966));
#44306=CARTESIAN_POINT('Ctrl Pts',(0.695115777203812,52.4650151243897,0.956803523791352));
#44307=CARTESIAN_POINT('Ctrl Pts',(0.604907023323138,52.4570043680273,1.01623754623564));
#44308=CARTESIAN_POINT('Ctrl Pts',(0.478168302727825,52.4467924540513,1.07681817625857));
#44309=CARTESIAN_POINT('Ctrl Pts',(0.447831796083334,52.444423703512,1.08978410638973));
#44310=CARTESIAN_POINT('Ctrl Pts',(0.408004685847074,52.4414427077446,1.10486176258627));
#44311=CARTESIAN_POINT('Ctrl Pts',(0.398979255703781,52.4407755216141,1.10815292568126));
#44312=CARTESIAN_POINT('Ctrl Pts',(0.384799070346671,52.4397413779465,1.11312808039989));
#44313=CARTESIAN_POINT('Ctrl Pts',(0.379671473402264,52.4393702858129,1.11488744867132));
#44314=CARTESIAN_POINT('Ctrl Pts',(0.368938736097225,52.4385997608268,1.11848740407647));
#44315=CARTESIAN_POINT('Ctrl Pts',(0.363331602395777,52.4382007615289,1.1203213882282));
#44316=CARTESIAN_POINT('Ctrl Pts',(0.349095760541582,52.4371961712028,1.12485953530908));
#44317=CARTESIAN_POINT('Ctrl Pts',(0.340449022952916,52.4365937761482,1.1275066738277));
#44318=CARTESIAN_POINT('Ctrl Pts',(0.303485243734229,52.4340482303545,1.13835886172159));
#44319=CARTESIAN_POINT('Ctrl Pts',(0.2748936922188,52.4321528036768,1.14559939002129));
#44320=CARTESIAN_POINT('Ctrl Pts',(0.227104160080551,52.4290600039825,1.15580898541881));
#44321=CARTESIAN_POINT('Ctrl Pts',(0.208058427749336,52.4278469008698,1.15938862518547));
#44322=CARTESIAN_POINT('Ctrl Pts',(0.188938431190144,52.4266410775339,1.16249616417406));
#44323=CARTESIAN_POINT('Origin',(0.,56.5393671147362,0.));
#44324=CARTESIAN_POINT('',(0.188969603130339,51.8285263152314,1.16268601701705));
#44325=CARTESIAN_POINT('',(0.188938462126305,51.9282531127635,1.16249615914606));
#44326=CARTESIAN_POINT('',(0.188938462403162,56.5393671147362,1.16249615910107));
#44327=CARTESIAN_POINT('',(-1.17791180984087,52.190632781682,0.00106564231497296));
#44328=CARTESIAN_POINT('Ctrl Pts',(-1.17791180984087,52.190632781682,0.00106564231497296));
#44329=CARTESIAN_POINT('Ctrl Pts',(-1.17509560602191,52.1700025203108,-0.30407589982206));
#44330=CARTESIAN_POINT('Ctrl Pts',(-0.898229779831263,52.1229140282017,
-1.00509144888255));
#44331=CARTESIAN_POINT('Ctrl Pts',(0.282546404343134,52.0493673053545,-1.36302106179178));
#44332=CARTESIAN_POINT('Ctrl Pts',(1.29832817159957,51.9699926131404,-0.501998847764824));
#44333=CARTESIAN_POINT('Ctrl Pts',(1.13850416835778,51.8963789497659,0.722572407938825));
#44334=CARTESIAN_POINT('Ctrl Pts',(0.49061617699014,51.8492235171297,1.11051665842283));
#44335=CARTESIAN_POINT('Ctrl Pts',(0.188969603130438,51.8285263152314,1.16268601701703));
#44336=CARTESIAN_POINT('Ctrl Pts',(-1.17774952282607,52.1907260775544,0.00106018062369387));
#44337=CARTESIAN_POINT('Ctrl Pts',(-1.17769032918845,52.1955572321385,0.0668181061152723));
#44338=CARTESIAN_POINT('Ctrl Pts',(-1.17212401445883,52.2004044666048,0.132462828800205));
#44339=CARTESIAN_POINT('Ctrl Pts',(-1.15963262707197,52.2056613724927,0.205972093646308));
#44340=CARTESIAN_POINT('Ctrl Pts',(-1.15806296705408,52.2062770878784,0.214621779343263));
#44341=CARTESIAN_POINT('Ctrl Pts',(-1.15493407317965,52.2074243986727,0.230828665966669));
#44342=CARTESIAN_POINT('Ctrl Pts',(-1.15339713908044,52.2079570419198,0.238389668752796));
#44343=CARTESIAN_POINT('Ctrl Pts',(-1.15060829706119,52.2088719746045,0.251450621687845));
#44344=CARTESIAN_POINT('Ctrl Pts',(-1.14939101848722,52.2092561139653,0.256957506328754));
#44345=CARTESIAN_POINT('Ctrl Pts',(-1.14662717537469,52.2100958285269,0.269048161890698));
#44346=CARTESIAN_POINT('Ctrl Pts',(-1.14506340845786,52.2105504427024,0.275627627351889));
#44347=CARTESIAN_POINT('Ctrl Pts',(-1.1403759545603,52.2118570065992,0.294621109323544));
#44348=CARTESIAN_POINT('Ctrl Pts',(-1.13710634302001,52.2127012458732,0.306998555720624));
#44349=CARTESIAN_POINT('Ctrl Pts',(-1.11855251730717,52.2171675021267,0.372867334790528));
#44350=CARTESIAN_POINT('Ctrl Pts',(-1.09969290062369,52.2206295643553,0.425284273843428));
#44351=CARTESIAN_POINT('Ctrl Pts',(-1.05271337054164,52.2278181382191,0.531560338401379));
#44352=CARTESIAN_POINT('Ctrl Pts',(-1.02399714289803,52.2315324211238,0.58497119338871));
#44353=CARTESIAN_POINT('Ctrl Pts',(-0.972067975520965,52.2376039740117,
0.665918785559562));
#44354=CARTESIAN_POINT('Ctrl Pts',(-0.951484922760657,52.2398858524232,
0.695010829204178));
#44355=CARTESIAN_POINT('Ctrl Pts',(-0.921037639220623,52.2431313858768,
0.734152550303415));
#44356=CARTESIAN_POINT('Ctrl Pts',(-0.912263281477002,52.2440530670737,
0.745027501352338));
#44357=CARTESIAN_POINT('Ctrl Pts',(-0.896754242571542,52.2456608338553,
0.763564588169125));
#44358=CARTESIAN_POINT('Ctrl Pts',(-0.890109537705958,52.2463432294325,
0.771300234377256));
#44359=CARTESIAN_POINT('Ctrl Pts',(-0.876200791494203,52.2477591689183,
0.787073429130178));
#44360=CARTESIAN_POINT('Ctrl Pts',(-0.868924647305794,52.2484931807043,
0.795098958274607));
#44361=CARTESIAN_POINT('Ctrl Pts',(-0.849724605774908,52.250413584928,0.815698107404455));
#44362=CARTESIAN_POINT('Ctrl Pts',(-0.837632464274675,52.2516070989924,
0.82811056444853));
#44363=CARTESIAN_POINT('Ctrl Pts',(-0.757202645107037,52.2594483670187,
0.907106504759963));
#44364=CARTESIAN_POINT('Ctrl Pts',(-0.681273277581618,52.2664498296871,
0.965431528704813));
#44365=CARTESIAN_POINT('Ctrl Pts',(-0.567686819930333,52.276136274248,1.03255192367435));
#44366=CARTESIAN_POINT('Ctrl Pts',(-0.535359389987347,52.2788101948645,
1.0496772939016));
#44367=CARTESIAN_POINT('Ctrl Pts',(-0.48266911596462,52.2829911610762,1.07452127169366));
#44368=CARTESIAN_POINT('Ctrl Pts',(-0.46279896966515,52.2845294175151,1.08322790429643));
#44369=CARTESIAN_POINT('Ctrl Pts',(-0.435139478996361,52.2866079736698,
1.09444745546263));
#44370=CARTESIAN_POINT('Ctrl Pts',(-0.427548748799424,52.2871720232298,
1.09743504404926));
#44371=CARTESIAN_POINT('Ctrl Pts',(-0.414559908927411,52.2881256347495,
1.10239201258553));
#44372=CARTESIAN_POINT('Ctrl Pts',(-0.409177425888736,52.2885174368609,
1.10440115335904));
#44373=CARTESIAN_POINT('Ctrl Pts',(-0.397642524409573,52.2893497030525,
1.10861092045666));
#44374=CARTESIAN_POINT('Ctrl Pts',(-0.391486202744324,52.2897895042055,
1.11079985071822));
#44375=CARTESIAN_POINT('Ctrl Pts',(-0.374230612917388,52.2910108418874,
1.11677393495456));
#44376=CARTESIAN_POINT('Ctrl Pts',(-0.363092226138677,52.2917861280334,
1.120444837762));
#44377=CARTESIAN_POINT('Ctrl Pts',(-0.279689054895377,52.2975074559658,
1.14655777292831));
#44378=CARTESIAN_POINT('Ctrl Pts',(-0.205456961507612,52.3021407684921,
1.16215799588203));
#44379=CARTESIAN_POINT('Ctrl Pts',(-0.0822393927391659,52.30980038585,1.17586718374556));
#44380=CARTESIAN_POINT('Ctrl Pts',(-0.0339651744219333,52.3127921893129,
1.17824992676322));
#44381=CARTESIAN_POINT('Ctrl Pts',(0.0455902504196925,52.3178411260906,
1.17728279789795));
#44382=CARTESIAN_POINT('Ctrl Pts',(0.0768341325579911,52.3198536061909,
1.17565705583618));
#44383=CARTESIAN_POINT('Ctrl Pts',(0.121268123307562,52.3227793350942,1.17156618523389));
#44384=CARTESIAN_POINT('Ctrl Pts',(0.134539625419161,52.3236612725303,1.17011638275284));
#44385=CARTESIAN_POINT('Ctrl Pts',(0.157809661834293,52.3252233382632,1.16717321406119));
#44386=CARTESIAN_POINT('Ctrl Pts',(0.167819125526565,52.3259003765286,1.16577610678777));
#44387=CARTESIAN_POINT('Ctrl Pts',(0.18152174898344,52.3268346504193,1.16368338578293));
#44388=CARTESIAN_POINT('Ctrl Pts',(0.185231575714379,52.3270883432989,1.16309863289516));
#44389=CARTESIAN_POINT('Ctrl Pts',(0.188938462485257,52.327342596858,1.16249615908772));
#44390=CARTESIAN_POINT('',(-1.17774983784145,52.2885366798091,-0.000618032721413477));
#44391=CARTESIAN_POINT('Ctrl Pts',(0.188938431190144,52.4266410775339,1.16249616417406));
#44392=CARTESIAN_POINT('Ctrl Pts',(0.151776937535318,52.4242974476015,1.1685359555542));
#44393=CARTESIAN_POINT('Ctrl Pts',(0.114334940736222,52.4219807809433,1.17279236171814));
#44394=CARTESIAN_POINT('Ctrl Pts',(0.0103317987625297,52.415535040879,1.17958352216524));
#44395=CARTESIAN_POINT('Ctrl Pts',(-0.056317377535304,52.4113854067649,
1.17828301993316));
#44396=CARTESIAN_POINT('Ctrl Pts',(-0.139007659187246,52.4059797257572,
1.16963565313208));
#44397=CARTESIAN_POINT('Ctrl Pts',(-0.155480588527765,52.404890484846,1.16756003360845));
#44398=CARTESIAN_POINT('Ctrl Pts',(-0.182473313775796,52.403082364707,1.16357754584739));
#44399=CARTESIAN_POINT('Ctrl Pts',(-0.193021112465399,52.4023699407749,
1.16187437049363));
#44400=CARTESIAN_POINT('Ctrl Pts',(-0.213660572531504,52.4009636371381,
1.15825287326899));
#44401=CARTESIAN_POINT('Ctrl Pts',(-0.22375320930376,52.4002701660734,1.15634555750961));
#44402=CARTESIAN_POINT('Ctrl Pts',(-0.247961293708739,52.3985922456276,
1.15144190489947));
#44403=CARTESIAN_POINT('Ctrl Pts',(-0.262048831482203,52.3976038045563,
1.14831774391731));
#44404=CARTESIAN_POINT('Ctrl Pts',(-0.314506945949762,52.3938763675163,
1.13566867702898));
#44405=CARTESIAN_POINT('Ctrl Pts',(-0.352443815663349,52.3910853182319,
1.12447352369067));
#44406=CARTESIAN_POINT('Ctrl Pts',(-0.460148504921617,52.3828868676463,
1.08670372802051));
#44407=CARTESIAN_POINT('Ctrl Pts',(-0.528045283947793,52.377363069702,1.05538056774806));
#44408=CARTESIAN_POINT('Ctrl Pts',(-0.628442439534823,52.3688701594635,
0.996936954408797));
#44409=CARTESIAN_POINT('Ctrl Pts',(-0.663240633826223,52.3658618403467,
0.974133335401085));
#44410=CARTESIAN_POINT('Ctrl Pts',(-0.704913086445368,52.3622379520388,
0.943554340942552));
#44411=CARTESIAN_POINT('Ctrl Pts',(-0.712986233733124,52.3615349063379,
0.9374688803604));
#44412=CARTESIAN_POINT('Ctrl Pts',(-0.725821580860414,52.3604168322989,
0.9275319833291));
#44413=CARTESIAN_POINT('Ctrl Pts',(-0.730633644072275,52.3599975863512,
0.923746193396292));
#44414=CARTESIAN_POINT('Ctrl Pts',(-0.740064153585596,52.3591761831589,
0.916207139592121));
#44415=CARTESIAN_POINT('Ctrl Pts',(-0.744684063678281,52.3587739111755,
0.912456093285352));
#44416=CARTESIAN_POINT('Ctrl Pts',(-0.756449312333146,52.3577492113737,
0.902754649692739));
#44417=CARTESIAN_POINT('Ctrl Pts',(-0.763553161930051,52.3571302484279,
0.896754203860163));
#44418=CARTESIAN_POINT('Ctrl Pts',(-0.795050379857613,52.3543808245062,
0.86950359687441));
#44419=CARTESIAN_POINT('Ctrl Pts',(-0.818635198461108,52.3523081537633,
0.847336074031021));
#44420=CARTESIAN_POINT('Ctrl Pts',(-0.896159246305273,52.3453223769718,
0.768207804278992));
#44421=CARTESIAN_POINT('Ctrl Pts',(-0.945308991245935,52.3405724328453,
0.70684976184605));
#44422=CARTESIAN_POINT('Ctrl Pts',(-1.01230515582932,52.3328722911216,0.603595695889756));
#44423=CARTESIAN_POINT('Ctrl Pts',(-1.03446057187771,52.330037095084,0.564783297154932));
#44424=CARTESIAN_POINT('Ctrl Pts',(-1.06115463939068,52.3261296745812,0.511154150840396));
#44425=CARTESIAN_POINT('Ctrl Pts',(-1.06768549417148,52.3251263076712,0.497368459867585));
#44426=CARTESIAN_POINT('Ctrl Pts',(-1.07779693388072,52.3234910526919,0.474907163525413));
#44427=CARTESIAN_POINT('Ctrl Pts',(-1.08154491185726,52.3228649462714,0.466308524065008));
#44428=CARTESIAN_POINT('Ctrl Pts',(-1.08919331255543,52.3215437085533,0.448173112589151));
#44429=CARTESIAN_POINT('Ctrl Pts',(-1.09307207574571,52.3208479079449,0.438628130004939));
#44430=CARTESIAN_POINT('Ctrl Pts',(-1.10214738196751,52.3191550241177,0.415427104644542));
#44431=CARTESIAN_POINT('Ctrl Pts',(-1.10721587552223,52.3181537684348,0.40172316606238));
#44432=CARTESIAN_POINT('Ctrl Pts',(-1.12558645437666,52.3142993566739,0.349062508197249));
#44433=CARTESIAN_POINT('Ctrl Pts',(-1.13709649825678,52.3113893178904,0.309516341717001));
#44434=CARTESIAN_POINT('Ctrl Pts',(-1.16731769116475,52.3018853919439,0.180926186713959));
#44435=CARTESIAN_POINT('Ctrl Pts',(-1.17779754836018,52.2950991319486,0.0903011917011576));
#44436=CARTESIAN_POINT('Ctrl Pts',(-1.17774983784145,52.2885366798091,-0.000618032721413477));
#44437=CARTESIAN_POINT('Ctrl Pts',(-1.17774983694482,52.288536556651,-0.000619739009734618));
#44438=CARTESIAN_POINT('Ctrl Pts',(-1.1777403719914,52.2872382631056,-0.0186069032548436));
#44439=CARTESIAN_POINT('Ctrl Pts',(-1.17731884383651,52.2859508669133,-0.0365926453733845));
#44440=CARTESIAN_POINT('Ctrl Pts',(-1.17593148901231,52.2838345935358,-0.0665068767745185));
#44441=CARTESIAN_POINT('Ctrl Pts',(-1.17519566071235,52.2829968513179,-0.0784424466870239));
#44442=CARTESIAN_POINT('Ctrl Pts',(-1.17383721644222,52.2817696162845,-0.0960951484339259));
#44443=CARTESIAN_POINT('Ctrl Pts',(-1.17335433743197,52.2813733305676,-0.10182185667435));
#44444=CARTESIAN_POINT('Ctrl Pts',(-1.17232804037805,52.2806027288331,-0.113014121334299));
#44445=CARTESIAN_POINT('Ctrl Pts',(-1.17178827100923,52.280228242115,-0.118479867256508));
#44446=CARTESIAN_POINT('Ctrl Pts',(-1.17052468247312,52.279414335236,-0.130420358555844));
#44447=CARTESIAN_POINT('Ctrl Pts',(-1.16978535268175,52.2789757671257,-0.1368931551809));
#44448=CARTESIAN_POINT('Ctrl Pts',(-1.16757498741823,52.2777610765878,-0.154917052144064));
#44449=CARTESIAN_POINT('Ctrl Pts',(-1.16598626240294,52.276991098589,-0.166453312947383));
#44450=CARTESIAN_POINT('Ctrl Pts',(-1.15616375299055,52.272734574301,-0.230711172826921));
#44451=CARTESIAN_POINT('Ctrl Pts',(-1.14452457587011,52.2694007019304,-0.282855252500812));
#44452=CARTESIAN_POINT('Ctrl Pts',(-1.11280521327593,52.2624721833434,-0.39009973665874));
#44453=CARTESIAN_POINT('Ctrl Pts',(-1.09207212252354,52.2588908043713,-0.444849997557872));
#44454=CARTESIAN_POINT('Ctrl Pts',(-1.05021288775303,52.2526703424289,-0.534596550502616));
#44455=CARTESIAN_POINT('Ctrl Pts',(-1.0311798510326,52.2500838596863,-0.570445600843968));
#44456=CARTESIAN_POINT('Ctrl Pts',(-1.00286230924222,52.2464830706194,-0.61771661188198));
#44457=CARTESIAN_POINT('Ctrl Pts',(-0.995157422317599,52.2455248748821,
-0.63005420234133));
#44458=CARTESIAN_POINT('Ctrl Pts',(-0.981614285113403,52.2438743723243,
-0.650872006609772));
#44459=CARTESIAN_POINT('Ctrl Pts',(-0.975889598715612,52.2431863241964,
-0.659424334816853));
#44460=CARTESIAN_POINT('Ctrl Pts',(-0.964013022111139,52.24177743545,-0.676673791131825));
#44461=CARTESIAN_POINT('Ctrl Pts',(-0.957853753611336,52.2410563578078,
-0.685364647520231));
#44462=CARTESIAN_POINT('Ctrl Pts',(-0.941890225642806,52.2392107009956,
-0.70725395770583));
#44463=CARTESIAN_POINT('Ctrl Pts',(-0.93192620100281,52.2380800151868,-0.720332468988305));
#44464=CARTESIAN_POINT('Ctrl Pts',(-0.881534318612431,52.2324609281526,
-0.78367937871711));
#44465=CARTESIAN_POINT('Ctrl Pts',(-0.837303464381893,52.2278221486448,
-0.830768708239352));
#44466=CARTESIAN_POINT('Ctrl Pts',(-0.753148904395042,52.2195277127737,
-0.906782453666861));
#44467=CARTESIAN_POINT('Ctrl Pts',(-0.714843039290224,52.2159155122293,
-0.937276422915876));
#44468=CARTESIAN_POINT('Ctrl Pts',(-0.643152045014247,52.209533125377,-0.987388980286748));
#44469=CARTESIAN_POINT('Ctrl Pts',(-0.610482887388668,52.2067510612345,
-1.00791507205607));
#44470=CARTESIAN_POINT('Ctrl Pts',(-0.568363204924382,52.2033677017779,
-1.03157809639927));
#44471=CARTESIAN_POINT('Ctrl Pts',(-0.559804545166975,52.2026903388203,
-1.03624755179716));
#44472=CARTESIAN_POINT('Ctrl Pts',(-0.545846045107572,52.2016030930085,
-1.04363964305366));
#44473=CARTESIAN_POINT('Ctrl Pts',(-0.540481687608634,52.2011893775031,
-1.04642780880987));
#44474=CARTESIAN_POINT('Ctrl Pts',(-0.53037694355811,52.2004181039419,-1.05158139093778));
#44475=CARTESIAN_POINT('Ctrl Pts',(-0.525641644892445,52.2000599462283,
-1.05395635005732));
#44476=CARTESIAN_POINT('Ctrl Pts',(-0.512875211630375,52.1991026904452,
-1.06025183084785));
#44477=CARTESIAN_POINT('Ctrl Pts',(-0.504815018707006,52.1985071249533,
-1.06411312206855));
#44478=CARTESIAN_POINT('Ctrl Pts',(-0.473087804209049,52.196194057678,-1.07887061504756));
#44479=CARTESIAN_POINT('Ctrl Pts',(-0.449104151052207,52.1945129462332,
-1.08907279828412));
#44480=CARTESIAN_POINT('Ctrl Pts',(-0.341887070871989,52.1872071361727,
-1.13053568256093));
#44481=CARTESIAN_POINT('Ctrl Pts',(-0.255607036281239,52.1818528927625,
-1.1531109208811));
#44482=CARTESIAN_POINT('Ctrl Pts',(-0.125624171152407,52.1736181012188,
-1.17179875744618));
#44483=CARTESIAN_POINT('Ctrl Pts',(-0.0833533954457211,52.1709184605159,
-1.1755617374923));
#44484=CARTESIAN_POINT('Ctrl Pts',(-0.0262408219167813,52.1671860909148,
-1.17754992843183));
#44485=CARTESIAN_POINT('Ctrl Pts',(-0.0114991196386139,52.1662152851507,
-1.17778612358545));
#44486=CARTESIAN_POINT('Ctrl Pts',(0.0135690026387033,52.1645498261323,
-1.17771710521445));
#44487=CARTESIAN_POINT('Ctrl Pts',(0.0238942854261437,52.1638596314378,
-1.17755286474316));
#44488=CARTESIAN_POINT('Ctrl Pts',(0.0448117046894879,52.1624522289535,
-1.17694491870802));
#44489=CARTESIAN_POINT('Ctrl Pts',(0.0554026549048939,52.1617348565697,
-1.17649392839258));
#44490=CARTESIAN_POINT('Ctrl Pts',(0.082141738014007,52.1599109721799,-1.17499346137691));
#44491=CARTESIAN_POINT('Ctrl Pts',(0.0982765511894411,52.1587986406084,
-1.17375405142512));
#44492=CARTESIAN_POINT('Ctrl Pts',(0.171621875077245,52.1536860080998,-1.16659711205167));
#44493=CARTESIAN_POINT('Ctrl Pts',(0.228369254966916,52.1495686203159,-1.15682696709697));
#44494=CARTESIAN_POINT('Ctrl Pts',(0.366723419396678,52.1391772254808,-1.122428396953));
#44495=CARTESIAN_POINT('Ctrl Pts',(0.446810743289781,52.1328341812726,-1.09301977991834));
#44496=CARTESIAN_POINT('Ctrl Pts',(0.537109170645427,52.125672451709,-1.04826315385924));
#44497=CARTESIAN_POINT('Ctrl Pts',(0.55104582959916,52.1245675457531,-1.0410045405235));
#44498=CARTESIAN_POINT('Ctrl Pts',(0.571178889405893,52.1229763535234,-1.03000098249192));
#44499=CARTESIAN_POINT('Ctrl Pts',(0.57749205349628,52.1224781311048,-1.02647468678925));
#44500=CARTESIAN_POINT('Ctrl Pts',(0.58868930128599,52.1215963123575,-1.02008431877586));
#44501=CARTESIAN_POINT('Ctrl Pts',(0.593585698103853,52.1212113858194,-1.01724290781309));
#44502=CARTESIAN_POINT('Ctrl Pts',(0.604638617511671,52.1203439702858,-1.01072184053095));
#44503=CARTESIAN_POINT('Ctrl Pts',(0.610782258868511,52.119862824206,-1.00702111972516));
#44504=CARTESIAN_POINT('Ctrl Pts',(0.629992400998763,52.1183602494314,-0.995209097555777));
#44505=CARTESIAN_POINT('Ctrl Pts',(0.64293462123777,52.1173507115199,-0.986897512649443));
#44506=CARTESIAN_POINT('Ctrl Pts',(0.717365879306775,52.1115382076419,-0.937011296165858));
#44507=CARTESIAN_POINT('Ctrl Pts',(0.774983511676959,52.107004151812,-0.889947778610385));
#44508=CARTESIAN_POINT('Ctrl Pts',(0.860255345979937,52.099592756026,-0.805691381819712));
#44509=CARTESIAN_POINT('Ctrl Pts',(0.890825245205523,52.0967582923776,-0.771756335652682));
#44510=CARTESIAN_POINT('Ctrl Pts',(0.938218338109724,52.0919397654832,-0.712567844610764));
#44511=CARTESIAN_POINT('Ctrl Pts',(0.956174460348708,52.0899948220292,-0.688285367962155));
#44512=CARTESIAN_POINT('Ctrl Pts',(0.980602373277928,52.0871496603094,-0.652447592520935));
#44513=CARTESIAN_POINT('Ctrl Pts',(0.987844159318308,52.0862783314602,-0.641430252712317));
#44514=CARTESIAN_POINT('Ctrl Pts',(1.00029525960691,52.0847283950172,-0.621776583646575));
#44515=CARTESIAN_POINT('Ctrl Pts',(1.00558152725818,52.0840527215541,-0.613190433330888));
#44516=CARTESIAN_POINT('Ctrl Pts',(1.01648502048386,52.082620574544,-0.594960338404486));
#44517=CARTESIAN_POINT('Ctrl Pts',(1.02207668217603,52.0818632550563,-0.585302350828057));
#44518=CARTESIAN_POINT('Ctrl Pts',(1.03678923532306,52.0798066669288,-0.559036772026138));
#44519=CARTESIAN_POINT('Ctrl Pts',(1.04564765340926,52.0784982753005,-0.542286771969206));
#44520=CARTESIAN_POINT('Ctrl Pts',(1.0907425530647,52.0714428712162,-0.45180207873871));
#44521=CARTESIAN_POINT('Ctrl Pts',(1.11958731859395,52.0654481658967,-0.374652266226838));
#44522=CARTESIAN_POINT('Ctrl Pts',(1.15569911571883,52.054858333392,-0.235149441131119));
#44523=CARTESIAN_POINT('Ctrl Pts',(1.16647140392589,52.0503038645972,-0.17401610427116));
#44524=CARTESIAN_POINT('Ctrl Pts',(1.17346852803646,52.0451408053934,-0.100977138017322));
#44525=CARTESIAN_POINT('Ctrl Pts',(1.17439015863073,52.0443463432203,-0.0896244845025087));
#44526=CARTESIAN_POINT('Ctrl Pts',(1.17557188497231,52.0431189023227,-0.0718796988791239));
#44527=CARTESIAN_POINT('Ctrl Pts',(1.17594481629151,52.042680231108,-0.0654961201234137));
#44528=CARTESIAN_POINT('Ctrl Pts',(1.17655315600599,52.0418542150555,-0.0533903239583587));
#44529=CARTESIAN_POINT('Ctrl Pts',(1.17679884593558,52.0414663620027,-0.047668995519125));
#44530=CARTESIAN_POINT('Ctrl Pts',(1.17730229496443,52.0405145247213,-0.0335422347585907));
#44531=CARTESIAN_POINT('Ctrl Pts',(1.17751178621274,52.0399531384632,-0.0251352110354523));
#44532=CARTESIAN_POINT('Ctrl Pts',(1.17794292822382,52.0379421085983,0.00521964359023661));
#44533=CARTESIAN_POINT('Ctrl Pts',(1.17764112803403,52.0365178209452,0.0271717178510554));
#44534=CARTESIAN_POINT('Ctrl Pts',(1.1738852236081,52.0307547079956,0.11717788314597));
#44535=CARTESIAN_POINT('Ctrl Pts',(1.16514259118797,52.0265936629039,0.184882192837355));
#44536=CARTESIAN_POINT('Ctrl Pts',(1.14132434971256,52.0196905084355,0.293868329754557));
#44537=CARTESIAN_POINT('Ctrl Pts',(1.12971762054493,52.0169882983758,0.335734398410216));
#44538=CARTESIAN_POINT('Ctrl Pts',(1.10646969669675,52.0123655056645,0.404567721056985));
#44539=CARTESIAN_POINT('Ctrl Pts',(1.09608433504862,52.0104796886056,0.431913352261917));
#44540=CARTESIAN_POINT('Ctrl Pts',(1.07961409093504,52.0077051256446,0.470848611551983));
#44541=CARTESIAN_POINT('Ctrl Pts',(1.07433654751678,52.0068432289193,0.482769055017956));
#44542=CARTESIAN_POINT('Ctrl Pts',(1.06463539382427,52.0053038335937,0.503733911713669));
#44543=CARTESIAN_POINT('Ctrl Pts',(1.06029157369158,52.0046291294446,0.512813946309728));
#44544=CARTESIAN_POINT('Ctrl Pts',(1.05085301851314,52.0031925222142,0.531910962571707));
#44545=CARTESIAN_POINT('Ctrl Pts',(1.04573025006512,52.0024296903396,0.541912878046723));
#44546=CARTESIAN_POINT('Ctrl Pts',(1.03140812917354,52.0003408345125,0.56891650022364));
#44547=CARTESIAN_POINT('Ctrl Pts',(1.02193241607423,51.9990051858091,0.585766824654158));
#44548=CARTESIAN_POINT('Ctrl Pts',(0.977902374343339,51.9929929596424,0.659741385520175));
#44549=CARTESIAN_POINT('Ctrl Pts',(0.938947417248091,51.9881620763671,0.714091748749712));
#44550=CARTESIAN_POINT('Ctrl Pts',(0.860344746519498,51.9792857709142,0.806132834848466));
#44551=CARTESIAN_POINT('Ctrl Pts',(0.822269868392659,51.9752749732389,0.844935380225857));
#44552=CARTESIAN_POINT('Ctrl Pts',(0.767739788395041,51.9700062307639,0.893317771083572));
#44553=CARTESIAN_POINT('Ctrl Pts',(0.753535473665955,51.968673152623,0.905331644784492));
#44554=CARTESIAN_POINT('Ctrl Pts',(0.728445017333622,51.9663931783941,0.925553077666798));
#44555=CARTESIAN_POINT('Ctrl Pts',(0.717690117892988,51.965438591955,0.933917328932445));
#44556=CARTESIAN_POINT('Ctrl Pts',(0.701316746098178,51.964021911007,0.946201212835682));
#44557=CARTESIAN_POINT('Ctrl Pts',(0.695805661787833,51.9635511410837,0.950261227464638));
#44558=CARTESIAN_POINT('Ctrl Pts',(0.685656593472072,51.9626956851575,0.957602405910396));
#44559=CARTESIAN_POINT('Ctrl Pts',(0.681029992262129,51.9623100650167,0.960898269246158));
#44560=CARTESIAN_POINT('Ctrl Pts',(0.670245717798173,51.9614210488624,0.968463668681551));
#44561=CARTESIAN_POINT('Ctrl Pts',(0.664070900610058,51.9609193070479,0.972708099163669));
#44562=CARTESIAN_POINT('Ctrl Pts',(0.643737550666441,51.9592892858567,0.986400904725979));
#44563=CARTESIAN_POINT('Ctrl Pts',(0.629413979444286,51.9581758021688,0.99560177430357));
#44564=CARTESIAN_POINT('Ctrl Pts',(0.530237200948051,51.9506637114619,1.05631253364499));
#44565=CARTESIAN_POINT('Ctrl Pts',(0.439359774789711,51.9447212659783,1.09723064688237));
#44566=CARTESIAN_POINT('Ctrl Pts',(0.302413612722851,51.935752898069,1.13910946384714));
#44567=CARTESIAN_POINT('Ctrl Pts',(0.259728364594098,51.9329607543732,1.14959336961719));
#44568=CARTESIAN_POINT('Ctrl Pts',(0.207372205591597,51.9294833560839,1.15938742853693));
#44569=CARTESIAN_POINT('Ctrl Pts',(0.19816421891786,51.928869914521,1.16099671307355));
#44570=CARTESIAN_POINT('Ctrl Pts',(0.188938462126305,51.9282531127635,1.16249615914606));
#44571=CARTESIAN_POINT('Origin',(0.,56.5393671147362,0.));
#44572=CARTESIAN_POINT('',(0.188938476720627,51.3293408135491,1.16249615677407));
#44573=CARTESIAN_POINT('',(0.18893837638019,51.427308721746,1.16249617308222));
#44574=CARTESIAN_POINT('',(0.188938462403162,56.5393671147362,1.16249615910107));
#44575=CARTESIAN_POINT('',(-1.1759637632873,51.6905636633131,-0.000120924575849058));
#44576=CARTESIAN_POINT('Ctrl Pts',(0.188938476720627,51.3293408135491,1.16249615677407));
#44577=CARTESIAN_POINT('Ctrl Pts',(0.204295852302049,51.330455194193,1.1600001492545));
#44578=CARTESIAN_POINT('Ctrl Pts',(0.219605556065176,51.3315599139334,1.15719952874471));
#44579=CARTESIAN_POINT('Ctrl Pts',(0.244849227074782,51.3333665079355,1.15206244040771));
#44580=CARTESIAN_POINT('Ctrl Pts',(0.254813562702692,51.3340757249261,1.14989959416533));
#44581=CARTESIAN_POINT('Ctrl Pts',(0.270733855217703,51.3352012759797,1.14622683936605));
#44582=CARTESIAN_POINT('Ctrl Pts',(0.276708021107776,51.3356219212953,1.14479931125938));
#44583=CARTESIAN_POINT('Ctrl Pts',(0.288436004635372,51.33644393593,1.14189973358364));
#44584=CARTESIAN_POINT('Ctrl Pts',(0.294190329613003,51.3368454438984,1.14043078830291));
#44585=CARTESIAN_POINT('Ctrl Pts',(0.308862464739228,51.3378651232474,1.13656689101226));
#44586=CARTESIAN_POINT('Ctrl Pts',(0.317763905949887,51.3384798991231,1.13411041492814));
#44587=CARTESIAN_POINT('Ctrl Pts',(0.356968644934529,51.3411742672938,1.12279347700888));
#44588=CARTESIAN_POINT('Ctrl Pts',(0.386940005314877,51.3431988982505,1.11282056608089));
#44589=CARTESIAN_POINT('Ctrl Pts',(0.485569861913291,51.3498545785977,1.07553385702165));
#44590=CARTESIAN_POINT('Ctrl Pts',(0.552054677732486,51.3543387212165,1.04297066901577));
#44591=CARTESIAN_POINT('Ctrl Pts',(0.656921200479987,51.3620050616451,0.978754222567422));
#44592=CARTESIAN_POINT('Ctrl Pts',(0.697140598540821,51.3651094298262,0.950525892203683));
#44593=CARTESIAN_POINT('Ctrl Pts',(0.747760118634869,51.3693319094633,0.910053361990254));
#44594=CARTESIAN_POINT('Ctrl Pts',(0.759843090062958,51.3703652733622,0.899989309212623));
#44595=CARTESIAN_POINT('Ctrl Pts',(0.778868986899859,51.3720361994635,0.883486113322305));
#44596=CARTESIAN_POINT('Ctrl Pts',(0.785942290698183,51.3726674692766,0.877199702457655));
#44597=CARTESIAN_POINT('Ctrl Pts',(0.80050894637034,51.3739891992263,0.863935939547535));
#44598=CARTESIAN_POINT('Ctrl Pts',(0.807988572685473,51.3746802130497,0.856944768198668));
#44599=CARTESIAN_POINT('Ctrl Pts',(0.825638188645483,51.3763412224887,0.840011250165949));
#44600=CARTESIAN_POINT('Ctrl Pts',(0.835720877618183,51.3773150033367,0.829980663980266));
#44601=CARTESIAN_POINT('Ctrl Pts',(0.871896093397634,51.3809030047322,0.792664782158837));
#44602=CARTESIAN_POINT('Ctrl Pts',(0.89685187925694,51.3835642420602,0.76431434781571));
#44603=CARTESIAN_POINT('Ctrl Pts',(0.962601441431847,51.3911198173678,0.681959202705431));
#44604=CARTESIAN_POINT('Ctrl Pts',(1.00016672617909,51.3961070886962,0.625567686225429));
#44605=CARTESIAN_POINT('Ctrl Pts',(1.05688066439141,51.4047603351659,0.522141111607394));
#44606=CARTESIAN_POINT('Ctrl Pts',(1.07822830368233,51.4084263908152,0.476500644738953));
#44607=CARTESIAN_POINT('Ctrl Pts',(1.10037299088285,51.4126857675529,0.419978327210269));
#44608=CARTESIAN_POINT('Ctrl Pts',(1.10402693406528,51.4134071443497,0.410276811301175));
#44609=CARTESIAN_POINT('Ctrl Pts',(1.10965364885438,51.4145472772309,0.394717641142936));
#44610=CARTESIAN_POINT('Ctrl Pts',(1.11170914159685,51.4149705327324,0.388890763026007));
#44611=CARTESIAN_POINT('Ctrl Pts',(1.11564160126565,51.4157934254934,0.377457062311811));
#44612=CARTESIAN_POINT('Ctrl Pts',(1.11752236302791,51.4161932493194,0.37185183444179));
#44613=CARTESIAN_POINT('Ctrl Pts',(1.12219110335492,51.4172025713412,0.357582199403794));
#44614=CARTESIAN_POINT('Ctrl Pts',(1.12492107481153,51.4178088125408,0.348898968193457));
#44615=CARTESIAN_POINT('Ctrl Pts',(1.13624379531362,51.4203984749306,0.311369536243215));
#44616=CARTESIAN_POINT('Ctrl Pts',(1.14383042014825,51.422332089449,0.282229075538648));
#44617=CARTESIAN_POINT('Ctrl Pts',(1.16451806006148,51.4284263090572,0.188106208900379));
#44618=CARTESIAN_POINT('Ctrl Pts',(1.17325643263249,51.4324659609223,0.12229687924145));
#44619=CARTESIAN_POINT('Ctrl Pts',(1.17915037553542,51.4401439341728,-0.00130084894931952));
#44620=CARTESIAN_POINT('Ctrl Pts',(1.1776827453898,51.443753398478,-0.0588175708633005));
#44621=CARTESIAN_POINT('Ctrl Pts',(1.17043043245947,51.4485457682019,-0.132096630816075));
#44622=CARTESIAN_POINT('Ctrl Pts',(1.16850507651486,51.449608273164,-0.148164643254995));
#44623=CARTESIAN_POINT('Ctrl Pts',(1.16477129821978,51.451384082156,-0.174686288475214));
#44624=CARTESIAN_POINT('Ctrl Pts',(1.16315155881476,51.4520914034204,-0.185164562659755));
#44625=CARTESIAN_POINT('Ctrl Pts',(1.15967484926206,51.4534967901287,-0.205805771127432));
#44626=CARTESIAN_POINT('Ctrl Pts',(1.15782518557047,51.4541945645206,-0.215968977508947));
#44627=CARTESIAN_POINT('Ctrl Pts',(1.15301025289662,51.4558991858753,-0.240582634548673));
#44628=CARTESIAN_POINT('Ctrl Pts',(1.14990678490847,51.456910344481,-0.255003918966528));
#44629=CARTESIAN_POINT('Ctrl Pts',(1.13682137261875,51.4608657882517,-0.310701572335646));
#44630=CARTESIAN_POINT('Ctrl Pts',(1.12488185392698,51.4638709623346,-0.351480245584576));
#44631=CARTESIAN_POINT('Ctrl Pts',(1.08111048217538,51.4733563049897,-0.475662099123581));
#44632=CARTESIAN_POINT('Ctrl Pts',(1.0419918374638,51.4800115924331,-0.556152383576708));
#44633=CARTESIAN_POINT('Ctrl Pts',(0.980357125459869,51.4883098255161,-0.653190793392505));
#44634=CARTESIAN_POINT('Ctrl Pts',(0.965838846964708,51.4901464650663,-0.674473012972362));
#44635=CARTESIAN_POINT('Ctrl Pts',(0.945377246506615,51.4925669777587,-0.702450137281952));
#44636=CARTESIAN_POINT('Ctrl Pts',(0.940039738079159,51.4931841249534,-0.709577082925663));
#44637=CARTESIAN_POINT('Ctrl Pts',(0.931401305635918,51.4941596674658,-0.720843034940442));
#44638=CARTESIAN_POINT('Ctrl Pts',(0.928152530112668,51.494521472602,-0.725021349416883));
#44639=CARTESIAN_POINT('Ctrl Pts',(0.921125536867816,51.4952929883284,-0.733934258207485));
#44640=CARTESIAN_POINT('Ctrl Pts',(0.917338720852213,51.4957020655959,-0.738661915521769));
#44641=CARTESIAN_POINT('Ctrl Pts',(0.907331277077833,51.4967664282709,-0.750960063750599));
#44642=CARTESIAN_POINT('Ctrl Pts',(0.901052212367415,51.4974177092726,-0.75848268931107));
#44643=CARTESIAN_POINT('Ctrl Pts',(0.869101728046392,51.5006551247009,-0.795804097540143));
#44644=CARTESIAN_POINT('Ctrl Pts',(0.842040284767702,51.5031550654204,-0.824385099925427));
#44645=CARTESIAN_POINT('Ctrl Pts',(0.778713982090678,51.508638232213,-0.884888182816776));
#44646=CARTESIAN_POINT('Ctrl Pts',(0.741815777710828,51.511598435189,-0.916041581488608));
#44647=CARTESIAN_POINT('Ctrl Pts',(0.65149993152245,51.518565560712,-0.983250473717295));
#44648=CARTESIAN_POINT('Ctrl Pts',(0.596836259757017,51.5225846863174,-1.01735868992179));
#44649=CARTESIAN_POINT('Ctrl Pts',(0.525065267729918,51.5278368025096,-1.05435826021732));
#44650=CARTESIAN_POINT('Ctrl Pts',(0.510309934395917,51.5289148440322,-1.06157835488417));
#44651=CARTESIAN_POINT('Ctrl Pts',(0.485746073276829,51.5307094963588,-1.07296750179758));
#44652=CARTESIAN_POINT('Ctrl Pts',(0.476023085479921,51.5314198522669,-1.0773163495677));
#44653=CARTESIAN_POINT('Ctrl Pts',(0.456787141156655,51.5328259077799,-1.08560885861115));
#44654=CARTESIAN_POINT('Ctrl Pts',(0.447278786255941,51.5335212479292,-1.08956081145188));
#44655=CARTESIAN_POINT('Ctrl Pts',(0.424199350082499,51.5352104241697,-1.09880029256941));
#44656=CARTESIAN_POINT('Ctrl Pts',(0.410579927974366,51.5362083843319,-1.10396162113239));
#44657=CARTESIAN_POINT('Ctrl Pts',(0.358535261909155,51.5400280796431,-1.12258862523402));
#44658=CARTESIAN_POINT('Ctrl Pts',(0.319520388980909,51.5429053432363,-1.13430983810323));
#44659=CARTESIAN_POINT('Ctrl Pts',(0.202378051358836,51.5515784693802,-1.16297940102476));
#44660=CARTESIAN_POINT('Ctrl Pts',(0.123046724142034,51.5575105349847,-1.17402541992342));
#44661=CARTESIAN_POINT('Ctrl Pts',(0.00778553855762457,51.5659110916455,
-1.17825788493766));
#44662=CARTESIAN_POINT('Ctrl Pts',(-0.0276918000622706,51.5684638894598,
-1.17795836367394));
#44663=CARTESIAN_POINT('Ctrl Pts',(-0.0728625043434388,51.5716320644978,
-1.17553460520429));
#44664=CARTESIAN_POINT('Ctrl Pts',(-0.0826138847234062,51.5723110723936,
-1.1748895754239));
#44665=CARTESIAN_POINT('Ctrl Pts',(-0.0983893040399858,51.5734003671119,
-1.17364868135226));
#44666=CARTESIAN_POINT('Ctrl Pts',(-0.104418532923595,51.5738145100978,
-1.17312763864856));
#44667=CARTESIAN_POINT('Ctrl Pts',(-0.116433102210884,51.5746350842565,
-1.17199598422113));
#44668=CARTESIAN_POINT('Ctrl Pts',(-0.122418303422446,51.5750415292047,
-1.17138593859082));
#44669=CARTESIAN_POINT('Ctrl Pts',(-0.137947007450418,51.5760906075994,
-1.16968284246732));
#44670=CARTESIAN_POINT('Ctrl Pts',(-0.147482506597035,51.5767294468237,
-1.16851882908204));
#44671=CARTESIAN_POINT('Ctrl Pts',(-0.193034680027101,51.5797602145142,
-1.16239168969202));
#44672=CARTESIAN_POINT('Ctrl Pts',(-0.22882635345683,51.5820787354112,-1.15587882887217));
#44673=CARTESIAN_POINT('Ctrl Pts',(-0.368084827267104,51.5910508119624,
-1.12381453878418));
#44674=CARTESIAN_POINT('Ctrl Pts',(-0.468179281988897,51.5974399658047,
-1.0859348471274));
#44675=CARTESIAN_POINT('Ctrl Pts',(-0.578917713397505,51.6055517601538,
-1.02583033448127));
#44676=CARTESIAN_POINT('Ctrl Pts',(-0.595783840754068,51.6068169062925,
-1.01612752182739));
#44677=CARTESIAN_POINT('Ctrl Pts',(-0.622939262400979,51.6089082562277,
-0.999596889057083));
#44678=CARTESIAN_POINT('Ctrl Pts',(-0.633375541021732,51.6097255652479,
-0.993016953551476));
#44679=CARTESIAN_POINT('Ctrl Pts',(-0.652088417036367,51.6112170046168,
-0.980803726309379));
#44680=CARTESIAN_POINT('Ctrl Pts',(-0.660400308096165,51.6118889997723,
-0.975226473986516));
#44681=CARTESIAN_POINT('Ctrl Pts',(-0.678277662071779,51.6133557549078,
-0.962897471208792));
#44682=CARTESIAN_POINT('Ctrl Pts',(-0.68781547785157,51.6141519155345,-0.956107723012773));
#44683=CARTESIAN_POINT('Ctrl Pts',(-0.71473260948134,51.6164389597027,-0.936334832596564));
#44684=CARTESIAN_POINT('Ctrl Pts',(-0.731855797574318,51.6179427980301,
-0.923012786952734));
#44685=CARTESIAN_POINT('Ctrl Pts',(-0.792300115840083,51.6234347148537,
-0.873246689953653));
#44686=CARTESIAN_POINT('Ctrl Pts',(-0.833343471649848,51.627522479204,-0.834168095435839));
#44687=CARTESIAN_POINT('Ctrl Pts',(-0.919007786596022,51.636842769047,-0.73994933985058));
#44688=CARTESIAN_POINT('Ctrl Pts',(-0.961788964807032,51.6420905156268,
-0.683420062062222));
#44689=CARTESIAN_POINT('Ctrl Pts',(-1.00917447221783,51.6484918496028,-0.607465471933665));
#44690=CARTESIAN_POINT('Ctrl Pts',(-1.01872864366801,51.649819238263,-0.591303187670937));
#44691=CARTESIAN_POINT('Ctrl Pts',(-1.03140932686091,51.6516269598634,-0.56863147377479));
#44692=CARTESIAN_POINT('Ctrl Pts',(-1.03486805929307,51.6521251204273,-0.562312243270667));
#44693=CARTESIAN_POINT('Ctrl Pts',(-1.04098717468099,51.6530152438195,-0.550884678177245));
#44694=CARTESIAN_POINT('Ctrl Pts',(-1.04366847687343,51.6534084488008,-0.545787818424753));
#44695=CARTESIAN_POINT('Ctrl Pts',(-1.04921575990447,51.654228407645,-0.5350526604289));
#44696=CARTESIAN_POINT('Ctrl Pts',(-1.05207388197608,51.6546546920453,-0.52941062684451));
#44697=CARTESIAN_POINT('Ctrl Pts',(-1.05980128202895,51.6558186354366,-0.513846718024227));
#44698=CARTESIAN_POINT('Ctrl Pts',(-1.06457670599092,51.6565508269861,-0.503878622269322));
#44699=CARTESIAN_POINT('Ctrl Pts',(-1.094184166711,51.6611845478249,-0.439776172494579));
#44700=CARTESIAN_POINT('Ctrl Pts',(-1.11502314715813,51.6648894378283,-0.383884423776815));
#44701=CARTESIAN_POINT('Ctrl Pts',(-1.1557425500198,51.6739706031755,-0.242828535582492));
#44702=CARTESIAN_POINT('Ctrl Pts',(-1.17054904363917,51.6793129584535,-0.156587701061906));
#44703=CARTESIAN_POINT('Ctrl Pts',(-1.17652583295087,51.6858798452696,-0.0554901756800495));
#44704=CARTESIAN_POINT('Ctrl Pts',(-1.17710371235242,51.6867971695693,-0.0414610539006681));
#44705=CARTESIAN_POINT('Ctrl Pts',(-1.17764313659771,51.6883232936628,-0.0183024361316305));
#44706=CARTESIAN_POINT('Ctrl Pts',(-1.1777495911096,51.6889276389105,-0.0091775618924337));
#44707=CARTESIAN_POINT('Ctrl Pts',(-1.17774999882436,51.6895352714817,-5.26234844835546E-5));
#44708=CARTESIAN_POINT('Ctrl Pts',(0.188969603130438,51.8285263152314,1.16268601701703));
#44709=CARTESIAN_POINT('Ctrl Pts',(0.105006823041406,51.8227652863916,1.17720726394182));
#44710=CARTESIAN_POINT('Ctrl Pts',(-0.372052432586408,51.7905460268137,
1.20724379575199));
#44711=CARTESIAN_POINT('Ctrl Pts',(-1.02786962445986,51.7445815501578,0.80164220951439));
#44712=CARTESIAN_POINT('Ctrl Pts',(-1.1756492492359,51.7043781023418,0.204084402645715));
#44713=CARTESIAN_POINT('Ctrl Pts',(-1.17584353021606,51.6906328852638,-0.000125521981853664));
#44714=CARTESIAN_POINT('Ctrl Pts',(0.188938462126305,51.9282531127635,1.16249615914606));
#44715=CARTESIAN_POINT('Ctrl Pts',(0.183462612124699,51.9278870166283,1.16338613944406));
#44716=CARTESIAN_POINT('Ctrl Pts',(0.17798050184252,51.9275197376481,1.16423742484463));
#44717=CARTESIAN_POINT('Ctrl Pts',(0.162250033160122,51.9264635056015,1.16656641379994));
#44718=CARTESIAN_POINT('Ctrl Pts',(0.151988266015469,51.9257716097238,1.16794769847221));
#44719=CARTESIAN_POINT('Ctrl Pts',(0.131223367283335,51.9243651229521,1.17046446894594));
#44720=CARTESIAN_POINT('Ctrl Pts',(0.120720525653028,51.9236504215511,1.17159429290802));
#44721=CARTESIAN_POINT('Ctrl Pts',(0.0942810529495212,51.9218423112242,
1.1740791846088));
#44722=CARTESIAN_POINT('Ctrl Pts',(0.0783298015161907,51.9207432881422,
1.17525114200211));
#44723=CARTESIAN_POINT('Ctrl Pts',(0.00946654721373525,51.9159611631068,
1.17890248171694));
#44724=CARTESIAN_POINT('Ctrl Pts',(-0.0435488067908089,51.9121803216698,
1.17813530308287));
#44725=CARTESIAN_POINT('Ctrl Pts',(-0.166315877857828,51.9032265274241,
1.16806062033052));
#44726=CARTESIAN_POINT('Ctrl Pts',(-0.235648561579883,51.8980148348431,
1.15606916970954));
#44727=CARTESIAN_POINT('Ctrl Pts',(-0.333346518993407,51.8906804285494,
1.13001301620693));
#44728=CARTESIAN_POINT('Ctrl Pts',(-0.362872370326534,51.8884670225882,
1.12088059606519));
#44729=CARTESIAN_POINT('Ctrl Pts',(-0.40065656146647,51.885666242194,1.10754390916431));
#44730=CARTESIAN_POINT('Ctrl Pts',(-0.409270125513075,51.8850299622536,
1.10438995313784));
#44731=CARTESIAN_POINT('Ctrl Pts',(-0.423385896769344,51.8839918834375,
1.09903346215587));
#44732=CARTESIAN_POINT('Ctrl Pts',(-0.428909762859666,51.8835868415959,
1.09688950641639));
#44733=CARTESIAN_POINT('Ctrl Pts',(-0.440139428377085,51.8827661709178,
1.09243317568849));
#44734=CARTESIAN_POINT('Ctrl Pts',(-0.445843696046905,51.8823507357693,
1.09011759127742));
#44735=CARTESIAN_POINT('Ctrl Pts',(-0.461011226969873,51.8812492676327,
1.08382152625517));
#44736=CARTESIAN_POINT('Ctrl Pts',(-0.470441283409505,51.8805677655078,
1.07976176487336));
#44737=CARTESIAN_POINT('Ctrl Pts',(-0.521620420814071,51.876880835444,1.05693067405765));
#44738=CARTESIAN_POINT('Ctrl Pts',(-0.562305680730351,51.8739921567228,
1.03585886770141));
#44739=CARTESIAN_POINT('Ctrl Pts',(-0.662850879550758,51.8667085882616,
0.976109397727067));
#44740=CARTESIAN_POINT('Ctrl Pts',(-0.720613813347096,51.8623748738761,
0.934278645186085));
#44741=CARTESIAN_POINT('Ctrl Pts',(-0.794027332826886,51.8562439551879,
0.870232556631485));
#44742=CARTESIAN_POINT('Ctrl Pts',(-0.813224159390333,51.8545753195536,
0.852320620385603));
#44743=CARTESIAN_POINT('Ctrl Pts',(-0.846381450553554,51.8515546387805,
0.819241967689644));
#44744=CARTESIAN_POINT('Ctrl Pts',(-0.860572636633313,51.8502124877072,
0.804321836139874));
#44745=CARTESIAN_POINT('Ctrl Pts',(-0.882062040004818,51.8480954694883,
0.780508565272471));
#44746=CARTESIAN_POINT('Ctrl Pts',(-0.889633772913021,51.8473321575135,
0.771867085235054));
#44747=CARTESIAN_POINT('Ctrl Pts',(-0.903573510775216,51.8458928802471,
0.755480297802631));
#44748=CARTESIAN_POINT('Ctrl Pts',(-0.909971419759694,51.8452182337526,
0.747761709495764));
#44749=CARTESIAN_POINT('Ctrl Pts',(-0.924200677327786,51.8436849647098,
0.730142116491861));
#44750=CARTESIAN_POINT('Ctrl Pts',(-0.931972831109019,51.8428240742604,
0.720195128117739));
#44751=CARTESIAN_POINT('Ctrl Pts',(-0.955698205260662,51.8401205614458,
0.68880353968434));
#44752=CARTESIAN_POINT('Ctrl Pts',(-0.971081380142646,51.8382564653814,
0.666940873993194));
#44753=CARTESIAN_POINT('Ctrl Pts',(-1.03571043092111,51.8299063779116,0.568107926069416));
#44754=CARTESIAN_POINT('Ctrl Pts',(-1.07664094282409,51.8231425871902,0.486088939257362));
#44755=CARTESIAN_POINT('Ctrl Pts',(-1.1175044777919,51.8143471076261,0.37298161413268));
#44756=CARTESIAN_POINT('Ctrl Pts',(-1.12632705418038,51.8122462181066,0.345425980429661));
#44757=CARTESIAN_POINT('Ctrl Pts',(-1.13914544761635,51.8088503706586,0.29964838659876));
#44758=CARTESIAN_POINT('Ctrl Pts',(-1.14373906035697,51.8075356226127,0.281607104561715));
#44759=CARTESIAN_POINT('Ctrl Pts',(-1.14962833587913,51.8057057362517,0.255947675947434));
#44760=CARTESIAN_POINT('Ctrl Pts',(-1.15127951918364,51.8051733804073,0.248414976116174));
#44761=CARTESIAN_POINT('Ctrl Pts',(-1.15400967826238,51.8042588570661,0.235347637755888));
#44762=CARTESIAN_POINT('Ctrl Pts',(-1.15512307649148,51.8038748424923,0.229820650276862));
#44763=CARTESIAN_POINT('Ctrl Pts',(-1.15748442910733,51.8030353196771,0.217647825057052));
#44764=CARTESIAN_POINT('Ctrl Pts',(-1.15871490075926,51.8025807729735,0.210998966248973));
#44765=CARTESIAN_POINT('Ctrl Pts',(-1.16210906460721,51.8012742409649,0.191732760728299));
#44766=CARTESIAN_POINT('Ctrl Pts',(-1.1641244742733,51.8004299677878,0.179089839836327));
#44767=CARTESIAN_POINT('Ctrl Pts',(-1.17375072987791,51.795983665926,0.111646945734306));
#44768=CARTESIAN_POINT('Ctrl Pts',(-1.17770009804705,51.7925397376763,0.0563886714383546));
#44769=CARTESIAN_POINT('Ctrl Pts',(-1.17782728655719,51.7837305019052,-0.085992224174415));
#44770=CARTESIAN_POINT('Ctrl Pts',(-1.16825572491506,51.7784043491381,-0.1727676935835));
#44771=CARTESIAN_POINT('Ctrl Pts',(-1.14517246557387,51.7715723035668,-0.275709991094904));
#44772=CARTESIAN_POINT('Ctrl Pts',(-1.14070963547905,51.7703647650872,-0.293628067370979));
#44773=CARTESIAN_POINT('Ctrl Pts',(-1.13290261332065,51.7684123258271,-0.322101060345485));
#44774=CARTESIAN_POINT('Ctrl Pts',(-1.12982749286203,51.7676761163491,-0.332726985111607));
#44775=CARTESIAN_POINT('Ctrl Pts',(-1.12365651968738,51.7662577041675,-0.352977733859893));
#44776=CARTESIAN_POINT('Ctrl Pts',(-1.12058549830709,51.7655763690396,-0.362609134945579));
#44777=CARTESIAN_POINT('Ctrl Pts',(-1.11316011443999,51.7639831317681,-0.384901092743328));
#44778=CARTESIAN_POINT('Ctrl Pts',(-1.10871316944721,51.7630682451989,-0.3975290851225));
#44779=CARTESIAN_POINT('Ctrl Pts',(-1.09306830405138,51.7599736353379,-0.439649712538828));
#44780=CARTESIAN_POINT('Ctrl Pts',(-1.08090184709768,51.7577624482988,-0.468765465494556));
#44781=CARTESIAN_POINT('Ctrl Pts',(-1.04690129990442,51.7520316309258,-0.541748231518111));
#44782=CARTESIAN_POINT('Ctrl Pts',(-1.02347318337572,51.7484680593363,-0.584803647398971));
#44783=CARTESIAN_POINT('Ctrl Pts',(-0.957882792449539,51.7394194147271,
-0.689266508583233));
#44784=CARTESIAN_POINT('Ctrl Pts',(-0.912448615953605,51.733910250578,-0.748376147206907));
#44785=CARTESIAN_POINT('Ctrl Pts',(-0.853654142501249,51.7278311656367,
-0.811486507626759));
#44786=CARTESIAN_POINT('Ctrl Pts',(-0.845438074450274,51.7270025886761,
-0.820042825921475));
#44787=CARTESIAN_POINT('Ctrl Pts',(-0.832478070147195,51.7257295984871,
-0.833137671720877));
#44788=CARTESIAN_POINT('Ctrl Pts',(-0.827823345229624,51.7252789876061,
-0.837762873152522));
#44789=CARTESIAN_POINT('Ctrl Pts',(-0.819028307480639,51.724440249119,-0.846357243693378));
#44790=CARTESIAN_POINT('Ctrl Pts',(-0.814897490186356,51.7240514926395,
-0.850335248209219));
#44791=CARTESIAN_POINT('Ctrl Pts',(-0.804866175146836,51.7231194887353,
-0.859855233922112));
#44792=CARTESIAN_POINT('Ctrl Pts',(-0.798937329851195,51.7225784962274,
-0.865366821297075));
#44793=CARTESIAN_POINT('Ctrl Pts',(-0.777248142279038,51.7206326835768,
-0.885116645071476));
#44794=CARTESIAN_POINT('Ctrl Pts',(-0.761159269944817,51.7192518850147,
-0.898989903656797));
#44795=CARTESIAN_POINT('Ctrl Pts',(-0.717299275868071,51.7156230491057,
-0.934787686266086));
#44796=CARTESIAN_POINT('Ctrl Pts',(-0.688900132699164,51.713410793343,-0.955909622099035));
#44797=CARTESIAN_POINT('Ctrl Pts',(-0.582598474065916,51.7054480087722,
-1.02776989880228));
#44798=CARTESIAN_POINT('Ctrl Pts',(-0.499722913953653,51.6997973497193,
-1.07051749683297));
#44799=CARTESIAN_POINT('Ctrl Pts',(-0.394552599406553,51.6925416584963,
-1.10986403371338));
#44800=CARTESIAN_POINT('Ctrl Pts',(-0.376255074585946,51.6912777969649,
-1.11619979246553));
#44801=CARTESIAN_POINT('Ctrl Pts',(-0.346998564878577,51.6892498088831,
-1.12552913933316));
#44802=CARTESIAN_POINT('Ctrl Pts',(-0.336137682807531,51.6884954377621,
-1.12882030923926));
#44803=CARTESIAN_POINT('Ctrl Pts',(-0.315576913408956,51.6870636050458,
-1.13472779765957));
#44804=CARTESIAN_POINT('Ctrl Pts',(-0.305887754359871,51.686387318489,-1.13737796441804));
#44805=CARTESIAN_POINT('Ctrl Pts',(-0.283736406909279,51.6848371172491,
-1.143133256206));
#44806=CARTESIAN_POINT('Ctrl Pts',(-0.271255138818756,51.683960730004,-1.14615907133421));
#44807=CARTESIAN_POINT('Ctrl Pts',(-0.231371702469412,51.6811498389345,
-1.15514002261123));
#44808=CARTESIAN_POINT('Ctrl Pts',(-0.203807017784058,51.6791913168755,
-1.16032056202564));
#44809=CARTESIAN_POINT('Ctrl Pts',(-0.135830482380693,51.6743208240502,
-1.17059927931991));
#44810=CARTESIAN_POINT('Ctrl Pts',(-0.095290299645714,51.6713806242783,
-1.17459432007002));
#44811=CARTESIAN_POINT('Ctrl Pts',(0.0325751078803395,51.6620355047494,
-1.1805315265436));
#44812=CARTESIAN_POINT('Ctrl Pts',(0.11995951507089,51.6555252719099,-1.17487304545372));
#44813=CARTESIAN_POINT('Ctrl Pts',(0.217803460915769,51.6485176827157,-1.15749834899699));
#44814=CARTESIAN_POINT('Ctrl Pts',(0.229656129652328,51.6476740536699,-1.15520511857476));
#44815=CARTESIAN_POINT('Ctrl Pts',(0.247938486595406,51.6463830553016,-1.15137536002117));
#44816=CARTESIAN_POINT('Ctrl Pts',(0.254393654611757,51.6459292229118,-1.14996634151417));
#44817=CARTESIAN_POINT('Ctrl Pts',(0.266417862057183,51.645088018983,-1.14723552068467));
#44818=CARTESIAN_POINT('Ctrl Pts',(0.271989372330439,51.644699968661,-1.14592739735966));
#44819=CARTESIAN_POINT('Ctrl Pts',(0.285334353671719,51.6437743353231,-1.14269134246325));
#44820=CARTESIAN_POINT('Ctrl Pts',(0.29309805058174,51.6432389225362,-1.14072465531099));
#44821=CARTESIAN_POINT('Ctrl Pts',(0.320778976967498,51.6413390276787,-1.13341129629457));
#44822=CARTESIAN_POINT('Ctrl Pts',(0.340576255218611,51.639997104275,-1.12762061618568));
#44823=CARTESIAN_POINT('Ctrl Pts',(0.392374374305499,51.6365059516286,-1.11098088946537));
#44824=CARTESIAN_POINT('Ctrl Pts',(0.424078938116739,51.6343892450726,-1.09926954799639));
#44825=CARTESIAN_POINT('Ctrl Pts',(0.534981711703971,51.6269177301872,-1.05278946823765));
#44826=CARTESIAN_POINT('Ctrl Pts',(0.610797641052369,51.6216631618294,-1.01069117959426));
#44827=CARTESIAN_POINT('Ctrl Pts',(0.701666518293402,51.614530729542,-0.946245868475442));
#44828=CARTESIAN_POINT('Ctrl Pts',(0.721546312291629,51.6129142313404,-0.93117556083893));
#44829=CARTESIAN_POINT('Ctrl Pts',(0.750501620864091,51.6104635545818,-0.907741126122959));
#44830=CARTESIAN_POINT('Ctrl Pts',(0.759949204460988,51.6096478816022,-0.899846554963675));
#44831=CARTESIAN_POINT('Ctrl Pts',(0.776847411884057,51.6081583233203,-0.885270170394331));
#44832=CARTESIAN_POINT('Ctrl Pts',(0.784340018322728,51.6074865511765,-0.878638663462971));
#44833=CARTESIAN_POINT('Ctrl Pts',(0.80042504274422,51.6060190012996,-0.864032532926315));
#44834=CARTESIAN_POINT('Ctrl Pts',(0.808984642098776,51.6052218063553,-0.856023538485632));
#44835=CARTESIAN_POINT('Ctrl Pts',(0.833101276107259,51.6029277711956,-0.832773435800495));
#44836=CARTESIAN_POINT('Ctrl Pts',(0.848356316405623,51.601417846077,-0.817227497283205));
#44837=CARTESIAN_POINT('Ctrl Pts',(0.903912679649658,51.5956890811113,-0.757379104189814));
#44838=CARTESIAN_POINT('Ctrl Pts',(0.941242425216576,51.5913564108608,-0.710452101871946));
#44839=CARTESIAN_POINT('Ctrl Pts',(1.01794877935151,51.5813396166399,-0.597308395673047));
#44840=CARTESIAN_POINT('Ctrl Pts',(1.05473596631605,51.5756392022864,-0.52965128678864));
#44841=CARTESIAN_POINT('Ctrl Pts',(1.08961458620735,51.5693172267289,-0.447209100276167));
#44842=CARTESIAN_POINT('Ctrl Pts',(1.09436761780922,51.568429716205,-0.435448591040879));
#44843=CARTESIAN_POINT('Ctrl Pts',(1.10135303589467,51.5670863866018,-0.417327133572524));
#44844=CARTESIAN_POINT('Ctrl Pts',(1.10372220198934,51.5666233053141,-0.411020379716992));
#44845=CARTESIAN_POINT('Ctrl Pts',(1.10779773877904,51.5658136540792,-0.399881837057961));
#44846=CARTESIAN_POINT('Ctrl Pts',(1.10952681527662,51.5654658073397,-0.395058934143007));
#44847=CARTESIAN_POINT('Ctrl Pts',(1.11368239724219,51.5646188140736,-0.383225276549293));
#44848=CARTESIAN_POINT('Ctrl Pts',(1.1160742213194,51.5641216738024,-0.376202650540096));
#44849=CARTESIAN_POINT('Ctrl Pts',(1.12366524190434,51.5625100933248,-0.353204903809116));
#44850=CARTESIAN_POINT('Ctrl Pts',(1.12858927690882,51.5614101221376,-0.337140317030607));
#44851=CARTESIAN_POINT('Ctrl Pts',(1.13995684128539,51.5587130084674,-0.297008325596261));
#44852=CARTESIAN_POINT('Ctrl Pts',(1.14598385459334,51.5571327784842,-0.272830902088554));
#44853=CARTESIAN_POINT('Ctrl Pts',(1.17139188461725,51.5495744396951,-0.155111820177261));
#44854=CARTESIAN_POINT('Ctrl Pts',(1.18011108972063,51.543823702531,-0.0596419259651858));
#44855=CARTESIAN_POINT('Ctrl Pts',(1.17634134878957,51.5359310763864,0.0641968616380028));
#44856=CARTESIAN_POINT('Ctrl Pts',(1.17445337618798,51.5340994748725,0.0925163385151291));
#44857=CARTESIAN_POINT('Ctrl Pts',(1.17022269009456,51.5313898052987,0.133567398215436));
#44858=CARTESIAN_POINT('Ctrl Pts',(1.16868995149018,51.5305367823428,0.146373391406597));
#44859=CARTESIAN_POINT('Ctrl Pts',(1.16558914833725,51.529007206507,0.169109464053154));
#44860=CARTESIAN_POINT('Ctrl Pts',(1.16410364264697,51.5283333170692,0.179049635434051));
#44861=CARTESIAN_POINT('Ctrl Pts',(1.16067551606526,51.5268920245428,0.200138597461469));
#44862=CARTESIAN_POINT('Ctrl Pts',(1.15869906833716,51.5261236103602,0.211280773301466));
#44863=CARTESIAN_POINT('Ctrl Pts',(1.15283865298841,51.5240019332518,0.241758145710643));
#44864=CARTESIAN_POINT('Ctrl Pts',(1.1486292690451,51.5226385236471,0.261026207841442));
#44865=CARTESIAN_POINT('Ctrl Pts',(1.13804664754031,51.5195294032643,0.304233895214888));
#44866=CARTESIAN_POINT('Ctrl Pts',(1.131397983325,51.5177758801429,0.32809585595942));
#44867=CARTESIAN_POINT('Ctrl Pts',(1.10523289699926,51.5115038488961,0.411710262156313));
#44868=CARTESIAN_POINT('Ctrl Pts',(1.08169359692449,51.5068836273392,0.470088012251854));
#44869=CARTESIAN_POINT('Ctrl Pts',(1.03021264018664,51.4984211413603,0.573148305380368));
#44870=CARTESIAN_POINT('Ctrl Pts',(1.00371227751021,51.4945888481177,0.618384760168006));
#44871=CARTESIAN_POINT('Ctrl Pts',(0.967079967850452,51.4899825960001,0.672321295255519));
#44872=CARTESIAN_POINT('Ctrl Pts',(0.959700108053729,51.4890847839051,0.682814267865826));
#44873=CARTESIAN_POINT('Ctrl Pts',(0.948167212845705,51.4877292062156,0.698655700986576));
#44874=CARTESIAN_POINT('Ctrl Pts',(0.944137299855534,51.4872639853379,0.704092051328692));
#44875=CARTESIAN_POINT('Ctrl Pts',(0.936664693908591,51.4864171068407,0.713993061478256));
#44876=CARTESIAN_POINT('Ctrl Pts',(0.933236619348428,51.4860345522981,0.718467991562704));
#44877=CARTESIAN_POINT('Ctrl Pts',(0.92504817000169,51.4851344890235,0.728999506546271));
#44878=CARTESIAN_POINT('Ctrl Pts',(0.920260315408643,51.4846188908422,0.735034255868959));
#44879=CARTESIAN_POINT('Ctrl Pts',(0.903735624037448,51.4828736218386,0.755447858438214));
#44880=CARTESIAN_POINT('Ctrl Pts',(0.891717651800982,51.4816619385389,0.769596820065839));
#44881=CARTESIAN_POINT('Ctrl Pts',(0.860211078138958,51.478610606278,0.804960509550186));
#44882=CARTESIAN_POINT('Ctrl Pts',(0.840269095950351,51.4767941649389,0.825755761557385));
#44883=CARTESIAN_POINT('Ctrl Pts',(0.754604125610371,51.4693460483427,0.908765443530676));
#44884=CARTESIAN_POINT('Ctrl Pts',(0.682588246703392,51.4638745660641,0.964030756287453));
#44885=CARTESIAN_POINT('Ctrl Pts',(0.581408599316212,51.4563524772678,1.02460345972236));
#44886=CARTESIAN_POINT('Ctrl Pts',(0.55737820462134,51.4545791247731,1.03787165066499));
#44887=CARTESIAN_POINT('Ctrl Pts',(0.52154317498901,51.4519393480716,1.05605406232302));
#44888=CARTESIAN_POINT('Ctrl Pts',(0.510086156307196,51.4510961011832,1.06163532248707));
#44889=CARTESIAN_POINT('Ctrl Pts',(0.489449043406567,51.449577221007,1.07127746621177));
#44890=CARTESIAN_POINT('Ctrl Pts',(0.480303222166705,51.4489041071393,1.0754090290398));
#44891=CARTESIAN_POINT('Ctrl Pts',(0.460648970576079,51.4474570419454,1.083986976827));
#44892=CARTESIAN_POINT('Ctrl Pts',(0.450126551769554,51.446681983352,1.08839850760892));
#44893=CARTESIAN_POINT('Ctrl Pts',(0.420812261144959,51.4445210165315,1.10019074457432));
#44894=CARTESIAN_POINT('Ctrl Pts',(0.401892955986705,51.4431243212654,1.1072418876155));
#44895=CARTESIAN_POINT('Ctrl Pts',(0.358629277967955,51.439924123658,1.12211117413984));
#44896=CARTESIAN_POINT('Ctrl Pts',(0.334193327887872,51.4381120951896,1.12962963170276));
#44897=CARTESIAN_POINT('Ctrl Pts',(0.269803577984737,51.433328066067,1.14716898750013));
#44898=CARTESIAN_POINT('Ctrl Pts',(0.229549396662269,51.4303272326354,1.15589573824819));
#44899=CARTESIAN_POINT('Ctrl Pts',(0.18893837638019,51.427308721746,1.16249617308222));
#44900=CARTESIAN_POINT('Origin',(0.,56.5393671147362,0.));
#44901=CARTESIAN_POINT('',(0.188938575466302,50.827546579051,1.16249614072511));
#44902=CARTESIAN_POINT('',(0.18893846240316,50.927164359664,1.16249615910107));
#44903=CARTESIAN_POINT('',(0.188938462403162,56.5393671147362,1.16249615910107));
#44904=CARTESIAN_POINT('Ctrl Pts',(0.188938575466302,50.827546579051,1.16249614072511));
#44905=CARTESIAN_POINT('Ctrl Pts',(0.259627942104656,50.8326143480709,1.15100711485622));
#44906=CARTESIAN_POINT('Ctrl Pts',(0.32914111607513,50.837863869476,1.13309119767087));
#44907=CARTESIAN_POINT('Ctrl Pts',(0.452718762653112,50.8475082684021,1.08889462587203));
#44908=CARTESIAN_POINT('Ctrl Pts',(0.507228187990633,50.8518793517914,1.0645969831142));
#44909=CARTESIAN_POINT('Ctrl Pts',(0.569393707715353,50.856846433725,1.03102281040476));
#44910=CARTESIAN_POINT('Ctrl Pts',(0.579044964963574,50.8576168822874,1.02563355093232));
#44911=CARTESIAN_POINT('Ctrl Pts',(0.594097261400788,50.8588157330355,1.01694813287376));
#44912=CARTESIAN_POINT('Ctrl Pts',(0.599549787651772,50.8592494239745,1.01374312220045));
#44913=CARTESIAN_POINT('Ctrl Pts',(0.609916913798747,50.8600725205075,1.00753639064356));
#44914=CARTESIAN_POINT('Ctrl Pts',(0.614835696914428,50.8604623522168,1.00454232736016));
#44915=CARTESIAN_POINT('Ctrl Pts',(0.62585658071665,50.8613346410909,0.99772264156154));
#44916=CARTESIAN_POINT('Ctrl Pts',(0.631946051661149,50.8618158193953,0.993876814996615));
#44917=CARTESIAN_POINT('Ctrl Pts',(0.653766830888981,50.8635386381763,0.979814182397296));
#44918=CARTESIAN_POINT('Ctrl Pts',(0.66928966843692,50.8647615419271,0.969277222256888));
#44919=CARTESIAN_POINT('Ctrl Pts',(0.742130557723507,50.8705210693014,0.917247801076728));
#44920=CARTESIAN_POINT('Ctrl Pts',(0.795888293366376,50.8748422967611,0.871013788436937));
#44921=CARTESIAN_POINT('Ctrl Pts',(0.876079641583324,50.8819643785318,0.788383684409174));
#44922=CARTESIAN_POINT('Ctrl Pts',(0.90515919190761,50.8847238538695,0.754818401878749));
#44923=CARTESIAN_POINT('Ctrl Pts',(0.95039813429856,50.8894316965573,0.696217001721589));
#44924=CARTESIAN_POINT('Ctrl Pts',(0.967627507292236,50.8913434449042,0.672065107411906));
#44925=CARTESIAN_POINT('Ctrl Pts',(0.991127301414742,50.8941490834824,0.636343788099257));
#44926=CARTESIAN_POINT('Ctrl Pts',(0.998145128453671,50.8950152376651,0.625278357165891));
#44927=CARTESIAN_POINT('Ctrl Pts',(1.01022974858605,50.8965594807933,0.605501788651564));
#44928=CARTESIAN_POINT('Ctrl Pts',(1.01537216888101,50.8972347132135,0.596838260167771));
#44929=CARTESIAN_POINT('Ctrl Pts',(1.02599781341864,50.8986695741594,0.578402193477325));
#44930=CARTESIAN_POINT('Ctrl Pts',(1.03145394912399,50.8994300952994,0.568615288398058));
#44931=CARTESIAN_POINT('Ctrl Pts',(1.04586092233997,50.9015050008596,0.541883032636944));
#44932=CARTESIAN_POINT('Ctrl Pts',(1.05453881475556,50.902828790241,0.524795296084028));
#44933=CARTESIAN_POINT('Ctrl Pts',(1.1046338387831,50.9109452721693,0.419888267125618));
#44934=CARTESIAN_POINT('Ctrl Pts',(1.1354705666607,50.9180975454135,0.327447643440453));
#44935=CARTESIAN_POINT('Ctrl Pts',(1.16115521099394,50.9276458069994,0.199783591125745));
#44936=CARTESIAN_POINT('Ctrl Pts',(1.16632057583926,50.9300645488661,0.1670074158695));
#44937=CARTESIAN_POINT('Ctrl Pts',(1.17241532842624,50.9339002675268,0.113809600453559));
#44938=CARTESIAN_POINT('Ctrl Pts',(1.17420915078907,50.9353431706389,0.0935057026633607));
#44939=CARTESIAN_POINT('Ctrl Pts',(1.17597065304988,50.9373163060155,0.0652049068412056));
#44940=CARTESIAN_POINT('Ctrl Pts',(1.17638521719627,50.9378673907132,0.0572406013884337));
#44941=CARTESIAN_POINT('Ctrl Pts',(1.17695814868201,50.9388062778386,0.0435579114685473));
#44942=CARTESIAN_POINT('Ctrl Pts',(1.17715580704249,50.9391961428226,0.0378416039196781));
#44943=CARTESIAN_POINT('Ctrl Pts',(1.17749261392439,50.9400327092992,0.0254978676405069));
#44944=CARTESIAN_POINT('Ctrl Pts',(1.17761747192257,50.9404786405492,0.0188704066778337));
#44945=CARTESIAN_POINT('Ctrl Pts',(1.17781283300023,50.9417349319346,7.66448210947528E-5));
#44946=CARTESIAN_POINT('Ctrl Pts',(1.17775078941898,50.942538460152,-0.0120905723682189));
#44947=CARTESIAN_POINT('Ctrl Pts',(1.17606276703339,50.9478974164786,-0.0940377489813075));
#44948=CARTESIAN_POINT('Ctrl Pts',(1.16842464807765,50.9521912191395,-0.163563645674606));
#44949=CARTESIAN_POINT('Ctrl Pts',(1.14450302802036,50.9596909249419,-0.282616780253624));
#44950=CARTESIAN_POINT('Ctrl Pts',(1.13101918996311,50.9628796035003,-0.332497474951011));
#44951=CARTESIAN_POINT('Ctrl Pts',(1.10707150503448,50.9675658029512,-0.402476418010754));
#44952=CARTESIAN_POINT('Ctrl Pts',(1.09923495366496,50.9689956724105,-0.423411160555576));
#44953=CARTESIAN_POINT('Ctrl Pts',(1.08392122243635,50.9716267128675,-0.461024279203603));
#44954=CARTESIAN_POINT('Ctrl Pts',(1.07664234484914,50.9728215155987,-0.477775894025711));
#44955=CARTESIAN_POINT('Ctrl Pts',(1.06435032769334,50.9747585415348,-0.504355979945449));
#44956=CARTESIAN_POINT('Ctrl Pts',(1.05958330952193,50.9754923288003,-0.514295411989171));
#44957=CARTESIAN_POINT('Ctrl Pts',(1.05017128423351,50.9769094867815,-0.533233398757788));
#44958=CARTESIAN_POINT('Ctrl Pts',(1.04554834160172,50.9775920368745,-0.542241863030465));
#44959=CARTESIAN_POINT('Ctrl Pts',(1.03460739559543,50.9791775539514,-0.562901632950017));
#44960=CARTESIAN_POINT('Ctrl Pts',(1.02820782095753,50.9800833504959,-0.574507931313546));
#44961=CARTESIAN_POINT('Ctrl Pts',(1.00708304617504,50.9830075197304,-0.611335988201504));
#44962=CARTESIAN_POINT('Ctrl Pts',(0.99161610508143,50.9850519746332,-0.636117281242357));
#44963=CARTESIAN_POINT('Ctrl Pts',(0.926139175970483,50.9933468432241,-0.732825468286185));
#44964=CARTESIAN_POINT('Ctrl Pts',(0.869099090636311,50.9998344007438,-0.799643706673251));
#44965=CARTESIAN_POINT('Ctrl Pts',(0.784475563347867,51.0083114337444,-0.87891922143992));
#44966=CARTESIAN_POINT('Ctrl Pts',(0.763062496210773,51.0103723366655,-0.897572685369569));
#44967=CARTESIAN_POINT('Ctrl Pts',(0.726708103191955,51.013712103079,-0.926999595952955));
#44968=CARTESIAN_POINT('Ctrl Pts',(0.712151388596709,51.0150100208736,-0.938228867528149));
#44969=CARTESIAN_POINT('Ctrl Pts',(0.691150571368268,51.0168210719332,-0.953658680536643));
#44970=CARTESIAN_POINT('Ctrl Pts',(0.684919799690257,51.0173509653471,-0.958143448199318));
#44971=CARTESIAN_POINT('Ctrl Pts',(0.673997653827916,51.018266365179,-0.965843964875581));
#44972=CARTESIAN_POINT('Ctrl Pts',(0.669326176891426,51.0186536420821,-0.969087135296385));
#44973=CARTESIAN_POINT('Ctrl Pts',(0.659006794931623,51.0194997633285,-0.976141137366368));
#44974=CARTESIAN_POINT('Ctrl Pts',(0.653349087719074,51.0199576375446,-0.97993696284044));
#44975=CARTESIAN_POINT('Ctrl Pts',(0.636423676373294,51.0213106196566,-0.991080676156905));
#44976=CARTESIAN_POINT('Ctrl Pts',(0.625062275531782,51.0221969647458,-0.998285125558602));
#44977=CARTESIAN_POINT('Ctrl Pts',(0.548574125885574,51.0280376486168,-1.04496954137573));
#44978=CARTESIAN_POINT('Ctrl Pts',(0.479865521743824,51.032690768697,-1.07825178185986));
#44979=CARTESIAN_POINT('Ctrl Pts',(0.364989823088811,51.040261270085,-1.12072349738529));
#44980=CARTESIAN_POINT('Ctrl Pts',(0.320656273835647,51.0431350511907,-1.13420362893105));
#44981=CARTESIAN_POINT('Ctrl Pts',(0.24602512001743,51.0480114631145,-1.15216969030049));
#44982=CARTESIAN_POINT('Ctrl Pts',(0.21614008615792,51.0499736311142,-1.15814790741264));
#44983=CARTESIAN_POINT('Ctrl Pts',(0.172996545306663,51.0528394671767,-1.16505031886907));
#44984=CARTESIAN_POINT('Ctrl Pts',(0.159900546748441,51.0537136395047,-1.16691980951486));
#44985=CARTESIAN_POINT('Ctrl Pts',(0.136764199236654,51.0552669344928,-1.16982581574905));
#44986=CARTESIAN_POINT('Ctrl Pts',(0.126736663711469,51.055943082723,-1.17095460738734));
#44987=CARTESIAN_POINT('Ctrl Pts',(0.10560838297638,51.0573745012184,-1.17305843369908));
#44988=CARTESIAN_POINT('Ctrl Pts',(0.0945058797306597,51.0581305959129,
-1.17400504393459));
#44989=CARTESIAN_POINT('Ctrl Pts',(0.0645870968504152,51.0601793831649,
-1.17612880819369));
#44990=CARTESIAN_POINT('Ctrl Pts',(0.0457539253395615,51.06148107527,-1.17701188315866));
#44991=CARTESIAN_POINT('Ctrl Pts',(-0.0563745238890062,51.0686088410396,
-1.17934586725071));
#44992=CARTESIAN_POINT('Ctrl Pts',(-0.139611160143111,51.0746908021634,
-1.17240733556285));
#44993=CARTESIAN_POINT('Ctrl Pts',(-0.282147149173311,51.0853557581067,
-1.1451257299012));
#44994=CARTESIAN_POINT('Ctrl Pts',(-0.341886065992276,51.0898981781938,
-1.12873174380644));
#44995=CARTESIAN_POINT('Ctrl Pts',(-0.410334145193804,51.0950125571576,
-1.10401093693003));
#44996=CARTESIAN_POINT('Ctrl Pts',(-0.420551110570461,51.0957733414174,
-1.10015955411338));
#44997=CARTESIAN_POINT('Ctrl Pts',(-0.436573322274917,51.0969606512547,
-1.09386399330535));
#44998=CARTESIAN_POINT('Ctrl Pts',(-0.442414770692499,51.0973923061009,
-1.09151448772327));
#44999=CARTESIAN_POINT('Ctrl Pts',(-0.453575493683122,51.0982143007377,
-1.08692118274831));
#45000=CARTESIAN_POINT('Ctrl Pts',(-0.458897525140794,51.0986050325418,
-1.08468495376965));
#45001=CARTESIAN_POINT('Ctrl Pts',(-0.472172864730658,51.0995770408817,
-1.07899168191695));
#45002=CARTESIAN_POINT('Ctrl Pts',(-0.480105039530118,51.1001554559465,
-1.07548566983944));
#45003=CARTESIAN_POINT('Ctrl Pts',(-0.509733511398159,51.1023096872442,
-1.06199677958033));
#45004=CARTESIAN_POINT('Ctrl Pts',(-0.531164678955256,51.1038551905542,
-1.05144171215719));
#45005=CARTESIAN_POINT('Ctrl Pts',(-0.611049015760629,51.1096225734624,
-1.00903131307519));
#45006=CARTESIAN_POINT('Ctrl Pts',(-0.667089120057695,51.1136876364292,
-0.972891821773245));
#45007=CARTESIAN_POINT('Ctrl Pts',(-0.770541370313129,51.121777531743,-0.893014058272752));
#45008=CARTESIAN_POINT('Ctrl Pts',(-0.818011571922139,51.1257859992835,
-0.84974334255876));
#45009=CARTESIAN_POINT('Ctrl Pts',(-0.872811216364997,51.1310168703948,
-0.790923722052533));
#45010=CARTESIAN_POINT('Ctrl Pts',(-0.883653081669486,51.1320849386948,
-0.77879197632036));
#45011=CARTESIAN_POINT('Ctrl Pts',(-0.901150760090802,51.1338674846273,
-0.758376654340316));
#45012=CARTESIAN_POINT('Ctrl Pts',(-0.907952178926406,51.134575882362,-0.7502204146024));
#45013=CARTESIAN_POINT('Ctrl Pts',(-0.921067773759815,51.1359735321554,
-0.734052619190414));
#45014=CARTESIAN_POINT('Ctrl Pts',(-0.927390011419804,51.1366623729528,
-0.726048790998807));
#45015=CARTESIAN_POINT('Ctrl Pts',(-0.941100457753503,51.1381906167781,
-0.708220359674336));
#45016=CARTESIAN_POINT('Ctrl Pts',(-0.948440327817344,51.1390318176979,
-0.698360275165104));
#45017=CARTESIAN_POINT('Ctrl Pts',(-0.973557659205522,51.1419937492174,
-0.663492218655802));
#45018=CARTESIAN_POINT('Ctrl Pts',(-0.990509802363704,51.1441449215001,
-0.637907889233139));
#45019=CARTESIAN_POINT('Ctrl Pts',(-1.05377161414093,51.1528131596257,-0.533820715178569));
#45020=CARTESIAN_POINT('Ctrl Pts',(-1.09189912605093,51.1595830022785,-0.450723545126745));
#45021=CARTESIAN_POINT('Ctrl Pts',(-1.12777674903422,51.1680416497381,-0.340348828181685));
#45022=CARTESIAN_POINT('Ctrl Pts',(-1.13473488269983,51.1698462128101,-0.316377326596745));
#45023=CARTESIAN_POINT('Ctrl Pts',(-1.1450997369968,51.1728211756122,-0.27590684676094));
#45024=CARTESIAN_POINT('Ctrl Pts',(-1.14892366495532,51.1740061863463,-0.259523560887414));
#45025=CARTESIAN_POINT('Ctrl Pts',(-1.15392749480546,51.1756892291304,-0.235799706364306));
#45026=CARTESIAN_POINT('Ctrl Pts',(-1.15539081485754,51.1762011132553,-0.228521852527856));
#45027=CARTESIAN_POINT('Ctrl Pts',(-1.15774799219058,51.1770599898401,-0.216196476381845));
#45028=CARTESIAN_POINT('Ctrl Pts',(-1.15867785046393,51.1774089288977,-0.211156274547567));
#45029=CARTESIAN_POINT('Ctrl Pts',(-1.16075383077045,51.1782121752737,-0.199476801350127));
#45030=CARTESIAN_POINT('Ctrl Pts',(-1.16187593012931,51.1786651446625,-0.192833551224834));
#45031=CARTESIAN_POINT('Ctrl Pts',(-1.16494535584697,51.179962116542,-0.1736610032469));
#45032=CARTESIAN_POINT('Ctrl Pts',(-1.1667475089576,51.1807985800248,-0.161108995408212));
#45033=CARTESIAN_POINT('Ctrl Pts',(-1.17456551124465,51.184845870989,-0.0996119622266914));
#45034=CARTESIAN_POINT('Ctrl Pts',(-1.17770665723725,51.1879323382119,-0.0503463966565076));
#45035=CARTESIAN_POINT('Ctrl Pts',(-1.17783255203574,51.1969082215981,0.0944037241186597));
#45036=CARTESIAN_POINT('Ctrl Pts',(-1.1663181155478,51.2027161345442,0.189478315892197));
#45037=CARTESIAN_POINT('Ctrl Pts',(-1.13930656857895,51.2100358070486,0.298958885154033));
#45038=CARTESIAN_POINT('Ctrl Pts',(-1.13478072718027,51.2111722248204,0.315703219194191));
#45039=CARTESIAN_POINT('Ctrl Pts',(-1.12682925057453,51.2130379320123,0.342736520701312));
#45040=CARTESIAN_POINT('Ctrl Pts',(-1.12362826754823,51.2137599065956,0.353089203523291));
#45041=CARTESIAN_POINT('Ctrl Pts',(-1.11713896443712,51.2151703743131,0.373094568546962));
#45042=CARTESIAN_POINT('Ctrl Pts',(-1.11386722459418,51.2158582672985,0.382751639497525));
#45043=CARTESIAN_POINT('Ctrl Pts',(-1.10581870568822,51.217498169777,0.405530555001746));
#45044=CARTESIAN_POINT('Ctrl Pts',(-1.10093321982709,51.2184537126734,0.418612060193123));
#45045=CARTESIAN_POINT('Ctrl Pts',(-1.08273700904316,51.2218791786702,0.464811232996171));
#45046=CARTESIAN_POINT('Ctrl Pts',(-1.06815608491228,51.2243906140529,0.497404294368731));
#45047=CARTESIAN_POINT('Ctrl Pts',(-1.02485615446862,51.2312829180026,0.583476859005111));
#45048=CARTESIAN_POINT('Ctrl Pts',(-0.993448591200546,51.2357361501649,
0.63547937547028));
#45049=CARTESIAN_POINT('Ctrl Pts',(-0.925922546140864,51.2442693530678,
0.729958843424596));
#45050=CARTESIAN_POINT('Ctrl Pts',(-0.890514443913304,51.2483367991947,
0.772759722888525));
#45051=CARTESIAN_POINT('Ctrl Pts',(-0.843382058520212,51.2531607508105,
0.822171301195518));
#45052=CARTESIAN_POINT('Ctrl Pts',(-0.834395174539325,51.2540567611435,
0.831290365152012));
#45053=CARTESIAN_POINT('Ctrl Pts',(-0.820436125759192,51.2554102760242,
0.845000213032642));
#45054=CARTESIAN_POINT('Ctrl Pts',(-0.815570432673642,51.2558752009452,
0.849697399961489));
#45055=CARTESIAN_POINT('Ctrl Pts',(-0.806573191788908,51.2567219567454,
0.858234558088236));
#45056=CARTESIAN_POINT('Ctrl Pts',(-0.80245430146567,51.2571046785391,0.862086983076733));
#45057=CARTESIAN_POINT('Ctrl Pts',(-0.792635459192559,51.2580056985756,
0.871139260230269));
#45058=CARTESIAN_POINT('Ctrl Pts',(-0.786911856515027,51.2585220756768,
0.87631291217442));
#45059=CARTESIAN_POINT('Ctrl Pts',(-0.767195435336329,51.2602726387528,
0.893785923625735));
#45060=CARTESIAN_POINT('Ctrl Pts',(-0.752961102993835,51.2614886933439,
0.905810014620946));
#45061=CARTESIAN_POINT('Ctrl Pts',(-0.715888275090469,51.2645541573368,
0.935648203641285));
#45062=CARTESIAN_POINT('Ctrl Pts',(-0.692666570512478,51.2663800891113,
0.952967375375869));
#45063=CARTESIAN_POINT('Ctrl Pts',(-0.593421352118865,51.2739072608547,
1.02143972436333));
#45064=CARTESIAN_POINT('Ctrl Pts',(-0.512204988751643,51.2794460883624,
1.06448767250117));
#45065=CARTESIAN_POINT('Ctrl Pts',(-0.402106936592523,51.2869912385975,
1.10729767693632));
#45066=CARTESIAN_POINT('Ctrl Pts',(-0.377078088286573,51.288706478194,1.11606903135868));
#45067=CARTESIAN_POINT('Ctrl Pts',(-0.339761589612949,51.2912764836053,
1.12774802547282));
#45068=CARTESIAN_POINT('Ctrl Pts',(-0.327688093268305,51.2921098654283,
1.13131518149038));
#45069=CARTESIAN_POINT('Ctrl Pts',(-0.305901419416378,51.2936182739578,
1.1373741203664));
#45070=CARTESIAN_POINT('Ctrl Pts',(-0.296209088502571,51.2942909284969,
1.13993672335503));
#45071=CARTESIAN_POINT('Ctrl Pts',(-0.275313088074717,51.295745134872,1.14517703369123));
#45072=CARTESIAN_POINT('Ctrl Pts',(-0.264100560390666,51.2965279010022,
1.14781471172112));
#45073=CARTESIAN_POINT('Ctrl Pts',(-0.232608376654076,51.2987341222224,
1.15473719504402));
#45074=CARTESIAN_POINT('Ctrl Pts',(-0.212252528496873,51.3001691190988,
1.15865155062833));
#45075=CARTESIAN_POINT('Ctrl Pts',(-0.165672349411034,51.3034749217905,
1.16634011382907));
#45076=CARTESIAN_POINT('Ctrl Pts',(-0.139403331971461,51.3053551220269,
1.16977054257879));
#45077=CARTESIAN_POINT('Ctrl Pts',(-0.0407383696870978,51.3124717240502,
1.17928451237274));
#45078=CARTESIAN_POINT('Ctrl Pts',(0.0320517482618634,51.3178436886102,
1.1795518796349));
#45079=CARTESIAN_POINT('Ctrl Pts',(0.132697673873903,51.3252393043525,1.17059549570839));
#45080=CARTESIAN_POINT('Ctrl Pts',(0.160897548225851,51.3273060734476,1.16705360006949));
#45081=CARTESIAN_POINT('Ctrl Pts',(0.188938476720627,51.3293408135491,1.16249615677407));
#45082=CARTESIAN_POINT('',(-1.17774999976701,51.2893671147362,2.34267279165755E-5));
#45083=CARTESIAN_POINT('Ctrl Pts',(0.18893837638019,51.427308721746,1.16249617308222));
#45084=CARTESIAN_POINT('Ctrl Pts',(0.167780174989307,51.4257360879916,1.16593497684819));
#45085=CARTESIAN_POINT('Ctrl Pts',(0.146525093563944,51.4241589555535,1.16879662929704));
#45086=CARTESIAN_POINT('Ctrl Pts',(0.0744055527542759,51.418832162536,1.17650673483916));
#45087=CARTESIAN_POINT('Ctrl Pts',(0.0233102087280465,51.4150970553667,
1.17862710853437));
#45088=CARTESIAN_POINT('Ctrl Pts',(-0.0405152136121301,51.4105874701334,
1.17712201115765));
#45089=CARTESIAN_POINT('Ctrl Pts',(-0.0532600023433328,51.4096949223222,
1.17661426000105));
#45090=CARTESIAN_POINT('Ctrl Pts',(-0.072735501794312,51.4083456019064,
1.17552124243315));
#45091=CARTESIAN_POINT('Ctrl Pts',(-0.0794731812488466,51.4078814729405,
1.17508496022441));
#45092=CARTESIAN_POINT('Ctrl Pts',(-0.091831473921267,51.4070355324296,
1.17417794590902));
#45093=CARTESIAN_POINT('Ctrl Pts',(-0.0974527636959587,51.4066528402923,
1.17372476714136));
#45094=CARTESIAN_POINT('Ctrl Pts',(-0.110767715544907,51.4057510925089,
1.17255501921064));
#45095=CARTESIAN_POINT('Ctrl Pts',(-0.118457900540155,51.4052339703768,
1.17180309514844));
#45096=CARTESIAN_POINT('Ctrl Pts',(-0.144744876568355,51.4034772420464,
1.16897139686902));
#45097=CARTESIAN_POINT('Ctrl Pts',(-0.163300211919216,51.4022559435375,
1.16652404168512));
#45098=CARTESIAN_POINT('Ctrl Pts',(-0.210591949586825,51.3991731845479,
1.15913582489187));
#45099=CARTESIAN_POINT('Ctrl Pts',(-0.239218277354355,51.3973355420423,
1.15356823024454));
#45100=CARTESIAN_POINT('Ctrl Pts',(-0.358192952257415,51.3897103972331,
1.1258085136181));
#45101=CARTESIAN_POINT('Ctrl Pts',(-0.445948766863184,51.3840880113415,
1.0940185434197));
#45102=CARTESIAN_POINT('Ctrl Pts',(-0.551737390743096,51.3765122948905,
1.04082932542601));
#45103=CARTESIAN_POINT('Ctrl Pts',(-0.574047382370542,51.3748674948078,
1.02869299991465));
#45104=CARTESIAN_POINT('Ctrl Pts',(-0.606634683896286,51.372382602165,1.009575640819));
#45105=CARTESIAN_POINT('Ctrl Pts',(-0.617222844451097,51.3715618199211,
1.00313735601702));
#45106=CARTESIAN_POINT('Ctrl Pts',(-0.636176652026868,51.3700669368533,
0.991198528930466));
#45107=CARTESIAN_POINT('Ctrl Pts',(-0.644577591169899,51.369395024632,0.985756042144522));
#45108=CARTESIAN_POINT('Ctrl Pts',(-0.662610458342805,51.3679318079224,
0.973744499216107));
#45109=CARTESIAN_POINT('Ctrl Pts',(-0.672216185156617,51.3671391486798,
0.967138228250668));
#45110=CARTESIAN_POINT('Ctrl Pts',(-0.699211437608676,51.3648726854243,
0.947975967038142));
#45111=CARTESIAN_POINT('Ctrl Pts',(-0.716357449216303,51.3633862892541,
0.935086610213727));
#45112=CARTESIAN_POINT('Ctrl Pts',(-0.793330562604256,51.3564904718998,
0.87386291113953));
#45113=CARTESIAN_POINT('Ctrl Pts',(-0.848677326237563,51.3508761527402,
0.820215294973942));
#45114=CARTESIAN_POINT('Ctrl Pts',(-0.937374133903037,51.3407959364567,
0.715582883139381));
#45115=CARTESIAN_POINT('Ctrl Pts',(-0.972770288346427,51.3363636073935,
0.66666958629533));
#45116=CARTESIAN_POINT('Ctrl Pts',(-1.01091726541823,51.3312059417839,0.604403318100627));
#45117=CARTESIAN_POINT('Ctrl Pts',(-1.01739081566078,51.3303151488728,0.593441698469523));
#45118=CARTESIAN_POINT('Ctrl Pts',(-1.02702163454418,51.3289679150825,0.576512911972019));
#45119=CARTESIAN_POINT('Ctrl Pts',(-1.03030723663795,51.3285041507016,0.570620345994147));
#45120=CARTESIAN_POINT('Ctrl Pts',(-1.03624659777287,51.3276585211019,0.559749824898884));
#45121=CARTESIAN_POINT('Ctrl Pts',(-1.03891538224669,51.3272757807603,0.554780774970583));
#45122=CARTESIAN_POINT('Ctrl Pts',(-1.04515906457285,51.3263734609112,0.542952495746081));
#45123=CARTESIAN_POINT('Ctrl Pts',(-1.0487022468717,51.3258558226858,0.536076942650783));
#45124=CARTESIAN_POINT('Ctrl Pts',(-1.06060816652715,51.324095201414,0.512403608216472));
#45125=CARTESIAN_POINT('Ctrl Pts',(-1.06863753754756,51.3228706354384,0.495440256450002));
#45126=CARTESIAN_POINT('Ctrl Pts',(-1.08814551674467,51.3197771614402,0.451543082856523));
#45127=CARTESIAN_POINT('Ctrl Pts',(-1.09903191498767,51.3179322813617,0.424359387068967));
#45128=CARTESIAN_POINT('Ctrl Pts',(-1.13882945481606,51.3105606260455,0.313140511963303));
#45129=CARTESIAN_POINT('Ctrl Pts',(-1.15920077778096,51.3051834696005,0.226369194553585));
#45130=CARTESIAN_POINT('Ctrl Pts',(-1.17285020539874,51.2977662631761,0.110793778666655));
#45131=CARTESIAN_POINT('Ctrl Pts',(-1.17511915485752,51.2959890681501,0.0833525912917017));
#45132=CARTESIAN_POINT('Ctrl Pts',(-1.17694443035614,51.2934631968828,0.0449109468104858));
#45133=CARTESIAN_POINT('Ctrl Pts',(-1.17731138884305,51.2927393751073,0.0339568204069161));
#45134=CARTESIAN_POINT('Ctrl Pts',(-1.17767546588511,51.2914999929461,0.0153168226509932));
#45135=CARTESIAN_POINT('Ctrl Pts',(-1.17775032938723,51.2909868759087,0.00763308451535553));
#45136=CARTESIAN_POINT('Ctrl Pts',(-1.17774999891067,51.2904714046889,-5.06548628808275E-5));
#45137=CARTESIAN_POINT('Ctrl Pts',(-1.17774999976701,51.2893671147362,2.34267279165755E-5));
#45138=CARTESIAN_POINT('Ctrl Pts',(-1.17775098584611,51.2860358491932,-0.0495504902548409));
#45139=CARTESIAN_POINT('Ctrl Pts',(-1.17461756283641,51.2827045836502,-0.0990659735613131));
#45140=CARTESIAN_POINT('Ctrl Pts',(-1.1683981279826,51.2793733181072,-0.148124532157086));
#45141=CARTESIAN_POINT('Ctrl Pts',(-1.16220075919595,51.2760538716331,-0.197009034833941));
#45142=CARTESIAN_POINT('Ctrl Pts',(-1.15293941438527,51.272734425159,-0.245439390503012));
#45143=CARTESIAN_POINT('Ctrl Pts',(-1.14071301295608,51.2694149786849,-0.293033930753193));
#45144=CARTESIAN_POINT('Ctrl Pts',(-1.12842131238035,51.2660778036074,-0.340882665410138));
#45145=CARTESIAN_POINT('Ctrl Pts',(-1.11313296878558,51.26274062853,-0.387886174007096));
#45146=CARTESIAN_POINT('Ctrl Pts',(-1.0949976714854,51.2594034534525,-0.433676333158223));
#45147=CARTESIAN_POINT('Ctrl Pts',(-1.07686237418522,51.256066278375,-0.479466492309345));
#45148=CARTESIAN_POINT('Ctrl Pts',(-1.0558803976495,51.2527291032976,-0.524042897517819));
#45149=CARTESIAN_POINT('Ctrl Pts',(-1.03224706539606,51.2493919282201,-0.567063540073974));
#45150=CARTESIAN_POINT('Ctrl Pts',(-1.00882545342797,51.2460846493779,-0.609698780240791));
#45151=CARTESIAN_POINT('Ctrl Pts',(-0.982702983883552,51.2427773705356,
-0.650980507097607));
#45152=CARTESIAN_POINT('Ctrl Pts',(-0.954064531220093,51.2394700916934,
-0.690547560105591));
#45153=CARTESIAN_POINT('Ctrl Pts',(-0.926613588631255,51.2362999510894,
-0.728473942277681));
#45154=CARTESIAN_POINT('Ctrl Pts',(-0.896851585769304,51.2331298104854,
-0.764824550574183));
#45155=CARTESIAN_POINT('Ctrl Pts',(-0.864987948315027,51.2299596698814,
-0.79930651928391));
#45156=CARTESIAN_POINT('Ctrl Pts',(-0.83315629824842,51.22679271173,-0.833753872105784));
#45157=CARTESIAN_POINT('Ctrl Pts',(-0.799227566282257,51.2236257535786,
-0.866335889631641));
#45158=CARTESIAN_POINT('Ctrl Pts',(-0.763451669643917,51.2204587954272,
-0.896792401070568));
#45159=CARTESIAN_POINT('Ctrl Pts',(-0.727695879834679,51.2172936171749,
-0.927231795290136));
#45160=CARTESIAN_POINT('Ctrl Pts',(-0.690095406083873,51.2141284389227,
-0.955547688190852));
#45161=CARTESIAN_POINT('Ctrl Pts',(-0.650935286476295,51.2109632606704,
-0.981518372380275));
#45162=CARTESIAN_POINT('Ctrl Pts',(-0.611779873486442,51.2077984628379,
-1.00748593517774));
#45163=CARTESIAN_POINT('Ctrl Pts',(-0.571065652962939,51.2046336650054,
-1.03110854201715));
#45164=CARTESIAN_POINT('Ctrl Pts',(-0.529106582671327,51.2014688671729,
-1.05220781534537));
#45165=CARTESIAN_POINT('Ctrl Pts',(-0.487104733704155,51.1983008427232,
-1.07332860008845));
#45166=CARTESIAN_POINT('Ctrl Pts',(-0.443856002868032,51.1951328182734,
-1.09192066801306));
#45167=CARTESIAN_POINT('Ctrl Pts',(-0.399697098116125,51.1919647938237,
-1.10785255889832));
#45168=CARTESIAN_POINT('Ctrl Pts',(-0.355511452057059,51.1887948509134,
-1.12379409765845));
#45169=CARTESIAN_POINT('Ctrl Pts',(-0.310415071177013,51.1856249080032,
-1.13707209616858));
#45170=CARTESIAN_POINT('Ctrl Pts',(-0.264759183772611,51.1824549650929,
-1.14760517474786));
#45171=CARTESIAN_POINT('Ctrl Pts',(-0.219019813394498,51.1792792258599,
-1.15815751333438));
#45172=CARTESIAN_POINT('Ctrl Pts',(-0.172719446179654,51.1761034866269,
-1.16595482962459));
#45173=CARTESIAN_POINT('Ctrl Pts',(-0.126216922168788,51.1729277473938,
-1.17096727155725));
#45174=CARTESIAN_POINT('Ctrl Pts',(-0.112010662799723,51.1719575769312,
-1.17249854435765));
#45175=CARTESIAN_POINT('Ctrl Pts',(-0.0977855444772725,51.1709874064686,
-1.1737702818834));
#45176=CARTESIAN_POINT('Ctrl Pts',(-0.083551780083155,51.1700172360059,
-1.17478260224815));
#45177=CARTESIAN_POINT('Ctrl Pts',(-0.0350293506342434,51.1667099571637,
-1.17823356870497));
#45178=CARTESIAN_POINT('Ctrl Pts',(0.0138210693818673,51.1634026783214,
-1.17868136187856));
#45179=CARTESIAN_POINT('Ctrl Pts',(0.0625957882037462,51.1600953994792,
-1.17608538371972));
#45180=CARTESIAN_POINT('Ctrl Pts',(0.109348059870649,51.1569252571873,-1.17359704797827));
#45181=CARTESIAN_POINT('Ctrl Pts',(0.156030159644109,51.1537551148954,-1.16831243738101));
#45182=CARTESIAN_POINT('Ctrl Pts',(0.202282451386361,51.1505849726035,-1.16024862523561));
#45183=CARTESIAN_POINT('Ctrl Pts',(0.248488310997001,51.1474180127802,-1.15219290825637));
#45184=CARTESIAN_POINT('Ctrl Pts',(0.294264668904109,51.1442510529569,-1.1413636068324));
#45185=CARTESIAN_POINT('Ctrl Pts',(0.339257391268508,51.1410840931336,-1.12782954606168));
#45186=CARTESIAN_POINT('Ctrl Pts',(0.384224826492013,51.1379189132283,-1.11430309180338));
#45187=CARTESIAN_POINT('Ctrl Pts',(0.428408964712441,51.1347537333231,-1.09807504974805));
#45188=CARTESIAN_POINT('Ctrl Pts',(0.471468933732513,51.1315885534178,-1.07926461399655));
#45189=CARTESIAN_POINT('Ctrl Pts',(0.514523727118959,51.1284237539544,-1.06045643918314));
#45190=CARTESIAN_POINT('Ctrl Pts',(0.556454108913126,51.1252589544909,-1.03906671208195));
#45191=CARTESIAN_POINT('Ctrl Pts',(0.596939920603469,51.1220941550275,-1.01526242602094));
#45192=CARTESIAN_POINT('Ctrl Pts',(0.637467008344609,51.1189261289911,-0.991433871040036));
#45193=CARTESIAN_POINT('Ctrl Pts',(0.676546105853428,51.1157581029547,-0.96518612986692));
#45194=CARTESIAN_POINT('Ctrl Pts',(0.713884128734477,51.1125900769183,-0.936730758137586));
#45195=CARTESIAN_POINT('Ctrl Pts',(0.751244762108054,51.1094201324454,-0.908258154912843));
#45196=CARTESIAN_POINT('Ctrl Pts',(0.786861799734846,51.1062501879724,-0.877575625595539));
#45197=CARTESIAN_POINT('Ctrl Pts',(0.820476352944512,51.1030802434994,-0.844934090186254));
#45198=CARTESIAN_POINT('Ctrl Pts',(0.854152370666398,51.0999045027546,-0.81223286943653));
#45199=CARTESIAN_POINT('Ctrl Pts',(0.885818225532972,51.0967287620097,-0.777565910679258));
#45200=CARTESIAN_POINT('Ctrl Pts',(0.915254187814639,51.0935530212648,-0.741218479389016));
#45201=CARTESIAN_POINT('Ctrl Pts',(0.924246599559352,51.0925828621071,-0.730114678368451));
#45202=CARTESIAN_POINT('Ctrl Pts',(0.933031212701967,51.0916127029495,-0.718854254181465));
#45203=CARTESIAN_POINT('Ctrl Pts',(0.941602586729074,51.0906425437918,-0.707445850341294));
#45204=CARTESIAN_POINT('Ctrl Pts',(0.970822456216233,51.0873352649495,-0.6685545278751));
#45205=CARTESIAN_POINT('Ctrl Pts',(0.997697300846977,51.0840279861073,-0.627758608695592));
#45206=CARTESIAN_POINT('Ctrl Pts',(1.021974034713,51.080720707265,-0.585375208624723));
#45207=CARTESIAN_POINT('Ctrl Pts',(1.04524415178131,51.0775505622916,-0.544749204861402));
#45208=CARTESIAN_POINT('Ctrl Pts',(1.06612707311976,51.0743804173181,-0.502665325701072));
#45209=CARTESIAN_POINT('Ctrl Pts',(1.08444205916883,51.0712102723447,-0.45943496036508));
#45210=CARTESIAN_POINT('Ctrl Pts',(1.1027386591622,51.0680433098177,-0.416247993145983));
#45211=CARTESIAN_POINT('Ctrl Pts',(1.11847220888306,51.0648763472907,-0.3719173293596));
#45212=CARTESIAN_POINT('Ctrl Pts',(1.13150842972917,51.0617093847637,-0.326777808230353));
#45213=CARTESIAN_POINT('Ctrl Pts',(1.14453732393725,51.0585442021381,-0.281663656488119));
#45214=CARTESIAN_POINT('Ctrl Pts',(1.15487173727667,51.0553790195126,-0.235742083379568));
#45215=CARTESIAN_POINT('Ctrl Pts',(1.1624268994366,51.052213836887,-0.189364109498653));
#45216=CARTESIAN_POINT('Ctrl Pts',(1.16998115352415,51.049049034692,-0.142991709893506));
#45217=CARTESIAN_POINT('Ctrl Pts',(1.17475673178944,51.045884232497,-0.0961635695605844));
#45218=CARTESIAN_POINT('Ctrl Pts',(1.1767202556796,51.0427194303021,-0.049239236116421));
#45219=CARTESIAN_POINT('Ctrl Pts',(1.17868578141524,51.0395514015383,-0.00226706252884466));
#45220=CARTESIAN_POINT('Ctrl Pts',(1.17783351024976,51.0363833727745,0.0448009409663622));
#45221=CARTESIAN_POINT('Ctrl Pts',(1.17418218625771,51.0332153440107,0.0916037989117204));
#45222=CARTESIAN_POINT('Ctrl Pts',(1.17052865116323,51.0300453968096,0.138434998881334));
#45223=CARTESIAN_POINT('Ctrl Pts',(1.16407276720998,51.0268754496086,0.185000180531924));
#45224=CARTESIAN_POINT('Ctrl Pts',(1.1548848974311,51.0237055024075,0.230945742947455));
#45225=CARTESIAN_POINT('Ctrl Pts',(1.14568022764256,51.0205297589615,0.276975316772712));
#45226=CARTESIAN_POINT('Ctrl Pts',(1.13373375151382,51.0173540155155,0.322382472471943));
#45227=CARTESIAN_POINT('Ctrl Pts',(1.11916592698197,51.0141782720695,0.366827875689118));
#45228=CARTESIAN_POINT('Ctrl Pts',(1.11471568346571,51.0132081319055,0.380405254182543));
#45229=CARTESIAN_POINT('Ctrl Pts',(1.11002115248972,51.0122379917416,0.393893025709404));
#45230=CARTESIAN_POINT('Ctrl Pts',(1.10508664395222,51.0112678515776,0.407281931662105));
#45231=CARTESIAN_POINT('Ctrl Pts',(1.08826454309579,51.0079605727353,0.452925692247782));
#45232=CARTESIAN_POINT('Ctrl Pts',(1.06857035799753,51.0046532938931,0.4976325612908));
#45233=CARTESIAN_POINT('Ctrl Pts',(1.04613320897857,51.0013460150508,0.54101790319009));
#45234=CARTESIAN_POINT('Ctrl Pts',(1.02462648268996,50.9981758823053,0.582604143597785));
#45235=CARTESIAN_POINT('Ctrl Pts',(1.00060010244264,50.9950057495598,0.622975750099127));
#45236=CARTESIAN_POINT('Ctrl Pts',(0.974217620543403,50.9918356168143,0.661811975052393));
#45237=CARTESIAN_POINT('Ctrl Pts',(0.947861623483634,50.9886686665009,0.70060921310567));
#45238=CARTESIAN_POINT('Ctrl Pts',(0.919154518118493,50.9855017161875,0.73787366022939));
#45239=CARTESIAN_POINT('Ctrl Pts',(0.888304759476732,50.9823347658741,0.773310879783147));
#45240=CARTESIAN_POINT('Ctrl Pts',(0.857472338765933,50.9791695954244,0.808728183198395));
#45241=CARTESIAN_POINT('Ctrl Pts',(0.824500015962497,50.9760044249747,0.842319872634824));
#45242=CARTESIAN_POINT('Ctrl Pts',(0.789636695488352,50.972839254525,0.873824325387109));
#45243=CARTESIAN_POINT('Ctrl Pts',(0.754777564660626,50.9696744644448,0.905324992139786));
#45244=CARTESIAN_POINT('Ctrl Pts',(0.718028302689345,50.9665096743647,0.93473854743771));
#45245=CARTESIAN_POINT('Ctrl Pts',(0.679672854675254,50.9633448842845,0.961841916906095));
#45246=CARTESIAN_POINT('Ctrl Pts',(0.641278300311027,50.9601768674557,0.98897292035899));
#45247=CARTESIAN_POINT('Ctrl Pts',(0.601274749852972,50.9570088506269,1.01378871647048));
#45248=CARTESIAN_POINT('Ctrl Pts',(0.559975621549293,50.9538408337982,1.03610924412944));
#45249=CARTESIAN_POINT('Ctrl Pts',(0.518651482791735,50.9506708984413,1.05844328893878));
#45250=CARTESIAN_POINT('Ctrl Pts',(0.476030711412737,50.9475009630844,1.07827882276602));
#45251=CARTESIAN_POINT('Ctrl Pts',(0.4324485306959,50.9443310277275,1.09548314948198));
#45252=CARTESIAN_POINT('Ctrl Pts',(0.388786656222819,50.9411552958718,1.11271893578526));
#45253=CARTESIAN_POINT('Ctrl Pts',(0.344160396506679,50.9379795640162,1.12731374621947));
#45254=CARTESIAN_POINT('Ctrl Pts',(0.298920163199764,50.9348038321606,1.13918470782074));
#45255=CARTESIAN_POINT('Ctrl Pts',(0.28509872797285,50.9338336078948,1.14281142932193));
#45256=CARTESIAN_POINT('Ctrl Pts',(0.271220048283304,50.9328633836291,1.14618427629002));
#45257=CARTESIAN_POINT('Ctrl Pts',(0.257294242770588,50.9318931593634,1.14930184683446));
#45258=CARTESIAN_POINT('Ctrl Pts',(0.23466980178663,50.930316892797,1.15436678119188));
#45259=CARTESIAN_POINT('Ctrl Pts',(0.211870534327436,50.9287406262305,1.1587690496606));
#45260=CARTESIAN_POINT('Ctrl Pts',(0.18893846240316,50.927164359664,1.16249615910107));
#45261=CARTESIAN_POINT('Origin',(0.,56.5393671147362,0.));
#45262=CARTESIAN_POINT('',(0.188938462403167,50.3284861847587,1.16249615910106));
#45263=CARTESIAN_POINT('',(0.188738354032613,50.4271343927849,1.1611983583706));
#45264=CARTESIAN_POINT('',(0.188938462403162,56.5393671147362,1.16249615910107));
#45265=CARTESIAN_POINT('',(-1.17774975332751,50.6906328852214,0.000762257828655969));
#45266=CARTESIAN_POINT('Ctrl Pts',(-1.17774975332751,50.6906328852214,0.000762257828655968));
#45267=CARTESIAN_POINT('Ctrl Pts',(-1.17777960133562,50.6875036592274,-0.0453553192892874));
#45268=CARTESIAN_POINT('Ctrl Pts',(-1.17509643829781,50.6843744332334,-0.0915797958995521));
#45269=CARTESIAN_POINT('Ctrl Pts',(-1.16968895932775,50.6812452072394,-0.137560172022192));
#45270=CARTESIAN_POINT('Ctrl Pts',(-1.16428831115918,50.6781199341265,-0.183482465104016));
#45271=CARTESIAN_POINT('Ctrl Pts',(-1.15617021436046,50.6749946610137,-0.229160700083915));
#45272=CARTESIAN_POINT('Ctrl Pts',(-1.1453753572639,50.6718693879008,-0.274245060981234));
#45273=CARTESIAN_POINT('Ctrl Pts',(-1.13458905489139,50.6687465915089,-0.319293693358658));
#45274=CARTESIAN_POINT('Ctrl Pts',(-1.12113032074461,50.665623795117,-0.363748824722831));
#45275=CARTESIAN_POINT('Ctrl Pts',(-1.1050910789745,50.6625009987251,-0.40726989782081));
#45276=CARTESIAN_POINT('Ctrl Pts',(-1.08905700047954,50.6593792076088,-0.450776960825402));
#45277=CARTESIAN_POINT('Ctrl Pts',(-1.07044425940943,50.6562574164924,-0.493350022218267));
#45278=CARTESIAN_POINT('Ctrl Pts',(-1.04939397700165,50.653135625376,-0.534665637134698));
#45279=CARTESIAN_POINT('Ctrl Pts',(-1.02832572433874,50.6500111692416,-0.576016522463505));
#45280=CARTESIAN_POINT('Ctrl Pts',(-1.00481603678679,50.6468867131071,-0.616107304310351));
#45281=CARTESIAN_POINT('Ctrl Pts',(-0.979052376769155,50.6437622569727,
-0.65463845444846));
#45282=CARTESIAN_POINT('Ctrl Pts',(-0.953276437597511,50.640636311699,-0.693187968822341));
#45283=CARTESIAN_POINT('Ctrl Pts',(-0.925244736251638,50.6375103664252,
-0.730175913647999));
#45284=CARTESIAN_POINT('Ctrl Pts',(-0.895186268754897,50.6343844211515,
-0.765334310437397));
#45285=CARTESIAN_POINT('Ctrl Pts',(-0.865072275691823,50.6312527014689,
-0.800557653648075));
#45286=CARTESIAN_POINT('Ctrl Pts',(-0.832924448549775,50.6281209817863,
-0.833944294490212));
#45287=CARTESIAN_POINT('Ctrl Pts',(-0.799008557989088,50.6249892621037,
-0.865263189301497));
#45288=CARTESIAN_POINT('Ctrl Pts',(-0.783246088514481,50.6235337899022,
-0.879818700458073));
#45289=CARTESIAN_POINT('Ctrl Pts',(-0.767102188339089,50.6220783177007,
-0.893928168453297));
#45290=CARTESIAN_POINT('Ctrl Pts',(-0.750605721389883,50.6206228454992,
-0.907571547326586));
#45291=CARTESIAN_POINT('Ctrl Pts',(-0.713120693467588,50.617315566657,-0.938573484868386));
#45292=CARTESIAN_POINT('Ctrl Pts',(-0.673623973074418,50.6140082878147,
-0.96732176496925));
#45293=CARTESIAN_POINT('Ctrl Pts',(-0.632420466200204,50.6107010089725,
-0.993548899869109));
#45294=CARTESIAN_POINT('Ctrl Pts',(-0.592917355023133,50.607530215666,-1.01869368739819));
#45295=CARTESIAN_POINT('Ctrl Pts',(-0.551846104246025,50.6043594223596,
-1.04152101376355));
#45296=CARTESIAN_POINT('Ctrl Pts',(-0.509509439020997,50.6011886290531,
-1.06183576604318));
#45297=CARTESIAN_POINT('Ctrl Pts',(-0.467215333017838,50.5980210232083,
-1.08213009677934));
#45298=CARTESIAN_POINT('Ctrl Pts',(-0.423658831060098,50.5948534173635,
-1.09991661186439));
#45299=CARTESIAN_POINT('Ctrl Pts',(-0.379168248237177,50.5916858115186,
-1.11504551567582));
#45300=CARTESIAN_POINT('Ctrl Pts',(-0.334702752040581,50.5885199917719,
-1.13016588884699));
#45301=CARTESIAN_POINT('Ctrl Pts',(-0.289304745753612,50.5853541720251,
-1.14263143956209));
#45302=CARTESIAN_POINT('Ctrl Pts',(-0.243321018792249,50.5821883522784,
-1.15234107117377));
#45303=CARTESIAN_POINT('Ctrl Pts',(-0.197342924872337,50.5790229203469,
-1.1620495133482));
#45304=CARTESIAN_POINT('Ctrl Pts',(-0.150779798929501,50.5758574884155,
-1.16900259328095));
#45305=CARTESIAN_POINT('Ctrl Pts',(-0.103989349852103,50.5726920564841,
-1.17315015135205));
#45306=CARTESIAN_POINT('Ctrl Pts',(-0.0571514356966482,50.5695234134812,
-1.17730191678109));
#45307=CARTESIAN_POINT('Ctrl Pts',(-0.0100862952838123,50.5663547704783,
-1.17864243359444));
#45308=CARTESIAN_POINT('Ctrl Pts',(0.0368444992566834,50.5631861274755,
-1.17717354089128));
#45309=CARTESIAN_POINT('Ctrl Pts',(0.0838035848038834,50.5600155743388,
-1.17570376270443));
#45310=CARTESIAN_POINT('Ctrl Pts',(0.130627607303061,50.556845021202,-1.17142125577396));
#45311=CARTESIAN_POINT('Ctrl Pts',(0.17695994161919,50.5536744680653,-1.1643797668983));
#45312=CARTESIAN_POINT('Ctrl Pts',(0.223376710912688,50.5504981369857,-1.15732544577572));
#45313=CARTESIAN_POINT('Ctrl Pts',(0.269299459827032,50.547321805906,-1.14750223200047));
#45314=CARTESIAN_POINT('Ctrl Pts',(0.314383465650027,50.5441454748264,-1.13501458097501));
#45315=CARTESIAN_POINT('Ctrl Pts',(0.328091404984733,50.5431797009793,-1.13121766986285));
#45316=CARTESIAN_POINT('Ctrl Pts',(0.34172193121587,50.5422139271322,-1.12717477801867));
#45317=CARTESIAN_POINT('Ctrl Pts',(0.355265722240397,50.5412481532851,-1.12288972259123));
#45318=CARTESIAN_POINT('Ctrl Pts',(0.401646242518149,50.5379408744428,-1.10821561105307));
#45319=CARTESIAN_POINT('Ctrl Pts',(0.447224421856732,50.5346335956006,-1.09062878989607));
#45320=CARTESIAN_POINT('Ctrl Pts',(0.491610142778868,50.5313263167583,-1.07024040757997));
#45321=CARTESIAN_POINT('Ctrl Pts',(0.534163917951637,50.5281555402707,-1.0506935213474));
#45322=CARTESIAN_POINT('Ctrl Pts',(0.575621176024836,50.524984763783,-1.02857207485304));
#45323=CARTESIAN_POINT('Ctrl Pts',(0.615653809146321,50.5218139872954,-1.00402462608425));
#45324=CARTESIAN_POINT('Ctrl Pts',(0.655646363744687,50.5186463852189,-0.979501752903342));
#45325=CARTESIAN_POINT('Ctrl Pts',(0.694216642462461,50.5154787831425,-0.952557974732043));
#45326=CARTESIAN_POINT('Ctrl Pts',(0.731060739788494,50.512311181066,-0.923387923486061));
#45327=CARTESIAN_POINT('Ctrl Pts',(0.767884212040613,50.5091453521916,-0.894234201435437));
#45328=CARTESIAN_POINT('Ctrl Pts',(0.802982980064314,50.5059795233171,-0.862857020689699));
#45329=CARTESIAN_POINT('Ctrl Pts',(0.836084039999323,50.5028136944427,-0.829492941837608));
#45330=CARTESIAN_POINT('Ctrl Pts',(0.869181178452938,50.4996482406239,-0.796132815626755));
#45331=CARTESIAN_POINT('Ctrl Pts',(0.900280687193004,50.496482786805,-0.760786656012133));
#45332=CARTESIAN_POINT('Ctrl Pts',(0.929146440585488,50.4933173329862,-0.723727817931104));
#45333=CARTESIAN_POINT('Ctrl Pts',(0.958041644055425,50.4901486496359,-0.68663117083685));
#45334=CARTESIAN_POINT('Ctrl Pts',(0.984698202406906,50.4869799662856,-0.647818800622675));
#45335=CARTESIAN_POINT('Ctrl Pts',(1.00892158498275,50.4838112829352,-0.607595505131413));
#45336=CARTESIAN_POINT('Ctrl Pts',(1.03315965209366,50.4806406786871,-0.567347825746148));
#45337=CARTESIAN_POINT('Ctrl Pts',(1.05496134947865,50.477470074439,-0.525688013787875));
#45338=CARTESIAN_POINT('Ctrl Pts',(1.07417844350484,50.4742994701909,-0.482944856075216));
#45339=CARTESIAN_POINT('Ctrl Pts',(1.09343064942889,50.4711230728748,-0.440123601570934));
#45340=CARTESIAN_POINT('Ctrl Pts',(1.11008863631632,50.4679466755587,-0.396215574995143));
#45341=CARTESIAN_POINT('Ctrl Pts',(1.12405323063788,50.4647702782426,-0.351567059310943));
#45342=CARTESIAN_POINT('Ctrl Pts',(1.12829838351607,50.4638046725187,-0.337994178459621));
#45343=CARTESIAN_POINT('Ctrl Pts',(1.13229499011369,50.4628390667948,-0.324352945767847));
#45344=CARTESIAN_POINT('Ctrl Pts',(1.13604120344335,50.4618734610709,-0.310653257795543));
#45345=CARTESIAN_POINT('Ctrl Pts',(1.14887229151292,50.4585661822287,-0.263730702289515));
#45346=CARTESIAN_POINT('Ctrl Pts',(1.1588219373472,50.4552589033864,-0.215900020683312));
#45347=CARTESIAN_POINT('Ctrl Pts',(1.16577105125511,50.4519516245441,-0.167549749494168));
#45348=CARTESIAN_POINT('Ctrl Pts',(1.17242391791113,50.4487853381048,-0.12126069577215));
#45349=CARTESIAN_POINT('Ctrl Pts',(1.17632682284683,50.4456190516655,-0.0744960820848609));
#45350=CARTESIAN_POINT('Ctrl Pts',(1.17742629591009,50.4424527652262,-0.027611233211309));
#45351=CARTESIAN_POINT('Ctrl Pts',(1.17852466466893,50.4392896589868,0.0192265247898934));
#45352=CARTESIAN_POINT('Ctrl Pts',(1.176825160427,50.4361265527474,0.0661837218374673));
#45353=CARTESIAN_POINT('Ctrl Pts',(1.1723261417246,50.4329634465079,0.112900309694455));
#45354=CARTESIAN_POINT('Ctrl Pts',(1.16782964112703,50.4298021106619,0.159590750235196));
#45355=CARTESIAN_POINT('Ctrl Pts',(1.16053678287553,50.4266407748159,0.206040291937972));
#45356=CARTESIAN_POINT('Ctrl Pts',(1.1504979143807,50.4234794389699,0.251892063204993));
#45357=CARTESIAN_POINT('Ctrl Pts',(1.14046020069847,50.4203184667854,0.297738559952893));
#45358=CARTESIAN_POINT('Ctrl Pts',(1.12767722550168,50.4171574946009,0.342986876561605));
#45359=CARTESIAN_POINT('Ctrl Pts',(1.11225025469533,50.4139965224165,0.387291148143334));
#45360=CARTESIAN_POINT('Ctrl Pts',(1.09680727846605,50.4108322707355,0.431641385236569));
#45361=CARTESIAN_POINT('Ctrl Pts',(1.07871501910745,50.4076680190546,0.475045093878604));
#45362=CARTESIAN_POINT('Ctrl Pts',(1.05812372171996,50.4045037673736,0.517174295603998));
#45363=CARTESIAN_POINT('Ctrl Pts',(1.0375197691433,50.4013375709777,0.559329389482157));
#45364=CARTESIAN_POINT('Ctrl Pts',(1.01441399866896,50.3981713745818,0.600207930638587));
#45365=CARTESIAN_POINT('Ctrl Pts',(0.989001906318251,50.3950051781859,0.639507851240988));
#45366=CARTESIAN_POINT('Ctrl Pts',(0.963542676605009,50.3918331087534,0.678880669996738));
#45367=CARTESIAN_POINT('Ctrl Pts',(0.935768925027702,50.388661039321,0.716668578269015));
#45368=CARTESIAN_POINT('Ctrl Pts',(0.905917433478278,50.3854889698885,0.752601266422087));
#45369=CARTESIAN_POINT('Ctrl Pts',(0.896537441149297,50.3844922362113,0.763892103889202));
#45370=CARTESIAN_POINT('Ctrl Pts',(0.886952577258788,50.383495502534,0.77500003826868));
#45371=CARTESIAN_POINT('Ctrl Pts',(0.877170910770406,50.3824987688568,0.785917461186744));
#45372=CARTESIAN_POINT('Ctrl Pts',(0.845949491876466,50.3793173641646,0.820764021798068));
#45373=CARTESIAN_POINT('Ctrl Pts',(0.812579211245098,50.3761359594725,0.853824453538088));
#45374=CARTESIAN_POINT('Ctrl Pts',(0.77729203235371,50.3729545547803,0.884823235985267));
#45375=CARTESIAN_POINT('Ctrl Pts',(0.742060225007989,50.3697781422497,0.91577337610535));
#45376=CARTESIAN_POINT('Ctrl Pts',(0.704917888945249,50.366601729719,0.944667907808254));
#45377=CARTESIAN_POINT('Ctrl Pts',(0.666134917544255,50.3634253171883,0.971266870704601));
#45378=CARTESIAN_POINT('Ctrl Pts',(0.627393529067787,50.3602523103927,0.997837314314606));
#45379=CARTESIAN_POINT('Ctrl Pts',(0.587015445270432,50.357079303597,1.02211674971657));
#45380=CARTESIAN_POINT('Ctrl Pts',(0.545302794957308,50.3539062968013,1.04390608979532));
#45381=CARTESIAN_POINT('Ctrl Pts',(0.50361723764742,50.350735350922,1.06568127736501));
#45382=CARTESIAN_POINT('Ctrl Pts',(0.460599324617646,50.3475644050427,1.08496931928487));
#45383=CARTESIAN_POINT('Ctrl Pts',(0.41657690880579,50.3443934591633,1.10161642214966));
#45384=CARTESIAN_POINT('Ctrl Pts',(0.37254562580824,50.3412218745784,1.11826687814602));
#45385=CARTESIAN_POINT('Ctrl Pts',(0.327509953016673,50.3380502899934,1.13227512669869));
#45386=CARTESIAN_POINT('Ctrl Pts',(0.281816798700614,50.3348787054084,1.14353589994811));
#45387=CARTESIAN_POINT('Ctrl Pts',(0.251117692865634,50.3327478651918,1.15110148991322));
#45388=CARTESIAN_POINT('Ctrl Pts',(0.220122192528981,50.3306170249752,1.15742792212166));
#45389=CARTESIAN_POINT('Ctrl Pts',(0.188938462403167,50.3284861847587,1.16249615910106));
#45390=CARTESIAN_POINT('Ctrl Pts',(-1.17774978721175,50.691380992042,0.000707970817746733));
#45391=CARTESIAN_POINT('Ctrl Pts',(-1.17773238358118,50.6934819144442,0.0296599017206249));
#45392=CARTESIAN_POINT('Ctrl Pts',(-1.17664741682129,50.6955591604751,0.0586042188794689));
#45393=CARTESIAN_POINT('Ctrl Pts',(-1.1739257268983,50.698130269672,0.0951446063022735));
#45394=CARTESIAN_POINT('Ctrl Pts',(-1.17327996126533,50.6986661946033,0.102801986002212));
#45395=CARTESIAN_POINT('Ctrl Pts',(-1.17202848744619,50.6995904147902,0.116087553336253));
#45396=CARTESIAN_POINT('Ctrl Pts',(-1.17145707416217,50.6999803896171,0.12171861854001));
#45397=CARTESIAN_POINT('Ctrl Pts',(-1.17023866037199,50.7007524192947,0.132921008251392));
#45398=CARTESIAN_POINT('Ctrl Pts',(-1.16959242134995,50.7011344733746,0.138492200352297));
#45399=CARTESIAN_POINT('Ctrl Pts',(-1.16808315669741,50.7019700059919,0.150738501743828));
#45400=CARTESIAN_POINT('Ctrl Pts',(-1.16720268496718,50.702422528339,0.157411100701953));
#45401=CARTESIAN_POINT('Ctrl Pts',(-1.16450344391011,50.7037167966332,0.176597518482482));
#45402=CARTESIAN_POINT('Ctrl Pts',(-1.16254022414858,50.7045510528989,0.189090489738766));
#45403=CARTESIAN_POINT('Ctrl Pts',(-1.14950230027356,50.7095255542255,0.264153218678005));
#45404=CARTESIAN_POINT('Ctrl Pts',(-1.133578717653,50.7134535287098,0.325781684112863));
#45405=CARTESIAN_POINT('Ctrl Pts',(-1.09503857902437,50.7207210221512,0.436933749774168));
#45406=CARTESIAN_POINT('Ctrl Pts',(-1.0738205461786,50.724052439107,0.486754164192088));
#45407=CARTESIAN_POINT('Ctrl Pts',(-1.03345953983596,50.7296679961069,0.565920369249477));
#45408=CARTESIAN_POINT('Ctrl Pts',(-1.01630061051121,50.7318977295043,0.596185549189738));
#45409=CARTESIAN_POINT('Ctrl Pts',(-0.990473830412874,50.7350808551219,
0.63737615676897));
#45410=CARTESIAN_POINT('Ctrl Pts',(-0.982912528188526,50.7359944587146,
0.648975892553797));
#45411=CARTESIAN_POINT('Ctrl Pts',(-0.969440003326239,50.7375930205735,
0.668868283703132));
#45412=CARTESIAN_POINT('Ctrl Pts',(-0.963622373339021,50.7382744151777,
0.67722271922699));
#45413=CARTESIAN_POINT('Ctrl Pts',(-0.951362601468362,50.739692920204,0.694350571444581));
#45414=CARTESIAN_POINT('Ctrl Pts',(-0.944905698764399,50.7404305561586,
0.703112168914322));
#45415=CARTESIAN_POINT('Ctrl Pts',(-0.927711725110049,50.7423712660027,
0.725778628177384));
#45416=CARTESIAN_POINT('Ctrl Pts',(-0.916783690469505,50.7435817405991,
0.739534494595114));
#45417=CARTESIAN_POINT('Ctrl Pts',(-0.845546143506708,50.7513350208662,
0.825199703958517));
#45418=CARTESIAN_POINT('Ctrl Pts',(-0.777139465905238,50.7582175682842,
0.889916106344646));
#45419=CARTESIAN_POINT('Ctrl Pts',(-0.671889906922505,50.7678408159439,
0.968011391517464));
#45420=CARTESIAN_POINT('Ctrl Pts',(-0.640943566762677,50.7705658364262,
0.988773861796829));
#45421=CARTESIAN_POINT('Ctrl Pts',(-0.590284600738896,50.7748152149674,
1.01938243874763));
#45422=CARTESIAN_POINT('Ctrl Pts',(-0.571190515499763,50.776371848158,1.03020289540381));
#45423=CARTESIAN_POINT('Ctrl Pts',(-0.544565636007778,50.7784707791179,
1.04432296651246));
#45424=CARTESIAN_POINT('Ctrl Pts',(-0.537287262139458,50.7790373879785,
1.04808615958777));
#45425=CARTESIAN_POINT('Ctrl Pts',(-0.524833065677163,50.7799940463966,
1.05436160922498));
#45426=CARTESIAN_POINT('Ctrl Pts',(-0.519677133943699,50.7803863690419,
1.05691240518364));
#45427=CARTESIAN_POINT('Ctrl Pts',(-0.508637859378323,50.7812182307483,
1.0622735499892));
#45428=CARTESIAN_POINT('Ctrl Pts',(-0.502749585441482,50.7816571254264,
1.0650729676542));
#45429=CARTESIAN_POINT('Ctrl Pts',(-0.486267054232453,50.7828731539292,
1.07274197997591));
#45430=CARTESIAN_POINT('Ctrl Pts',(-0.475622965746376,50.7836441257516,
1.07750351432911));
#45431=CARTESIAN_POINT('Ctrl Pts',(-0.39482868279484,50.789401960397,1.11221546494007));
#45432=CARTESIAN_POINT('Ctrl Pts',(-0.321978978616777,50.7940703672457,
1.13544951884604));
#45433=CARTESIAN_POINT('Ctrl Pts',(-0.200486535163913,50.8017483197142,
1.16155122599014));
#45434=CARTESIAN_POINT('Ctrl Pts',(-0.153018001884107,50.8047211660809,
1.16875196966845));
#45435=CARTESIAN_POINT('Ctrl Pts',(-0.0742224313004178,50.809742454362,
1.17582152210263));
#45436=CARTESIAN_POINT('Ctrl Pts',(-0.0431037979658147,50.8117469367186,
1.17737293426376));
#45437=CARTESIAN_POINT('Ctrl Pts',(0.00136815300788591,50.8146631670213,
1.17782465011632));
#45438=CARTESIAN_POINT('Ctrl Pts',(0.0146993375790103,50.8155438987066,
1.17773370662409));
#45439=CARTESIAN_POINT('Ctrl Pts',(0.0381269527773765,50.8171046190051,
1.17717606656907));
#45440=CARTESIAN_POINT('Ctrl Pts',(0.0482244427663947,50.8177815359742,
1.17680565448047));
#45441=CARTESIAN_POINT('Ctrl Pts',(0.0693956119694622,50.8192102927326,
1.17575608812076));
#45442=CARTESIAN_POINT('Ctrl Pts',(0.0804669115761797,50.8199629029164,
1.17505029301462));
#45443=CARTESIAN_POINT('Ctrl Pts',(0.110079462898091,50.8219912839454,1.17274203767767));
#45444=CARTESIAN_POINT('Ctrl Pts',(0.128594790068155,50.8232757438431,1.17085638999268));
#45445=CARTESIAN_POINT('Ctrl Pts',(0.161058491999941,50.8255576316109,1.16677091894303));
#45446=CARTESIAN_POINT('Ctrl Pts',(0.175021311207389,50.826548840862,1.16475809067173));
#45447=CARTESIAN_POINT('Ctrl Pts',(0.188938575466302,50.827546579051,1.16249614072511));
#45448=CARTESIAN_POINT('',(-1.17774953461646,50.7893671294558,-0.00104700082271912));
#45449=CARTESIAN_POINT('Ctrl Pts',(0.18893846240316,50.927164359664,1.16249615910107));
#45450=CARTESIAN_POINT('Ctrl Pts',(0.142784164703441,50.9239918824189,1.16999753617867));
#45451=CARTESIAN_POINT('Ctrl Pts',(0.0960912008263255,50.9208194051738,
1.17476079817481));
#45452=CARTESIAN_POINT('Ctrl Pts',(0.0492132149086467,50.9176469279288,
1.17672134423506));
#45453=CARTESIAN_POINT('Ctrl Pts',(0.0023935893101753,50.9144784002301,
1.17867944953144));
#45454=CARTESIAN_POINT('Ctrl Pts',(-0.0446100484742123,50.9113098725315,
1.17784171922707));
#45455=CARTESIAN_POINT('Ctrl Pts',(-0.0914375188926661,50.9081413448329,
1.17419514674468));
#45456=CARTESIAN_POINT('Ctrl Pts',(-0.138227383916993,50.9049753616607,
1.17055150268857));
#45457=CARTESIAN_POINT('Ctrl Pts',(-0.184840806630934,50.9018093784884,
1.16410352514596));
#45458=CARTESIAN_POINT('Ctrl Pts',(-0.230918938622777,50.8986433953162,
1.15489025724756));
#45459=CARTESIAN_POINT('Ctrl Pts',(-0.276980426257284,50.8954785557614,
1.14568031736868));
#45460=CARTESIAN_POINT('Ctrl Pts',(-0.322506459461986,50.8923137162066,
1.13370717669309));
#45461=CARTESIAN_POINT('Ctrl Pts',(-0.367147365638656,50.8891488766518,
1.11906115758014));
#45462=CARTESIAN_POINT('Ctrl Pts',(-0.411826012401549,50.8859813614591,
1.10440275634068));
#45463=CARTESIAN_POINT('Ctrl Pts',(-0.455617503926761,50.8828138462664,
1.08706713215073));
#45464=CARTESIAN_POINT('Ctrl Pts',(-0.498188217486216,50.8796463310737,
1.06719424776275));
#45465=CARTESIAN_POINT('Ctrl Pts',(-0.540775509334069,50.8764775823574,
1.04731362428889));
#45466=CARTESIAN_POINT('Ctrl Pts',(-0.5821405815923,50.8733088336411,1.02489403398469));
#45467=CARTESIAN_POINT('Ctrl Pts',(-0.621974046690846,50.8701400849247,
1.00012166647014));
#45468=CARTESIAN_POINT('Ctrl Pts',(-0.661887316002142,50.8669649877902,
0.975299668844766));
#45469=CARTESIAN_POINT('Ctrl Pts',(-0.700262388733832,50.8637898906556,
0.948115798200907));
#45470=CARTESIAN_POINT('Ctrl Pts',(-0.736819797934553,50.8606147935211,
0.91879902474463));
#45471=CARTESIAN_POINT('Ctrl Pts',(-0.767892938235702,50.8579160180638,
0.893880294596601));
#45472=CARTESIAN_POINT('Ctrl Pts',(-0.797653289032728,50.8552172426065,
0.867421451720827));
#45473=CARTESIAN_POINT('Ctrl Pts',(-0.825950597196265,50.8525184671493,
0.839583631028579));
#45474=CARTESIAN_POINT('Ctrl Pts',(-0.858767565167755,50.8493886419648,
0.807299540090532));
#45475=CARTESIAN_POINT('Ctrl Pts',(-0.88977284264808,50.8462588167803,0.77300549370469));
#45476=CARTESIAN_POINT('Ctrl Pts',(-0.918705936922051,50.8431289915958,
0.736935861499613));
#45477=CARTESIAN_POINT('Ctrl Pts',(-0.94759557596985,50.840003867162,0.700920403037952));
#45478=CARTESIAN_POINT('Ctrl Pts',(-0.974418826007374,50.8368787427281,
0.663135074061715));
#45479=CARTESIAN_POINT('Ctrl Pts',(-0.998951946545905,50.8337536182943,
0.623851000634083));
#45480=CARTESIAN_POINT('Ctrl Pts',(-1.0234597983108,50.8306317126952,0.584607389256827));
#45481=CARTESIAN_POINT('Ctrl Pts',(-1.04568188243562,50.8275098070962,0.543868572739639));
#45482=CARTESIAN_POINT('Ctrl Pts',(-1.06543653331898,50.8243879014971,0.501936306685644));
#45483=CARTESIAN_POINT('Ctrl Pts',(-1.08518858364019,50.8212664068752,0.460009560722331));
#45484=CARTESIAN_POINT('Ctrl Pts',(-1.10247357640349,50.8181449122533,0.416890186179884));
#45485=CARTESIAN_POINT('Ctrl Pts',(-1.11715603410307,50.8150234176313,0.372904086820056));
#45486=CARTESIAN_POINT('Ctrl Pts',(-1.13183652688546,50.8119023407513,0.328923874011706));
#45487=CARTESIAN_POINT('Ctrl Pts',(-1.14391500222188,50.8087812638714,0.284077716200727));
#45488=CARTESIAN_POINT('Ctrl Pts',(-1.15330554738567,50.8056601869914,0.238707722684957));
#45489=CARTESIAN_POINT('Ctrl Pts',(-1.16270689885228,50.802535518488,0.193285519006744));
#45490=CARTESIAN_POINT('Ctrl Pts',(-1.16941404099522,50.7994108499846,0.147338843973864));
#45491=CARTESIAN_POINT('Ctrl Pts',(-1.17339242612076,50.7962861814812,0.101218954857428));
#45492=CARTESIAN_POINT('Ctrl Pts',(-1.17632891401069,50.7939798308061,0.0671773797958268));
#45493=CARTESIAN_POINT('Ctrl Pts',(-1.17777983888489,50.7916734801309,0.0330416429229676));
#45494=CARTESIAN_POINT('Ctrl Pts',(-1.17774953461646,50.7893671294558,-0.00104700082271912));
#45495=CARTESIAN_POINT('Ctrl Pts',(-1.17810120469558,50.7893671147362,-0.00104753107751893));
#45496=CARTESIAN_POINT('Ctrl Pts',(-1.1788378426409,50.7839593348025,-0.0810009332839553));
#45497=CARTESIAN_POINT('Ctrl Pts',(-1.13496814489393,50.7520933241307,-0.551332790626785));
#45498=CARTESIAN_POINT('Ctrl Pts',(-0.502684486253736,50.6937690827209,
-1.29806349587743));
#45499=CARTESIAN_POINT('Ctrl Pts',(0.817803162580305,50.6143943905067,-1.12642683757311));
#45500=CARTESIAN_POINT('Ctrl Pts',(1.38993487805217,50.5350196982925,0.0760013926731982));
#45501=CARTESIAN_POINT('Ctrl Pts',(0.839567365761362,50.4725996990519,0.966914061782009));
#45502=CARTESIAN_POINT('Ctrl Pts',(0.328078249322183,50.4366379305494,1.13955181241402));
#45503=CARTESIAN_POINT('Ctrl Pts',(0.18873835403253,50.4271343927849,1.16119835837062));
#45504=CARTESIAN_POINT('Origin',(0.,55.715,0.));
#45505=CARTESIAN_POINT('',(-1.46349970539298,55.454344954121,0.000928608990242965));
#45506=CARTESIAN_POINT('',(-1.46357455043502,55.5256550458429,0.0014857082342598));
#45507=CARTESIAN_POINT('',(-1.4635,55.715,-1.79227059055215E-16));
#45508=CARTESIAN_POINT('',(0.634286466388226,55.6149831334283,1.31890595895111));
#45509=CARTESIAN_POINT('Ctrl Pts',(-1.46349970539256,55.4543449541571,0.000928609651264057));
#45510=CARTESIAN_POINT('Ctrl Pts',(-1.4634682143009,55.4570563262928,0.0505589395830078));
#45511=CARTESIAN_POINT('Ctrl Pts',(-1.46091230617661,55.4597676984285,0.10011308468285));
#45512=CARTESIAN_POINT('Ctrl Pts',(-1.45585397646145,55.4624790705642,0.149403645274732));
#45513=CARTESIAN_POINT('Ctrl Pts',(-1.45023131890728,55.4654929344045,0.204193261307642));
#45514=CARTESIAN_POINT('Ctrl Pts',(-1.44149964314002,55.4685067982449,0.258779993253343));
#45515=CARTESIAN_POINT('Ctrl Pts',(-1.42968466713854,55.4715206620852,0.312784274778906));
#45516=CARTESIAN_POINT('Ctrl Pts',(-1.41789104075309,55.4745290798852,0.366690970776174));
#45517=CARTESIAN_POINT('Ctrl Pts',(-1.40302528350236,55.4775374976852,0.420016794785235));
#45518=CARTESIAN_POINT('Ctrl Pts',(-1.38516471160696,55.4805459154852,0.472388581274784));
#45519=CARTESIAN_POINT('Ctrl Pts',(-1.36732216386837,55.4835512973133,0.524707516304846));
#45520=CARTESIAN_POINT('Ctrl Pts',(-1.34649095805777,55.4865566791415,0.576073825096052));
#45521=CARTESIAN_POINT('Ctrl Pts',(-1.32279872936154,55.4895620609696,0.626127600094015));
#45522=CARTESIAN_POINT('Ctrl Pts',(-1.29912110990318,55.492565589602,0.676150510646314));
#45523=CARTESIAN_POINT('Ctrl Pts',(-1.27258618939207,55.4955691182343,0.724862016522588));
#45524=CARTESIAN_POINT('Ctrl Pts',(-1.24336956297523,55.4985726468667,0.771922521932601));
#45525=CARTESIAN_POINT('Ctrl Pts',(-1.21415948458859,55.5015755023482,0.818972480142311));
#45526=CARTESIAN_POINT('Ctrl Pts',(-1.1822691713679,55.5045783578297,0.864371725312425));
#45527=CARTESIAN_POINT('Ctrl Pts',(-1.14791881148039,55.5075812133113,0.907807607508025));
#45528=CARTESIAN_POINT('Ctrl Pts',(-1.11353807289256,55.5105867244519,0.951281903439411));
#45529=CARTESIAN_POINT('Ctrl Pts',(-1.07669326758234,55.5135922355926,0.992788952558395));
#45530=CARTESIAN_POINT('Ctrl Pts',(-1.03764544852851,55.5165977467332,1.03204853236079));
#45531=CARTESIAN_POINT('Ctrl Pts',(-0.998580863004207,55.5196045483894,
1.07132496956014));
#45532=CARTESIAN_POINT('Ctrl Pts',(-0.957311769947083,55.5226113500455,
1.10835166023693));
#45533=CARTESIAN_POINT('Ctrl Pts',(-0.914134350043771,55.5256181517016,
1.14288697606984));
#45534=CARTESIAN_POINT('Ctrl Pts',(-0.870876293319733,55.528630568768,1.17748678899584));
#45535=CARTESIAN_POINT('Ctrl Pts',(-0.825703219598404,55.5316429858343,
1.20958562469138));
#45536=CARTESIAN_POINT('Ctrl Pts',(-0.778941555092246,55.5346554029007,
1.23898438398168));
#45537=CARTESIAN_POINT('Ctrl Pts',(-0.74169490982564,55.5370548561933,1.26240111155391));
#45538=CARTESIAN_POINT('Ctrl Pts',(-0.703441039287024,55.5394543094858,
1.28410560897184));
#45539=CARTESIAN_POINT('Ctrl Pts',(-0.664354874088175,55.5418537627784,
1.30401873118268));
#45540=CARTESIAN_POINT('Ctrl Pts',(-0.614719493413587,55.5449008198888,
1.32930633349225));
#45541=CARTESIAN_POINT('Ctrl Pts',(-0.563520193639003,55.5479478769992,
1.35181588548473));
#45542=CARTESIAN_POINT('Ctrl Pts',(-0.511105263984488,55.5509949341097,
1.37135103424592));
#45543=CARTESIAN_POINT('Ctrl Pts',(-0.459990530233786,55.5539664064354,
1.39040159740206));
#45544=CARTESIAN_POINT('Ctrl Pts',(-0.407720314823116,55.5569378787611,
1.40662340207885));
#45545=CARTESIAN_POINT('Ctrl Pts',(-0.354642567370892,55.5599093510868,
1.4198805933629));
#45546=CARTESIAN_POINT('Ctrl Pts',(-0.301615480101468,55.5628779872836,
1.43312513128907));
#45547=CARTESIAN_POINT('Ctrl Pts',(-0.24778290885404,55.5658466234804,1.44341052655117));
#45548=CARTESIAN_POINT('Ctrl Pts',(-0.193509041103219,55.5688152596773,
1.45065037173377));
#45549=CARTESIAN_POINT('Ctrl Pts',(-0.139264365231086,55.571782299156,1.45788632287506));
#45550=CARTESIAN_POINT('Ctrl Pts',(-0.0845793984116932,55.5747493386348,
1.46207989783114));
#45551=CARTESIAN_POINT('Ctrl Pts',(-0.0298271696790935,55.5777163781135,
1.46319601897659));
#45552=CARTESIAN_POINT('Ctrl Pts',(0.0274813001988054,55.5808219410564,
1.46436424895598));
#45553=CARTESIAN_POINT('Ctrl Pts',(0.0848628353463616,55.5839275039993,
1.46216048954602));
#45554=CARTESIAN_POINT('Ctrl Pts',(0.141888195121509,55.5870330669422,1.45660563986453));
#45555=CARTESIAN_POINT('Ctrl Pts',(0.196413795785491,55.5900024946763,1.4512942921295));
#45556=CARTESIAN_POINT('Ctrl Pts',(0.25061324320126,55.5929719224103,1.44291969991955));
#45557=CARTESIAN_POINT('Ctrl Pts',(0.30411845769905,55.5959413501444,1.43155307749547));
#45558=CARTESIAN_POINT('Ctrl Pts',(0.357654942063916,55.5989125132908,1.42017981211564));
#45559=CARTESIAN_POINT('Ctrl Pts',(0.410495865403998,55.6018836764372,1.40581118259737));
#45560=CARTESIAN_POINT('Ctrl Pts',(0.462287531165772,55.6048548395837,1.38856850336188));
#45561=CARTESIAN_POINT('Ctrl Pts',(0.514162411669356,55.6078307765594,1.37129811995663));
#45562=CARTESIAN_POINT('Ctrl Pts',(0.56498417446405,55.6108067135352,1.35114468492091));
#45563=CARTESIAN_POINT('Ctrl Pts',(0.61442003466674,55.613782650511,1.3282771815401));
#45564=CARTESIAN_POINT('Ctrl Pts',(0.621067454303904,55.6141828114834,1.32520229034972));
#45565=CARTESIAN_POINT('Ctrl Pts',(0.627689855127081,55.6145829724558,1.32207839229904));
#45566=CARTESIAN_POINT('Ctrl Pts',(0.634286466388226,55.6149831334283,1.31890595895111));
#45567=CARTESIAN_POINT('',(-0.634007094575041,55.615,1.31904027763693));
#45568=CARTESIAN_POINT('Origin',(0.,55.615,0.));
#45569=CARTESIAN_POINT('Ctrl Pts',(-0.63400709457504,55.615,1.31904027763693));
#45570=CARTESIAN_POINT('Ctrl Pts',(-1.07256679420512,55.588541769262,1.10824310512125));
#45571=CARTESIAN_POINT('Ctrl Pts',(-1.43427071524654,55.5587601178763,0.607354686391449));
#45572=CARTESIAN_POINT('Ctrl Pts',(-1.46522723293725,55.5289784664906,0.062380321776885));
#45573=CARTESIAN_POINT('Ctrl Pts',(-1.46474336208885,55.5256550458429,0.0014868947218889));
#45574=CARTESIAN_POINT('Origin',(0.,55.715,0.));
#45575=CARTESIAN_POINT('',(-1.4634496027614,54.9543449877359,0.000746977488451873));
#45576=CARTESIAN_POINT('',(-1.4634998802993,55.0256550458709,0.000591915479193347));
#45577=CARTESIAN_POINT('',(-1.4635,55.715,-1.79227059055215E-16));
#45578=CARTESIAN_POINT('Ctrl Pts',(-1.46349980934833,54.954344988597,0.000747019002576732));
#45579=CARTESIAN_POINT('Ctrl Pts',(-1.4634685843509,54.9576560770049,0.0619205335156351));
#45580=CARTESIAN_POINT('Ctrl Pts',(-1.45959766985196,54.9609671654128,0.122961773930032));
#45581=CARTESIAN_POINT('Ctrl Pts',(-1.45196136132378,54.9642782538206,0.183413345269103));
#45582=CARTESIAN_POINT('Ctrl Pts',(-1.44429538136574,54.9676022077024,0.244099805566855));
#45583=CARTESIAN_POINT('Ctrl Pts',(-1.43283483841439,54.9709261615841,0.304191696763971));
#45584=CARTESIAN_POINT('Ctrl Pts',(-1.41770468045198,54.9742501154658,0.36324329178188));
#45585=CARTESIAN_POINT('Ctrl Pts',(-1.40250127100869,54.9775901620112,0.422580780495997));
#45586=CARTESIAN_POINT('Ctrl Pts',(-1.38359278817325,54.9809302085567,0.480867578854932));
#45587=CARTESIAN_POINT('Ctrl Pts',(-1.36115385057846,54.9842702551021,0.537673176804868));
#45588=CARTESIAN_POINT('Ctrl Pts',(-1.3567631756147,54.9849238091611,0.548788449783657));
#45589=CARTESIAN_POINT('Ctrl Pts',(-1.35223746983837,54.9855773632201,0.559847085362521));
#45590=CARTESIAN_POINT('Ctrl Pts',(-1.34757824592688,54.9862309172791,0.570845969684141));
#45591=CARTESIAN_POINT('Ctrl Pts',(-1.32613120233688,54.9892393158146,0.621475335425864));
#45592=CARTESIAN_POINT('Ctrl Pts',(-1.30178119111294,54.9922477143501,0.671002303954884));
#45593=CARTESIAN_POINT('Ctrl Pts',(-1.274663492119,54.9952561128856,0.71907248025425));
#45594=CARTESIAN_POINT('Ctrl Pts',(-1.24759452264009,54.9982591054388,0.767056276201849));
#45595=CARTESIAN_POINT('Ctrl Pts',(-1.2177679924346,55.001262097992,0.813588017926406));
#45596=CARTESIAN_POINT('Ctrl Pts',(-1.18536665257206,55.0042650905452,0.858334520434843));
#45597=CARTESIAN_POINT('Ctrl Pts',(-1.15299776236589,55.0072650756278,0.903036209715288));
#45598=CARTESIAN_POINT('Ctrl Pts',(-1.11805947891956,55.0102650607104,0.945955775088201));
#45599=CARTESIAN_POINT('Ctrl Pts',(-1.08077877794127,55.013265045793,0.986787455915294));
#45600=CARTESIAN_POINT('Ctrl Pts',(-1.04352063769655,55.0162632154091,1.02759442710312));
#45601=CARTESIAN_POINT('Ctrl Pts',(-1.00392324518647,55.0192613850252,1.06631562812772));
#45602=CARTESIAN_POINT('Ctrl Pts',(-0.962253460080595,55.0222595546413,
1.10267879664158));
#45603=CARTESIAN_POINT('Ctrl Pts',(-0.920592377607056,55.025257098097,1.13903437079696));
#45604=CARTESIAN_POINT('Ctrl Pts',(-0.876860160158432,55.0282546415527,
1.17303254274021));
#45605=CARTESIAN_POINT('Ctrl Pts',(-0.831358363940373,55.0312521850084,
1.20443991992394));
#45606=CARTESIAN_POINT('Ctrl Pts',(-0.785814511376617,55.0342524990301,
1.23587632628063));
#45607=CARTESIAN_POINT('Ctrl Pts',(-0.738498248211412,55.0372528130516,
1.26471685212984));
#45608=CARTESIAN_POINT('Ctrl Pts',(-0.689740646933369,55.0402531270732,
1.29077112222421));
#45609=CARTESIAN_POINT('Ctrl Pts',(-0.640961171813114,55.0432547871085,
1.3168370808959));
#45610=CARTESIAN_POINT('Ctrl Pts',(-0.590739550243402,55.0462564471437,
1.34011406912444));
#45611=CARTESIAN_POINT('Ctrl Pts',(-0.539429025217443,55.0492581071789,
1.36045895812882));
#45612=CARTESIAN_POINT('Ctrl Pts',(-0.488019840116207,55.0522655388176,
1.38084296636419));
#45613=CARTESIAN_POINT('Ctrl Pts',(-0.435518071857954,55.0552729704563,
1.39828344465212));
#45614=CARTESIAN_POINT('Ctrl Pts',(-0.382293312057844,55.058280402095,1.41268682784113));
#45615=CARTESIAN_POINT('Ctrl Pts',(-0.33908009326065,55.0607221378945,1.42438094447978));
#45616=CARTESIAN_POINT('Ctrl Pts',(-0.295390679312955,55.0631638736939,
1.43407400534725));
#45617=CARTESIAN_POINT('Ctrl Pts',(-0.251426222477321,55.0656056094934,
1.44174099776998));
#45618=CARTESIAN_POINT('Ctrl Pts',(-0.197257943091071,55.0686140539618,
1.45118744195465));
#45619=CARTESIAN_POINT('Ctrl Pts',(-0.142441105338817,55.0716224984301,
1.45759699901049));
#45620=CARTESIAN_POINT('Ctrl Pts',(-0.0873468318633905,55.0746309428985,
1.4608910914108));
#45621=CARTESIAN_POINT('Ctrl Pts',(-0.0323515139282667,55.0776339838607,
1.46417926724895));
#45622=CARTESIAN_POINT('Ctrl Pts',(0.022919727367197,55.0806370248228,1.46436305137819));
#45623=CARTESIAN_POINT('Ctrl Pts',(0.0780878397517109,55.083640065785,1.46141525217267));
#45624=CARTESIAN_POINT('Ctrl Pts',(0.133200729689996,55.0866401007486,1.45847040366958));
#45625=CARTESIAN_POINT('Ctrl Pts',(0.188210169783137,55.0896401357122,1.45240020909698));
#45626=CARTESIAN_POINT('Ctrl Pts',(0.242736159893193,55.0926401706758,1.44322950589305));
#45627=CARTESIAN_POINT('Ctrl Pts',(0.297229178550358,55.0956383915409,1.43406434814384));
#45628=CARTESIAN_POINT('Ctrl Pts',(0.351238806173742,55.0986366124061,1.42180248507628));
#45629=CARTESIAN_POINT('Ctrl Pts',(0.404391551688584,55.1016348332713,1.40652043103643));
#45630=CARTESIAN_POINT('Ctrl Pts',(0.457533219018479,55.1046324292422,1.39124156210808));
#45631=CARTESIAN_POINT('Ctrl Pts',(0.509817850889621,55.1076300252131,1.37294389811306));
#45632=CARTESIAN_POINT('Ctrl Pts',(0.560885791387536,55.1106276211841,1.35175418587093));
#45633=CARTESIAN_POINT('Ctrl Pts',(0.612000957901915,55.113627989237,1.33054487805299));
#45634=CARTESIAN_POINT('Ctrl Pts',(0.661896695340679,55.1166283572898,1.30643838128853));
#45635=CARTESIAN_POINT('Ctrl Pts',(0.710233476738354,55.1196287253427,1.2796095726901));
#45636=CARTESIAN_POINT('Ctrl Pts',(0.7585919576928,55.1226304403338,1.252768719987));
#45637=CARTESIAN_POINT('Ctrl Pts',(0.805389639508389,55.1256321553249,1.22320340211702));
#45638=CARTESIAN_POINT('Ctrl Pts',(0.850314661533951,55.128633870316,1.1911327492687));
#45639=CARTESIAN_POINT('Ctrl Pts',(0.895326075978649,55.131641357712,1.15900042341148));
#45640=CARTESIAN_POINT('Ctrl Pts',(0.938457222594922,55.134648845108,1.12435346937979));
#45641=CARTESIAN_POINT('Ctrl Pts',(0.979429011371886,55.1376563325041,1.08745163648003));
#45642=CARTESIAN_POINT('Ctrl Pts',(1.01268779516711,55.1400976555719,1.05749663283736));
#45643=CARTESIAN_POINT('Ctrl Pts',(1.04452428496812,55.1425389786397,1.02605664842551));
#45644=CARTESIAN_POINT('Ctrl Pts',(1.07480842371899,55.1449803017075,0.993287019095031));
#45645=CARTESIAN_POINT('Ctrl Pts',(1.11212006042545,55.147988138917,0.952913128503586));
#45646=CARTESIAN_POINT('Ctrl Pts',(1.14723335600289,55.1509959761264,0.910347695448135));
#45647=CARTESIAN_POINT('Ctrl Pts',(1.17988101179648,55.1540038133358,0.865859716121563));
#45648=CARTESIAN_POINT('Ctrl Pts',(1.21246999821183,55.1570062453198,0.82145168379342));
#45649=CARTESIAN_POINT('Ctrl Pts',(1.24260182698818,55.1600086773038,0.775128384058019));
#45650=CARTESIAN_POINT('Ctrl Pts',(1.27004805762475,55.1630111092878,0.727193358965556));
#45651=CARTESIAN_POINT('Ctrl Pts',(1.29746680377979,55.1660105346554,0.679306335703612));
#45652=CARTESIAN_POINT('Ctrl Pts',(1.32220501722386,55.169009960023,0.629811240817045));
#45653=CARTESIAN_POINT('Ctrl Pts',(1.34407744651238,55.1720093853906,0.579040644321941));
#45654=CARTESIAN_POINT('Ctrl Pts',(1.36593665021578,55.175006997098,0.528300747244649));
#45655=CARTESIAN_POINT('Ctrl Pts',(1.38493329515023,55.1780046088054,0.476287361988805));
#45656=CARTESIAN_POINT('Ctrl Pts',(1.40092907082036,55.1810022205128,0.423355628910736));
#45657=CARTESIAN_POINT('Ctrl Pts',(1.41692151991189,55.1839992088186,0.370434903837164));
#45658=CARTESIAN_POINT('Ctrl Pts',(1.42991418591346,55.1869961971245,0.316596716318655));
#45659=CARTESIAN_POINT('Ctrl Pts',(1.43981846179572,55.1899931854303,0.262211836254961));
#45660=CARTESIAN_POINT('Ctrl Pts',(1.44973192234837,55.1929929529752,0.207776522701447));
#45661=CARTESIAN_POINT('Ctrl Pts',(1.45655117529059,55.19599272052,0.152794025308403));
#45662=CARTESIAN_POINT('Ctrl Pts',(1.46023896601188,55.1989924880649,0.0976443144302231));
#45663=CARTESIAN_POINT('Ctrl Pts',(1.46392841627738,55.2019936055363,0.0424697856080811));
#45664=CARTESIAN_POINT('Ctrl Pts',(1.46448358984535,55.2049947230078,-0.0128715766705545));
#45665=CARTESIAN_POINT('Ctrl Pts',(1.46191941648469,55.2079958404792,-0.0679990419421796));
#45666=CARTESIAN_POINT('Ctrl Pts',(1.45935030043546,55.2110027428907,-0.123232770658072));
#45667=CARTESIAN_POINT('Ctrl Pts',(1.45364987951497,55.2140096453022,-0.178251250939895));
#45668=CARTESIAN_POINT('Ctrl Pts',(1.4448849835864,55.2170165477137,-0.232679251774885));
#45669=CARTESIAN_POINT('Ctrl Pts',(1.43775464273627,55.2194626964497,-0.276957039087768));
#45670=CARTESIAN_POINT('Ctrl Pts',(1.4285972490309,55.2219088451857,-0.320844079201327));
#45671=CARTESIAN_POINT('Ctrl Pts',(1.41747316725082,55.2243549939217,-0.364145671571044));
#45672=CARTESIAN_POINT('Ctrl Pts',(1.4037896749191,55.2273639485602,-0.417410023528928));
#45673=CARTESIAN_POINT('Ctrl Pts',(1.38707060222972,55.2303729031987,-0.47001542865737));
#45674=CARTESIAN_POINT('Ctrl Pts',(1.36739710706093,55.2333818578372,-0.521591220786352));
#45675=CARTESIAN_POINT('Ctrl Pts',(1.34775899147727,55.2363854013596,-0.573074262231615));
#45676=CARTESIAN_POINT('Ctrl Pts',(1.32517718370166,55.239388944882,-0.623530875210123));
#45677=CARTESIAN_POINT('Ctrl Pts',(1.29978293645842,55.2423924884044,-0.672604317627782));
#45678=CARTESIAN_POINT('Ctrl Pts',(1.27441414639096,55.2453930209403,-0.721628564995936));
#45679=CARTESIAN_POINT('Ctrl Pts',(1.24623874338507,55.2483935534762,-0.769271921294565));
#45680=CARTESIAN_POINT('Ctrl Pts',(1.21543578882913,55.2513940860121,-0.815198192609205));
#45681=CARTESIAN_POINT('Ctrl Pts',(1.18465151691794,55.2543927986614,-0.86109660866696));
#45682=CARTESIAN_POINT('Ctrl Pts',(1.15124314584916,55.2573915113108,-0.905279565680527));
#45683=CARTESIAN_POINT('Ctrl Pts',(1.11543415722865,55.2603902239601,-0.947438067045866));
#45684=CARTESIAN_POINT('Ctrl Pts',(1.07963270949874,55.2633883051209,-0.98958769039876));
#45685=CARTESIAN_POINT('Ctrl Pts',(1.04143199003147,55.2663863862818,-1.02971330190103));
#45686=CARTESIAN_POINT('Ctrl Pts',(1.00109557116825,55.2693844674426,-1.06753918306886));
#45687=CARTESIAN_POINT('Ctrl Pts',(0.960722044703797,55.2723853066966,-1.10539986226174));
#45688=CARTESIAN_POINT('Ctrl Pts',(0.918209279542544,55.2753861459506,-1.14095622140911));
#45689=CARTESIAN_POINT('Ctrl Pts',(0.87385643315756,55.2783869852046,-1.17397069138422));
#45690=CARTESIAN_POINT('Ctrl Pts',(0.829483781968685,55.2813891644184,-1.20699990325657));
#45691=CARTESIAN_POINT('Ctrl Pts',(0.783269853607096,55.2843913436322,-1.2374846714938));
#45692=CARTESIAN_POINT('Ctrl Pts',(0.735542760091726,55.287393522846,-1.26523084774149));
#45693=CARTESIAN_POINT('Ctrl Pts',(0.687724175251795,55.2904014571422,-1.29303021252905));
#45694=CARTESIAN_POINT('Ctrl Pts',(0.638387102763967,55.2934093914384,-1.31808025697743));
#45695=CARTESIAN_POINT('Ctrl Pts',(0.587883196447786,55.2964173257345,-1.34023341151246));
#45696=CARTESIAN_POINT('Ctrl Pts',(0.546957794017624,55.2988547792016,-1.35818502814124));
#45697=CARTESIAN_POINT('Ctrl Pts',(0.505266710682442,55.3012922326688,-1.37423527324438));
#45698=CARTESIAN_POINT('Ctrl Pts',(0.463004067676604,55.3037296861359,-1.38832974588709));
#45699=CARTESIAN_POINT('Ctrl Pts',(0.410832891124243,55.3067386038497,-1.40572868661481));
#45700=CARTESIAN_POINT('Ctrl Pts',(0.357568794285465,55.3097475215634,-1.42021973131096));
#45701=CARTESIAN_POINT('Ctrl Pts',(0.303567241783893,55.3127564392772,-1.43167006664096));
#45702=CARTESIAN_POINT('Ctrl Pts',(0.24966245862682,55.3157599650906,-1.44309988327486));
#45703=CARTESIAN_POINT('Ctrl Pts',(0.195023355111327,55.3187634909039,-1.45149969473198));
#45704=CARTESIAN_POINT('Ctrl Pts',(0.140020861134086,55.3217670167173,-1.45678632902951));
#45705=CARTESIAN_POINT('Ctrl Pts',(0.0850732919769199,55.3247675432463,
-1.46206768415846));
#45706=CARTESIAN_POINT('Ctrl Pts',(0.0297635747249087,55.3277680697754,
-1.46424196981431));
#45707=CARTESIAN_POINT('Ctrl Pts',(-0.0255287033080896,55.3307685963045,
-1.46327732686166));
#45708=CARTESIAN_POINT('Ctrl Pts',(-0.0807876585500475,55.3337673145174,
-1.46231326526678));
#45709=CARTESIAN_POINT('Ctrl Pts',(-0.136028667932132,55.3367660327303,
-1.45821403354496));
#45710=CARTESIAN_POINT('Ctrl Pts',(-0.190870910656135,55.3397647509433,
-1.45099984337191));
#45711=CARTESIAN_POINT('Ctrl Pts',(-0.245701813826826,55.3427628491209,
-1.44378714485364));
#45712=CARTESIAN_POINT('Ctrl Pts',(-0.300133590235123,55.3457609472986,
-1.43346083566842));
#45713=CARTESIAN_POINT('Ctrl Pts',(-0.35379164221338,55.3487590454763,-1.42009285749206));
#45714=CARTESIAN_POINT('Ctrl Pts',(-0.407499367981711,55.3517599191348,
-1.40671250394766));
#45715=CARTESIAN_POINT('Ctrl Pts',(-0.460431424062973,55.3547607927934,
-1.39028498329125));
#45716=CARTESIAN_POINT('Ctrl Pts',(-0.512225969490007,55.357761666452,-1.37093282336518));
#45717=CARTESIAN_POINT('Ctrl Pts',(-0.564043809213344,55.3607638897361,
-1.35157195991746));
#45718=CARTESIAN_POINT('Ctrl Pts',(-0.614722633606314,55.3637661130202,
-1.32928404823263));
#45719=CARTESIAN_POINT('Ctrl Pts',(-0.663921385527143,55.3667683363043,
-1.30423948868286));
#45720=CARTESIAN_POINT('Ctrl Pts',(-0.713214697242056,55.3697763298489,
-1.27914679359506));
#45721=CARTESIAN_POINT('Ctrl Pts',(-0.761021795231998,55.3727843233935,
-1.25128713242896));
#45722=CARTESIAN_POINT('Ctrl Pts',(-0.807027992491674,55.3757923169381,
-1.22087594346635));
#45723=CARTESIAN_POINT('Ctrl Pts',(-0.844306456768326,55.3782296707421,
-1.1962339932753));
#45724=CARTESIAN_POINT('Ctrl Pts',(-0.88040295285426,55.3806670245461,-1.16991769516912));
#45725=CARTESIAN_POINT('Ctrl Pts',(-0.915166532093658,55.3831043783501,
-1.14206062384432));
#45726=CARTESIAN_POINT('Ctrl Pts',(-0.957503727813097,55.3860727356739,
-1.10813459244442));
#45727=CARTESIAN_POINT('Ctrl Pts',(-0.998054495391826,55.3890410929977,
-1.07176862385729));
#45728=CARTESIAN_POINT('Ctrl Pts',(-1.03651833694835,55.3920094503214,-1.03318052012696));
#45729=CARTESIAN_POINT('Ctrl Pts',(-1.07489554527512,55.3949711219276,-0.994679329505699));
#45730=CARTESIAN_POINT('Ctrl Pts',(-1.11119478090176,55.3979327935338,-0.953966326324882));
#45731=CARTESIAN_POINT('Ctrl Pts',(-1.14514877261919,55.40089446514,-0.91129936824776));
#45732=CARTESIAN_POINT('Ctrl Pts',(-1.17906926620127,55.4038532148372,-0.868674504294599));
#45733=CARTESIAN_POINT('Ctrl Pts',(-1.21064875745915,55.4068119645343,-0.824099924521325));
#45734=CARTESIAN_POINT('Ctrl Pts',(-1.23965810540703,55.4097707142314,-0.777868903928321));
#45735=CARTESIAN_POINT('Ctrl Pts',(-1.26865107833675,55.4127277937918,-0.731663979537253));
#45736=CARTESIAN_POINT('Ctrl Pts',(-1.29507649266034,55.4156848733521,-0.683804926928464));
#45737=CARTESIAN_POINT('Ctrl Pts',(-1.31874816875926,55.4186419529124,-0.634614463587228));
#45738=CARTESIAN_POINT('Ctrl Pts',(-1.34256530159622,55.4216172030131,-0.585121736717594));
#45739=CARTESIAN_POINT('Ctrl Pts',(-1.36359445535666,55.4245924531138,-0.534281661715596));
#45740=CARTESIAN_POINT('Ctrl Pts',(-1.38169379472098,55.4275677032145,-0.482446377983639));
#45741=CARTESIAN_POINT('Ctrl Pts',(-1.39969521979474,55.4305268577276,-0.430891514157128));
#45742=CARTESIAN_POINT('Ctrl Pts',(-1.41479833346101,55.4334860122407,-0.378352722285895));
#45743=CARTESIAN_POINT('Ctrl Pts',(-1.42691362714353,55.4364451667538,-0.325191867475339));
#45744=CARTESIAN_POINT('Ctrl Pts',(-1.4391277680324,55.4394284646483,-0.271597279721673));
#45745=CARTESIAN_POINT('Ctrl Pts',(-1.44830499876274,55.4424117625429,-0.217370983158963));
#45746=CARTESIAN_POINT('Ctrl Pts',(-1.45440663779413,55.4453950604374,-0.16289131941386));
#45747=CARTESIAN_POINT('Ctrl Pts',(-1.46050827682551,55.4483783583319,-0.108411655668757));
#45748=CARTESIAN_POINT('Ctrl Pts',(-1.46353435472766,55.4513616562265,-0.0536791878676936));
#45749=CARTESIAN_POINT('Ctrl Pts',(-1.46349970539298,55.454344954121,0.000928608990243761));
#45750=CARTESIAN_POINT('Ctrl Pts',(-1.46349924595067,55.5256550458429,0.00148563179094337));
#45751=CARTESIAN_POINT('Ctrl Pts',(-1.46355384318984,55.5227171263939,-0.0522982323151164));
#45752=CARTESIAN_POINT('Ctrl Pts',(-1.46063941780497,55.5197792069449,-0.10621577743416));
#45753=CARTESIAN_POINT('Ctrl Pts',(-1.45473831007084,55.5168412874958,-0.159902155120703));
#45754=CARTESIAN_POINT('Ctrl Pts',(-1.44884470734304,55.5139071044816,-0.21352025467661));
#45755=CARTESIAN_POINT('Ctrl Pts',(-1.43997199045938,55.5109729214673,-0.266907222341851));
#45756=CARTESIAN_POINT('Ctrl Pts',(-1.42815449504172,55.5080387384531,-0.319698276961466));
#45757=CARTESIAN_POINT('Ctrl Pts',(-1.41634689186904,55.5051070115986,-0.372445140995297));
#45758=CARTESIAN_POINT('Ctrl Pts',(-1.4015995059739,55.5021752847442,-0.42459654015682));
#45759=CARTESIAN_POINT('Ctrl Pts',(-1.38399813666318,55.4992435578897,-0.475795552430716));
#45760=CARTESIAN_POINT('Ctrl Pts',(-1.3664038572382,55.4963130119439,-0.526973941584838));
#45761=CARTESIAN_POINT('Ctrl Pts',(-1.34595805090473,55.493382465998,-0.577200180277564));
#45762=CARTESIAN_POINT('Ctrl Pts',(-1.32279625441777,55.4904519200522,-0.626132828797794));
#45763=CARTESIAN_POINT('Ctrl Pts',(-1.29961665952346,55.4875191221631,-0.675103079030449));
#45764=CARTESIAN_POINT('Ctrl Pts',(-1.27371713703299,55.484586324274,-0.722777248762854));
#45765=CARTESIAN_POINT('Ctrl Pts',(-1.24528050137009,55.4816535263849,-0.768835953183423));
#45766=CARTESIAN_POINT('Ctrl Pts',(-1.21683417100642,55.4787197286379,-0.814910360071822));
#45767=CARTESIAN_POINT('Ctrl Pts',(-1.18584932148862,55.4757859308908,-0.859367748945078));
#45768=CARTESIAN_POINT('Ctrl Pts',(-1.15255169799166,55.4728521331437,-0.901918418404091));
#45769=CARTESIAN_POINT('Ctrl Pts',(-1.11918966051721,55.4699126599891,-0.944551401781544));
#45770=CARTESIAN_POINT('Ctrl Pts',(-1.0835062805902,55.4669731868346,-0.985269882275895));
#45771=CARTESIAN_POINT('Ctrl Pts',(-1.04576617187633,55.46403371368,-1.02381900927807));
#45772=CARTESIAN_POINT('Ctrl Pts',(-1.01245691844994,55.4614393476439,-1.057842298676));
#45773=CARTESIAN_POINT('Ctrl Pts',(-0.977546272076871,55.4588449816078,
-1.09017610936883));
#45774=CARTESIAN_POINT('Ctrl Pts',(-0.941236463326947,55.4562506155717,
-1.12067219565035));
#45775=CARTESIAN_POINT('Ctrl Pts',(-0.89908941689693,55.4532391740482,-1.15607089392754));
#45776=CARTESIAN_POINT('Ctrl Pts',(-0.85485358911812,55.4502277325247,-1.18916344235199));
#45777=CARTESIAN_POINT('Ctrl Pts',(-0.808811171130817,55.4472162910012,
-1.21969534698383));
#45778=CARTESIAN_POINT('Ctrl Pts',(-0.762851855995484,55.4442102848868,
-1.25017214398965));
#45779=CARTESIAN_POINT('Ctrl Pts',(-0.715092857972174,55.4412042787724,
-1.27809718026094));
#45780=CARTESIAN_POINT('Ctrl Pts',(-0.66584898706299,55.4381982726581,-1.30325645075219));
#45781=CARTESIAN_POINT('Ctrl Pts',(-0.61665471834428,55.4351952944228,-1.32839037890328));
#45782=CARTESIAN_POINT('Ctrl Pts',(-0.565979007125824,55.4321923161875,
-1.35076382126136));
#45783=CARTESIAN_POINT('Ctrl Pts',(-0.514163582315877,55.4291893379523,
-1.37020730570965));
#45784=CARTESIAN_POINT('Ctrl Pts',(-0.46237993191135,55.4261882012121,-1.38963886696789));
#45785=CARTESIAN_POINT('Ctrl Pts',(-0.409458446126396,55.4231870644718,
-1.40614384656038));
#45786=CARTESIAN_POINT('Ctrl Pts',(-0.355761160543727,55.4201859277316,
-1.41960073494225));
#45787=CARTESIAN_POINT('Ctrl Pts',(-0.302075645105117,55.4171854488238,
-1.43305467364961));
#45788=CARTESIAN_POINT('Ctrl Pts',(-0.247615178994482,55.4141849699159,
-1.4434617195614));
#45789=CARTESIAN_POINT('Ctrl Pts',(-0.192755059142475,55.411184491008,-1.45075074950006));
#45790=CARTESIAN_POINT('Ctrl Pts',(-0.137845635759255,55.4081813155292,
-1.45804633018844));
#45791=CARTESIAN_POINT('Ctrl Pts',(-0.0825363650716257,55.4051781400504,
-1.46221822581618));
#45792=CARTESIAN_POINT('Ctrl Pts',(-0.0272093101413858,55.4021749645716,
-1.46324704115253));
#45793=CARTESIAN_POINT('Ctrl Pts',(0.0281418707602797,55.399170479525,-1.46427630511513));
#45794=CARTESIAN_POINT('Ctrl Pts',(0.0835103231341836,55.3961659944785,
-1.46215977587118));
#45795=CARTESIAN_POINT('Ctrl Pts',(0.138515650026584,55.3931615094319,-1.45693021957049));
#45796=CARTESIAN_POINT('Ctrl Pts',(0.193624860538797,55.3901513500844,-1.45169078667658));
#45797=CARTESIAN_POINT('Ctrl Pts',(0.248369052342751,55.3871411907368,-1.44332666007825));
#45798=CARTESIAN_POINT('Ctrl Pts',(0.302375736754545,55.3841310313892,-1.43192219195812));
#45799=CARTESIAN_POINT('Ctrl Pts',(0.345764838415967,55.3817126620453,-1.42275981452192));
#45800=CARTESIAN_POINT('Ctrl Pts',(0.38867800768965,55.3792942927014,-1.41163606378852));
#45801=CARTESIAN_POINT('Ctrl Pts',(0.430930136872908,55.3768759233575,-1.39861769870637));
#45802=CARTESIAN_POINT('Ctrl Pts',(0.483576999531882,55.3738625945343,-1.38239659714835));
#45803=CARTESIAN_POINT('Ctrl Pts',(0.535414735736252,55.3708492657111,-1.36316547803516));
#45804=CARTESIAN_POINT('Ctrl Pts',(0.586076255091749,55.3678359368879,-1.34102456100462));
#45805=CARTESIAN_POINT('Ctrl Pts',(0.636649562556188,55.3648278548761,-1.31892219576221));
#45806=CARTESIAN_POINT('Ctrl Pts',(0.686050238750951,55.3618197728643,-1.29392029700104));
#45807=CARTESIAN_POINT('Ctrl Pts',(0.733927662556537,55.3588116908524,-1.26616840749337));
#45808=CARTESIAN_POINT('Ctrl Pts',(0.781758704685495,55.3558065229466,-1.23844340287345));
#45809=CARTESIAN_POINT('Ctrl Pts',(0.828068964271635,55.3528013550407,-1.2079739483108));
#45810=CARTESIAN_POINT('Ctrl Pts',(0.872530785051554,55.3497961871349,-1.17495628818153));
#45811=CARTESIAN_POINT('Ctrl Pts',(0.916966985596722,55.3467927508969,-1.14195765381838));
#45812=CARTESIAN_POINT('Ctrl Pts',(0.959556436513209,55.3437893146589,-1.10641403797563));
#45813=CARTESIAN_POINT('Ctrl Pts',(1.00000089248573,55.340785878421,-1.06856467517308));
#45814=CARTESIAN_POINT('Ctrl Pts',(1.04043791773393,55.3377829939943,-1.03072226630707));
#45815=CARTESIAN_POINT('Ctrl Pts',(1.07873034637521,55.3347801095676,-0.990575311700769));
#45816=CARTESIAN_POINT('Ctrl Pts',(1.11461517874458,55.3317772251409,-0.948401419923113));
#45817=CARTESIAN_POINT('Ctrl Pts',(1.15053398718889,55.3287714975568,-0.906187597533764));
#45818=CARTESIAN_POINT('Ctrl Pts',(1.18404030302639,55.3257657699727,-0.861943405947744));
#45819=CARTESIAN_POINT('Ctrl Pts',(1.21491099080409,55.3227600423887,-0.815980106634614));
#45820=CARTESIAN_POINT('Ctrl Pts',(1.24579600263332,55.3197529201419,-0.769995480272567));
#45821=CARTESIAN_POINT('Ctrl Pts',(1.27404267968776,55.3167457978951,-0.722290610220477));
#45822=CARTESIAN_POINT('Ctrl Pts',(1.29947267887532,55.3137386756483,-0.673203540436759));
#45823=CARTESIAN_POINT('Ctrl Pts',(1.32495157941273,55.3107257707691,-0.624022077257494));
#45824=CARTESIAN_POINT('Ctrl Pts',(1.34760276506019,55.3077128658899,-0.573453586299472));
#45825=CARTESIAN_POINT('Ctrl Pts',(1.36729556336216,55.3046999610108,-0.521857348717217));
#45826=CARTESIAN_POINT('Ctrl Pts',(1.38297955616363,55.3023003843883,-0.48076440669777));
#45827=CARTESIAN_POINT('Ctrl Pts',(1.39678796259989,55.2999008077658,-0.439020032257649));
#45828=CARTESIAN_POINT('Ctrl Pts',(1.40867778461437,55.2975012311433,-0.396811226068455));
#45829=CARTESIAN_POINT('Ctrl Pts',(1.42356683378495,55.2944963573717,-0.343955179105175));
#45830=CARTESIAN_POINT('Ctrl Pts',(1.43550931560213,55.2914914836001,-0.290144737559877));
#45831=CARTESIAN_POINT('Ctrl Pts',(1.44438875528196,55.2884866098284,-0.235740055177355));
#45832=CARTESIAN_POINT('Ctrl Pts',(1.45325200784476,55.2854872139073,-0.181434551908938));
#45833=CARTESIAN_POINT('Ctrl Pts',(1.45906321348545,55.2824878179862,-0.126537476220011));
#45834=CARTESIAN_POINT('Ctrl Pts',(1.46175617560072,55.2794884220651,-0.0714222170836544));
#45835=CARTESIAN_POINT('Ctrl Pts',(1.46444640034116,55.2764920750065,-0.0163629821753025));
#45836=CARTESIAN_POINT('Ctrl Pts',(1.4640246336337,55.2734957279477,0.0389134700365081));
#45837=CARTESIAN_POINT('Ctrl Pts',(1.46047632558275,55.270499380889,0.0940274024543575));
#45838=CARTESIAN_POINT('Ctrl Pts',(1.45693020887449,55.2675048842963,0.149107297942038));
#45839=CARTESIAN_POINT('Ctrl Pts',(1.45026141118792,55.2645103877036,0.204024344470546));
#45840=CARTESIAN_POINT('Ctrl Pts',(1.44050745448951,55.2615158911108,0.258399929489455));
#45841=CARTESIAN_POINT('Ctrl Pts',(1.43075563074694,55.2585220493425,0.312763623875092));
#45842=CARTESIAN_POINT('Ctrl Pts',(1.41792008089446,55.2555282075742,0.366585570154613));
#45843=CARTESIAN_POINT('Ctrl Pts',(1.40208971802482,55.2525343658058,0.419495736103585));
#45844=CARTESIAN_POINT('Ctrl Pts',(1.386244785755,55.2495377686693,0.472454597675473));
#45845=CARTESIAN_POINT('Ctrl Pts',(1.36739968532074,55.2465411715327,0.524499492965711));
#45846=CARTESIAN_POINT('Ctrl Pts',(1.34569327485495,55.2435445743962,0.575275464460424));
#45847=CARTESIAN_POINT('Ctrl Pts',(1.32397721920763,55.2405466457302,0.626073998113151));
#45848=CARTESIAN_POINT('Ctrl Pts',(1.29939755524102,55.2375487170643,0.675602008087615));
#45849=CARTESIAN_POINT('Ctrl Pts',(1.27213999548243,55.2345507883984,0.723527526700929));
#45850=CARTESIAN_POINT('Ctrl Pts',(1.2448297464843,55.2315470646949,0.771545686003748));
#45851=CARTESIAN_POINT('Ctrl Pts',(1.21483154885192,55.2285433409915,0.817954718840988));
#45852=CARTESIAN_POINT('Ctrl Pts',(1.18237487347815,55.225539617288,0.862451105030028));
#45853=CARTESIAN_POINT('Ctrl Pts',(1.15567425100956,55.2230685911684,0.899056246966732));
#45854=CARTESIAN_POINT('Ctrl Pts',(1.12731071301053,55.2205975650487,0.934367454944674));
#45855=CARTESIAN_POINT('Ctrl Pts',(1.09743113615349,55.218126538929,0.968234037514105));
#45856=CARTESIAN_POINT('Ctrl Pts',(1.06104696853818,55.2151175863943,1.0094731562158));
#45857=CARTESIAN_POINT('Ctrl Pts',(1.02225765640098,55.2121086338597,1.0487462821852));
#45858=CARTESIAN_POINT('Ctrl Pts',(0.981303895793412,55.209099681325,1.0857600628595));
#45859=CARTESIAN_POINT('Ctrl Pts',(0.940423693769962,55.2060961332827,1.12270736169529));
#45860=CARTESIAN_POINT('Ctrl Pts',(0.897387147029046,55.2030925852404,1.15740301676308));
#45861=CARTESIAN_POINT('Ctrl Pts',(0.852473253623644,55.2000890371981,1.18958883731158));
#45862=CARTESIAN_POINT('Ctrl Pts',(0.807604325458639,55.1970884961376,1.22174243524368));
#45863=CARTESIAN_POINT('Ctrl Pts',(0.76086220113353,55.1940879550772,1.25139086956008));
#45864=CARTESIAN_POINT('Ctrl Pts',(0.712559134285563,55.1910874140167,1.2783159742983));
#45865=CARTESIAN_POINT('Ctrl Pts',(0.664285301521891,55.18808868895,1.30522478336768));
#45866=CARTESIAN_POINT('Ctrl Pts',(0.614452859391236,55.1850899638833,1.32941327266492));
#45867=CARTESIAN_POINT('Ctrl Pts',(0.563401278014001,55.1820912388166,1.35070768485716));
#45868=CARTESIAN_POINT('Ctrl Pts',(0.512360382915796,55.1790931414526,1.37199763963546));
#45869=CARTESIAN_POINT('Ctrl Pts',(0.460101342890859,55.1760950440886,1.39039451677633));
#45870=CARTESIAN_POINT('Ctrl Pts',(0.406984225354113,55.1730969467245,1.40577241768108));
#45871=CARTESIAN_POINT('Ctrl Pts',(0.353818145098614,55.1700960857505,1.42116449374955));
#45872=CARTESIAN_POINT('Ctrl Pts',(0.2997929158096,55.1670952247765,1.43353188582999));
#45873=CARTESIAN_POINT('Ctrl Pts',(0.24528297634443,55.1640943638024,1.44279884651867));
#45874=CARTESIAN_POINT('Ctrl Pts',(0.190748640841548,55.1610921597867,1.45206995465505));
#45875=CARTESIAN_POINT('Ctrl Pts',(0.135729689007291,55.1580899557711,1.4582378060625));
#45876=CARTESIAN_POINT('Ctrl Pts',(0.0806066288835818,55.1550877517554,
1.46127848864617));
#45877=CARTESIAN_POINT('Ctrl Pts',(0.0253778166797984,55.1520797880936,
1.46432500469604));
#45878=CARTESIAN_POINT('Ctrl Pts',(-0.02995497274921,55.1490718244318,1.46423236689615));
#45879=CARTESIAN_POINT('Ctrl Pts',(-0.0850114179338464,55.14606386077,1.46102885283655));
#45880=CARTESIAN_POINT('Ctrl Pts',(-0.12962338207046,55.1436265227517,1.4584330613019));
#45881=CARTESIAN_POINT('Ctrl Pts',(-0.174053837648228,55.1411891847333,
1.45379575896721));
#45882=CARTESIAN_POINT('Ctrl Pts',(-0.218105165681863,55.138751846715,1.44715665589558));
#45883=CARTESIAN_POINT('Ctrl Pts',(-0.27248642703196,55.1357429586362,1.43896069869328));
#45884=CARTESIAN_POINT('Ctrl Pts',(-0.326520527592842,55.1327340705574,
1.42767776515773));
#45885=CARTESIAN_POINT('Ctrl Pts',(-0.379830470494731,55.1297251824786,
1.41335100512355));
#45886=CARTESIAN_POINT('Ctrl Pts',(-0.433044981610845,55.1267216807039,
1.39904989186781));
#45887=CARTESIAN_POINT('Ctrl Pts',(-0.485537401230335,55.1237181789292,
1.38171590105493));
#45888=CARTESIAN_POINT('Ctrl Pts',(-0.536939504491591,55.1207146771545,
1.3614434319928));
#45889=CARTESIAN_POINT('Ctrl Pts',(-0.588290337110829,55.1177141712001,
1.34119118355274));
#45890=CARTESIAN_POINT('Ctrl Pts',(-0.638552518272102,55.1147136652457,
1.31800645561976));
#45891=CARTESIAN_POINT('Ctrl Pts',(-0.687373420401407,55.1117131592913,
1.29203329327292));
#45892=CARTESIAN_POINT('Ctrl Pts',(-0.736164957429819,55.1087144580999,
1.26607575342586));
#45893=CARTESIAN_POINT('Ctrl Pts',(-0.783516467821157,55.1057157569085,
1.23733335106368));
#45894=CARTESIAN_POINT('Ctrl Pts',(-0.829097879551163,55.1027170557172,
1.20599707964977));
#45895=CARTESIAN_POINT('Ctrl Pts',(-0.874669921934138,55.0997189709146,
1.17466724946683));
#45896=CARTESIAN_POINT('Ctrl Pts',(-0.91847215273347,55.096720886112,1.14074490824729));
#45897=CARTESIAN_POINT('Ctrl Pts',(-0.960203543664407,55.0937228013095,
1.10446430668189));
#45898=CARTESIAN_POINT('Ctrl Pts',(-1.00197365063869,55.090721935052,1.06815004600973));
#45899=CARTESIAN_POINT('Ctrl Pts',(-1.0416686792142,55.0877210687946,1.02947350114224));
#45900=CARTESIAN_POINT('Ctrl Pts',(-1.07902194531063,55.0847202025371,0.988708193319984));
#45901=CARTESIAN_POINT('Ctrl Pts',(-1.11639205187186,55.0817179833596,0.947924506737228));
#45902=CARTESIAN_POINT('Ctrl Pts',(-1.15141795619799,55.0787157641822,0.905050590072751));
#45903=CARTESIAN_POINT('Ctrl Pts',(-1.18387323762103,55.0757135450047,0.860393170152288));
#45904=CARTESIAN_POINT('Ctrl Pts',(-1.21639095955814,55.0727055498764,0.815649834099376));
#45905=CARTESIAN_POINT('Ctrl Pts',(-1.24632789125963,55.0696975547481,0.76911658548395));
#45906=CARTESIAN_POINT('Ctrl Pts',(-1.27350156397274,55.0666895596198,0.721128294105139));
#45907=CARTESIAN_POINT('Ctrl Pts',(-1.29552120329789,55.0642520912468,0.682241947046049));
#45908=CARTESIAN_POINT('Ctrl Pts',(-1.31572721393398,55.0618146228737,0.64240077918245));
#45909=CARTESIAN_POINT('Ctrl Pts',(-1.33404579483354,55.0593771545007,0.601792378887404));
#45910=CARTESIAN_POINT('Ctrl Pts',(-1.35874262868613,55.0560909964867,0.547044747473952));
#45911=CARTESIAN_POINT('Ctrl Pts',(-1.38009909771906,55.0528048384726,0.490700317698954));
#45912=CARTESIAN_POINT('Ctrl Pts',(-1.39792695643952,55.0495186804585,0.43316564321254));
#45913=CARTESIAN_POINT('Ctrl Pts',(-1.41570101042178,55.0462424401174,0.375804609214719));
#45914=CARTESIAN_POINT('Ctrl Pts',(-1.42996753253458,55.0429661997763,0.317260822737725));
#45915=CARTESIAN_POINT('Ctrl Pts',(-1.44058626795848,55.0396899594351,0.257960180201249));
#45916=CARTESIAN_POINT('Ctrl Pts',(-1.45115547624072,55.0364289998984,0.19893612345452));
#45917=CARTESIAN_POINT('Ctrl Pts',(-1.45811070118538,55.0331680403617,0.139162595522109));
#45918=CARTESIAN_POINT('Ctrl Pts',(-1.46136203782201,55.0299070808251,0.0790774583095327));
#45919=CARTESIAN_POINT('Ctrl Pts',(-1.46277520030494,55.0284897358403,0.0529620260488936));
#45920=CARTESIAN_POINT('Ctrl Pts',(-1.4634892852701,55.0270723908556,0.0267879257304701));
#45921=CARTESIAN_POINT('Ctrl Pts',(-1.4634998802993,55.0256550458709,0.000591915479186377));
#45922=CARTESIAN_POINT('Origin',(0.,55.715,0.));
#45923=CARTESIAN_POINT('',(-1.46349946245349,54.4543449264189,-0.00125435176163375));
#45924=CARTESIAN_POINT('',(-1.46349941614739,54.5256550458061,-0.00130726288314624));
#45925=CARTESIAN_POINT('',(-1.4635,55.715,-1.79227059055215E-16));
#45926=CARTESIAN_POINT('Ctrl Pts',(-1.46258057639989,54.4543449541571,-0.00125305338302531));
#45927=CARTESIAN_POINT('Ctrl Pts',(-1.45979356777586,54.4728908907694,0.340279369314991));
#45928=CARTESIAN_POINT('Ctrl Pts',(-1.17029252859884,54.51789505812,1.17331067980076));
#45929=CARTESIAN_POINT('Ctrl Pts',(0.217062202804517,54.5893574562082,1.71605622949271));
#45930=CARTESIAN_POINT('Ctrl Pts',(1.55938868398063,54.6687321484225,0.748514022091191));
#45931=CARTESIAN_POINT('Ctrl Pts',(1.47470200890391,54.7481068406366,-0.904002308136149));
#45932=CARTESIAN_POINT('Ctrl Pts',(0.0405007560907972,54.8274815328507,
-1.72925446836193));
#45933=CARTESIAN_POINT('Ctrl Pts',(-1.23375485783567,54.896227570691,-1.07344525015692));
#45934=CARTESIAN_POINT('Ctrl Pts',(-1.46014652428568,54.9385153777931,-0.291311080189099));
#45935=CARTESIAN_POINT('Ctrl Pts',(-1.46149175089378,54.9543449541571,0.000745358607108643));
#45936=CARTESIAN_POINT('Ctrl Pts',(-1.46349988029951,55.0256550458429,0.000591914962299759));
#45937=CARTESIAN_POINT('Ctrl Pts',(-1.46352273945175,55.0225970709691,-0.0559269580044757));
#45938=CARTESIAN_POINT('Ctrl Pts',(-1.46026720689571,55.0195390960954,-0.112428152305842));
#45939=CARTESIAN_POINT('Ctrl Pts',(-1.45376562565274,55.0164811212216,-0.168516336509234));
#45940=CARTESIAN_POINT('Ctrl Pts',(-1.4472533939806,55.0134181369904,-0.224696400397169));
#45941=CARTESIAN_POINT('Ctrl Pts',(-1.43748455285694,55.0103551527591,-0.280461606436067));
#45942=CARTESIAN_POINT('Ctrl Pts',(-1.42454317052395,55.0072921685278,-0.335423620685192));
#45943=CARTESIAN_POINT('Ctrl Pts',(-1.41159150289028,55.0042267499574,-0.390429316577325));
#45944=CARTESIAN_POINT('Ctrl Pts',(-1.39546241426794,55.001161331387,-0.44463007058759));
#45945=CARTESIAN_POINT('Ctrl Pts',(-1.37628990407881,54.9980959128166,-0.497652840774301));
#45946=CARTESIAN_POINT('Ctrl Pts',(-1.35707046383798,54.9950229907815,-0.550805398939841));
#45947=CARTESIAN_POINT('Ctrl Pts',(-1.33479290857018,54.9919500687465,-0.602773749554788));
#45948=CARTESIAN_POINT('Ctrl Pts',(-1.30963927072332,54.9888771467114,-0.653205351003256));
#45949=CARTESIAN_POINT('Ctrl Pts',(-1.28542446849519,54.9859189185698,-0.701754640873667));
#45950=CARTESIAN_POINT('Ctrl Pts',(-1.25854478280758,54.9829606904283,-0.748879575681883));
#45951=CARTESIAN_POINT('Ctrl Pts',(-1.22920027887007,54.9800024622867,-0.794291460627482));
#45952=CARTESIAN_POINT('Ctrl Pts',(-1.19935762844891,54.9769940158504,-0.84047424873267));
#45953=CARTESIAN_POINT('Ctrl Pts',(-1.16684502167947,54.9739855694142,-0.885071281384762));
#45954=CARTESIAN_POINT('Ctrl Pts',(-1.1318567431638,54.9709771229779,-0.927756736949206));
#45955=CARTESIAN_POINT('Ctrl Pts',(-1.09693131524253,54.9679740807128,-0.970365515227181));
#45956=CARTESIAN_POINT('Ctrl Pts',(-1.05953937299723,54.9649710384477,-1.01106912495695));
#45957=CARTESIAN_POINT('Ctrl Pts',(-1.01991831143784,54.9619679961826,-1.04957081132898));
#45958=CARTESIAN_POINT('Ctrl Pts',(-0.980336915308954,54.9589679603227,
-1.08803395289921));
#45959=CARTESIAN_POINT('Ctrl Pts',(-0.938531197625199,54.9559679244628,
-1.12429917090959));
#45960=CARTESIAN_POINT('Ctrl Pts',(-0.894777395778928,54.9529678886028,
-1.15810433986022));
#45961=CARTESIAN_POINT('Ctrl Pts',(-0.851050057434734,54.9499696672471,
-1.19188906251542));
#45962=CARTESIAN_POINT('Ctrl Pts',(-0.805377387735205,54.9469714458913,
-1.22321636233412));
#45963=CARTESIAN_POINT('Ctrl Pts',(-0.758069145018266,54.9439732245355,
-1.25186397878175));
#45964=CARTESIAN_POINT('Ctrl Pts',(-0.71077076876065,54.9409756284794,-1.28050562057198));
#45965=CARTESIAN_POINT('Ctrl Pts',(-0.661837948886245,54.9379780324233,
-1.30646841488371));
#45966=CARTESIAN_POINT('Ctrl Pts',(-0.611607930138179,54.9349804363673,
-1.32957436414519));
#45967=CARTESIAN_POINT('Ctrl Pts',(-0.561331470795344,54.931980068858,-1.3527016762103));
#45968=CARTESIAN_POINT('Ctrl Pts',(-0.509755897711565,54.9289797013488,
-1.37296664414412));
#45969=CARTESIAN_POINT('Ctrl Pts',(-0.457240125395904,54.9259793338395,
-1.39023872688396));
#45970=CARTESIAN_POINT('Ctrl Pts',(-0.404700783568403,54.9229776197406,
-1.40751856147702));
#45971=CARTESIAN_POINT('Ctrl Pts',(-0.351220913178297,54.9199759056417,
-1.42180269638156));
#45972=CARTESIAN_POINT('Ctrl Pts',(-0.297173134507942,54.9169741915427,
-1.43301094836248));
#45973=CARTESIAN_POINT('Ctrl Pts',(-0.243021430149966,54.9139667056025,
-1.44424075211338));
#45974=CARTESIAN_POINT('Ctrl Pts',(-0.188300160387169,54.9109592196622,
-1.45238277874376));
#45975=CARTESIAN_POINT('Ctrl Pts',(-0.133389517620246,54.907951733722,-1.45740848309218));
#45976=CARTESIAN_POINT('Ctrl Pts',(-0.088815903689603,54.9055104125054,
-1.46148808941379));
#45977=CARTESIAN_POINT('Ctrl Pts',(-0.044117724991045,54.9030690912889,
-1.46351523952389));
#45978=CARTESIAN_POINT('Ctrl Pts',(0.000502671042219297,54.9006277700723,
-1.46349991367332));
#45979=CARTESIAN_POINT('Ctrl Pts',(0.0554874744758696,54.8976193797588,
-1.46348102794044));
#45980=CARTESIAN_POINT('Ctrl Pts',(0.110588412878166,54.8946109894453,-1.46035905738128));
#45981=CARTESIAN_POINT('Ctrl Pts',(0.165426389183475,54.8916025991318,-1.45412047635735));
#45982=CARTESIAN_POINT('Ctrl Pts',(0.220165879294719,54.8885996117331,-1.4478930995051));
#45983=CARTESIAN_POINT('Ctrl Pts',(0.274642823368808,54.8855966243344,-1.43856027877067));
#45984=CARTESIAN_POINT('Ctrl Pts',(0.328479157627615,54.8825936369356,-1.4261604723888));
#45985=CARTESIAN_POINT('Ctrl Pts',(0.382261608791315,54.8795936551326,-1.41377307658347));
#45986=CARTESIAN_POINT('Ctrl Pts',(0.435404207407102,54.8765936733296,-1.39832489362432));
#45987=CARTESIAN_POINT('Ctrl Pts',(0.487536911658011,54.8735936915266,-1.37990579742639));
#45988=CARTESIAN_POINT('Ctrl Pts',(0.539638099813497,54.8705955233206,-1.36149783623483));
#45989=CARTESIAN_POINT('Ctrl Pts',(0.590730105965462,54.8675973551145,-1.34012269716246));
#45990=CARTESIAN_POINT('Ctrl Pts',(0.640458195559618,54.8645991869084,-1.3159200392655));
#45991=CARTESIAN_POINT('Ctrl Pts',(0.690175930519373,54.8616016429961,-1.29172242096841));
#45992=CARTESIAN_POINT('Ctrl Pts',(0.738529837567229,54.8586040990838,-1.26469868417835));
#45993=CARTESIAN_POINT('Ctrl Pts',(0.785187457789192,54.8556065551715,-1.23503558901375));
#45994=CARTESIAN_POINT('Ctrl Pts',(0.831888247611472,54.852606237805,-1.20534504830101));
#45995=CARTESIAN_POINT('Ctrl Pts',(0.876889167374615,54.8496059204385,-1.17301055417713));
#45996=CARTESIAN_POINT('Ctrl Pts',(0.919885871830842,54.846605603072,-1.13826281359184));
#45997=CARTESIAN_POINT('Ctrl Pts',(0.962901888589307,54.8436039380897,-1.10349946579021));
#45998=CARTESIAN_POINT('Ctrl Pts',(1.0039115029153,54.8406022731075,-1.06632106656798));
#45999=CARTESIAN_POINT('Ctrl Pts',(1.04264524109831,54.8376006081252,-1.02699715248634));
#46000=CARTESIAN_POINT('Ctrl Pts',(1.08145348983831,54.834593168959,-0.987597592549722));
#46001=CARTESIAN_POINT('Ctrl Pts',(1.11797676575785,54.8315857297928,-0.946044670508383));
#46002=CARTESIAN_POINT('Ctrl Pts',(1.1519848691766,54.8285782906266,-0.90264229414989));
#46003=CARTESIAN_POINT('Ctrl Pts',(1.17959602267748,54.8261365530371,-0.86740393753878));
#46004=CARTESIAN_POINT('Ctrl Pts',(1.20554994260307,54.8236948154477,-0.830947182786983));
#46005=CARTESIAN_POINT('Ctrl Pts',(1.22974520446427,54.8212530778583,-0.79344752951731));
#46006=CARTESIAN_POINT('Ctrl Pts',(1.25955426048327,54.8182448073545,-0.747247191971024));
#46007=CARTESIAN_POINT('Ctrl Pts',(1.28681973469681,54.8152365368508,-0.699266104732976));
#46008=CARTESIAN_POINT('Ctrl Pts',(1.31132461368342,54.8122282663471,-0.649815364198196));
#46009=CARTESIAN_POINT('Ctrl Pts',(1.33578545153028,54.8092254024263,-0.600453498494248));
#46010=CARTESIAN_POINT('Ctrl Pts',(1.35749530680087,54.8062225385056,-0.549627690924813));
#46011=CARTESIAN_POINT('Ctrl Pts',(1.37628139507752,54.8032196745848,-0.497676372317858));
#46012=CARTESIAN_POINT('Ctrl Pts',(1.39504866671308,54.8002198184117,-0.445777089520705));
#46013=CARTESIAN_POINT('Ctrl Pts',(1.41089779322862,54.7972199622386,-0.392755023596504));
#46014=CARTESIAN_POINT('Ctrl Pts',(1.42370353352889,54.7942201060654,-0.338969760623804));
#46015=CARTESIAN_POINT('Ctrl Pts',(1.43650152374846,54.7912220654162,-0.285217048688247));
#46016=CARTESIAN_POINT('Ctrl Pts',(1.44625965588852,54.788224024767,-0.230702568584233));
#46017=CARTESIAN_POINT('Ctrl Pts',(1.45290281510818,54.7852259841177,-0.175800056458286));
#46018=CARTESIAN_POINT('Ctrl Pts',(1.45954458721925,54.782228569467,-0.120909008116791));
#46019=CARTESIAN_POINT('Ctrl Pts',(1.46307261434322,54.7792311548163,-0.0656306134065736));
#46020=CARTESIAN_POINT('Ctrl Pts',(1.46346343367585,54.7762337401656,-0.0103454479689026));
#46021=CARTESIAN_POINT('Ctrl Pts',(1.46385461441479,54.7732335536855,0.0449908418770366));
#46022=CARTESIAN_POINT('Ctrl Pts',(1.46110278696083,54.7702333672053,0.100333384890216));
#46023=CARTESIAN_POINT('Ctrl Pts',(1.45523665797459,54.7672331807251,0.155301382115353));
#46024=CARTESIAN_POINT('Ctrl Pts',(1.44936789622432,54.7642316477381,0.210294049402625));
#46025=CARTESIAN_POINT('Ctrl Pts',(1.44038213257665,54.761230114751,0.264911312928163));
#46026=CARTESIAN_POINT('Ctrl Pts',(1.42835961035724,54.7582285817639,0.318780604021195));
#46027=CARTESIAN_POINT('Ctrl Pts',(1.41631396052695,54.7552212747566,0.372753522953688));
#46028=CARTESIAN_POINT('Ctrl Pts',(1.40122002588493,54.7522139677493,0.425975084581314));
#46029=CARTESIAN_POINT('Ctrl Pts',(1.38320822925877,54.749206660742,0.478087067918401));
#46030=CARTESIAN_POINT('Ctrl Pts',(1.36857770873395,54.746763902376,0.520416295681001));
#46031=CARTESIAN_POINT('Ctrl Pts',(1.35202301228425,54.74432114401,0.5620136445533));
#46032=CARTESIAN_POINT('Ctrl Pts',(1.33363668231757,54.741878385644,0.602698473182883));
#46033=CARTESIAN_POINT('Ctrl Pts',(1.31099320721888,54.7388700344215,0.652803410146271));
#46034=CARTESIAN_POINT('Ctrl Pts',(1.28547384292371,54.735861683199,0.701737332544859));
#46035=CARTESIAN_POINT('Ctrl Pts',(1.25722224614297,54.7328533319765,0.749149166590487));
#46036=CARTESIAN_POINT('Ctrl Pts',(1.22902140692497,54.7298503856371,0.796475819286555));
#46037=CARTESIAN_POINT('Ctrl Pts',(1.19809834478068,54.7268474392976,0.842285359687871));
#46038=CARTESIAN_POINT('Ctrl Pts',(1.16464367048006,54.7238444929581,0.886249045590872));
#46039=CARTESIAN_POINT('Ctrl Pts',(1.13122249344159,54.7208445533878,0.93016871184213));
#46040=CARTESIAN_POINT('Ctrl Pts',(1.09527504391662,54.7178446138174,0.972245765785033));
#46041=CARTESIAN_POINT('Ctrl Pts',(1.05703549326846,54.714844674247,1.01217993260621));
#46042=CARTESIAN_POINT('Ctrl Pts',(1.01881907412523,54.7118465493716,1.05208994283137));
#46043=CARTESIAN_POINT('Ctrl Pts',(0.978313666816864,54.7088484244961,1.08985925377929));
#46044=CARTESIAN_POINT('Ctrl Pts',(0.935792519379252,54.7058502996206,1.12522202727899));
#46045=CARTESIAN_POINT('Ctrl Pts',(0.893280240561043,54.7028528000629,1.16057742517859));
#46046=CARTESIAN_POINT('Ctrl Pts',(0.848753462785047,54.6998553005051,1.19352694426159));
#46047=CARTESIAN_POINT('Ctrl Pts',(0.802519196972512,54.6968578009474,1.22384442985642));
#46048=CARTESIAN_POINT('Ctrl Pts',(0.756242171850833,54.6938575291815,1.25418995428168));
#46049=CARTESIAN_POINT('Ctrl Pts',(0.708254946661054,54.6908572574156,1.28189829080232));
#46050=CARTESIAN_POINT('Ctrl Pts',(0.658893017884118,54.6878569856497,1.30678699143493));
#46051=CARTESIAN_POINT('Ctrl Pts',(0.609508930020067,54.6848553670303,1.33168686486608));
#46052=CARTESIAN_POINT('Ctrl Pts',(0.558749394219457,54.681853748411,1.35376436774521));
#46053=CARTESIAN_POINT('Ctrl Pts',(0.506970947798101,54.6788521297916,1.37288481238911));
#46054=CARTESIAN_POINT('Ctrl Pts',(0.455092907428903,54.6758447376686,1.39204203450895));
#46055=CARTESIAN_POINT('Ctrl Pts',(0.402192548117434,54.6728373455457,1.40823067989922));
#46056=CARTESIAN_POINT('Ctrl Pts',(0.348641572802339,54.6698299534227,1.42136599921129));
#46057=CARTESIAN_POINT('Ctrl Pts',(0.305156680467599,54.6673878667584,1.43203224651504));
#46058=CARTESIAN_POINT('Ctrl Pts',(0.261243144667189,54.6649457800941,1.44068611617323));
#46059=CARTESIAN_POINT('Ctrl Pts',(0.217102745319451,54.6625036934298,1.44730737853946));
#46060=CARTESIAN_POINT('Ctrl Pts',(0.16272743217266,54.6594953557377,1.45546392492125));
#46061=CARTESIAN_POINT('Ctrl Pts',(0.107775865216766,54.6564870180457,1.4605692797054));
#46062=CARTESIAN_POINT('Ctrl Pts',(0.0526209011115321,54.6534786803536,
1.4625536881654));
#46063=CARTESIAN_POINT('Ctrl Pts',(-0.00243496989973289,54.6504757475329,
1.46453453137651));
#46064=CARTESIAN_POINT('Ctrl Pts',(-0.0576929887456028,54.6474728147122,
1.46340553636841));
#46065=CARTESIAN_POINT('Ctrl Pts',(-0.112773589062501,54.6444698818916,
1.45914850772975));
#46066=CARTESIAN_POINT('Ctrl Pts',(-0.167799038727877,54.6414699558228,
1.4548957415338));
#46067=CARTESIAN_POINT('Ctrl Pts',(-0.222646897102024,54.6384700297541,
1.44752118616505));
#46068=CARTESIAN_POINT('Ctrl Pts',(-0.276937883601701,54.6354701036854,
1.43705868308368));
#46069=CARTESIAN_POINT('Ctrl Pts',(-0.331196029517262,54.6324719922701,
1.42660250876395));
#46070=CARTESIAN_POINT('Ctrl Pts',(-0.384897452908743,54.6294738808548,
1.41306218858695));
#46071=CARTESIAN_POINT('Ctrl Pts',(-0.437670606045531,54.6264757694394,
1.3965230719912));
#46072=CARTESIAN_POINT('Ctrl Pts',(-0.49043275341438,54.6234782832761,1.3799874046053));
#46073=CARTESIAN_POINT('Ctrl Pts',(-0.54226651052236,54.6204807971128,1.36045434063509));
#46074=CARTESIAN_POINT('Ctrl Pts',(-0.592815352842416,54.6174833109495,
1.33805911955874));
#46075=CARTESIAN_POINT('Ctrl Pts',(-0.643410948547461,54.6144830523661,
1.31564318480539));
#46076=CARTESIAN_POINT('Ctrl Pts',(-0.692718770243103,54.6114827937827,
1.29036001821938));
#46077=CARTESIAN_POINT('Ctrl Pts',(-0.740403559142361,54.6084825351993,
1.26239249823869));
#46078=CARTESIAN_POINT('Ctrl Pts',(-0.788109755862552,54.6054809296665,
1.23441242239536));
#46079=CARTESIAN_POINT('Ctrl Pts',(-0.834191026089493,54.6024793241337,
1.20374588427166));
#46080=CARTESIAN_POINT('Ctrl Pts',(-0.878340820641819,54.5994777186008,
1.17061934581411));
#46081=CARTESIAN_POINT('Ctrl Pts',(-0.922575540900822,54.5964703392366,
1.13742908577605));
#46082=CARTESIAN_POINT('Ctrl Pts',(-0.964870957345358,54.5934629598724,
1.10176971345234));
#46083=CARTESIAN_POINT('Ctrl Pts',(-1.00495424712117,54.5904555805082,1.06390752003786));
#46084=CARTESIAN_POINT('Ctrl Pts',(-1.03750455812629,54.5880133874106,1.03316088776615));
#46085=CARTESIAN_POINT('Ctrl Pts',(-1.06859667897818,54.5855711943131,1.00096242404768));
#46086=CARTESIAN_POINT('Ctrl Pts',(-1.09810414428273,54.5831290012156,0.96747069118867));
#46087=CARTESIAN_POINT('Ctrl Pts',(-1.1341172943334,54.5801483634155,0.926594838638836));
#46088=CARTESIAN_POINT('Ctrl Pts',(-1.16792915694634,54.5771677256153,0.883609641676309));
#46089=CARTESIAN_POINT('Ctrl Pts',(-1.19928058434743,54.5741870878152,0.838783839858214));
#46090=CARTESIAN_POINT('Ctrl Pts',(-1.23058534817692,54.5712108864065,0.79402475691661));
#46091=CARTESIAN_POINT('Ctrl Pts',(-1.25943662076532,54.5682346849978,0.747430930264581));
#46092=CARTESIAN_POINT('Ctrl Pts',(-1.28561436600705,54.5652584835892,0.699305335255124));
#46093=CARTESIAN_POINT('Ctrl Pts',(-1.31176399018126,54.5622854793222,0.651231438476151));
#46094=CARTESIAN_POINT('Ctrl Pts',(-1.33524551999412,54.5593124750552,0.601629504235346));
#46095=CARTESIAN_POINT('Ctrl Pts',(-1.3558826571817,54.5563394707882,0.550830708978623));
#46096=CARTESIAN_POINT('Ctrl Pts',(-1.3765107506202,54.5533677693718,0.500054175121516));
#46097=CARTESIAN_POINT('Ctrl Pts',(-1.39429670909912,54.5503960679553,0.448082314244971));
#46098=CARTESIAN_POINT('Ctrl Pts',(-1.40911156259441,54.5474243665388,0.395268078856282));
#46099=CARTESIAN_POINT('Ctrl Pts',(-1.4239225907283,54.544453432449,0.342467480695771));
#46100=CARTESIAN_POINT('Ctrl Pts',(-1.43576389637017,54.5414824983592,0.288825460409155));
#46101=CARTESIAN_POINT('Ctrl Pts',(-1.44455659671544,54.5385115642694,0.234709371107956));
#46102=CARTESIAN_POINT('Ctrl Pts',(-1.45335457797144,54.5355388458315,0.180560779591822));
#46103=CARTESIAN_POINT('Ctrl Pts',(-1.45910022057736,54.5325661273937,0.125938084675089));
#46104=CARTESIAN_POINT('Ctrl Pts',(-1.46176623275603,54.5295934089558,0.0712160850809124));
#46105=CARTESIAN_POINT('Ctrl Pts',(-1.46294357534021,54.5282806212515,0.0470502013204441));
#46106=CARTESIAN_POINT('Ctrl Pts',(-1.46352100787057,54.5269678335472,0.022864991273397));
#46107=CARTESIAN_POINT('Ctrl Pts',(-1.463499416148,54.5256550458429,-0.00130726220482866));
#46108=CARTESIAN_POINT('Origin',(0.,55.715,0.));
#46109=CARTESIAN_POINT('',(-1.46349999999901,53.9543449541294,1.70220316479836E-6));
#46110=CARTESIAN_POINT('',(-1.46349998499324,54.0256550457892,0.000209582428622512));
#46111=CARTESIAN_POINT('',(-1.4635,55.715,-1.79227059055215E-16));
#46112=CARTESIAN_POINT('Ctrl Pts',(-1.46349999999901,53.9543449541572,1.70271267885967E-6));
#46113=CARTESIAN_POINT('Ctrl Pts',(-1.46349993602608,53.9573533892216,0.0549871306756696));
#46114=CARTESIAN_POINT('Ctrl Pts',(-1.4603967571549,53.9603618242859,0.110089773684055));
#46115=CARTESIAN_POINT('Ctrl Pts',(-1.45417680140553,53.9633702593503,0.16493053160035));
#46116=CARTESIAN_POINT('Ctrl Pts',(-1.44796802121601,53.9663732890793,0.219672755669014));
#46117=CARTESIAN_POINT('Ctrl Pts',(-1.43865363596765,53.9693763188084,0.274153507271366));
#46118=CARTESIAN_POINT('Ctrl Pts',(-1.42627196782833,53.9723793485375,0.327994700852163));
#46119=CARTESIAN_POINT('Ctrl Pts',(-1.4139026984683,53.9753793710868,0.381781978832245));
#46120=CARTESIAN_POINT('Ctrl Pts',(-1.39847234824465,53.978379393636,0.434930454602946));
#46121=CARTESIAN_POINT('Ctrl Pts',(-1.38007065789482,53.9813794161852,0.487070045494232));
#46122=CARTESIAN_POINT('Ctrl Pts',(-1.36168010205213,53.9843776234788,0.539178087726878));
#46123=CARTESIAN_POINT('Ctrl Pts',(-1.3403219449858,53.9873758307724,0.590277957279319));
#46124=CARTESIAN_POINT('Ctrl Pts',(-1.31613571827124,53.990374038066,0.640014860054559));
#46125=CARTESIAN_POINT('Ctrl Pts',(-1.29195454166697,53.9933716193307,0.689741377710707));
#46126=CARTESIAN_POINT('Ctrl Pts',(-1.26494669903289,53.9963692005953,0.738105018336184));
#46127=CARTESIAN_POINT('Ctrl Pts',(-1.23529883145681,53.99936678186,0.784773245594821));
#46128=CARTESIAN_POINT('Ctrl Pts',(-1.20562354636837,54.0023671352034,0.831484630314773));
#46129=CARTESIAN_POINT('Ctrl Pts',(-1.17330364236257,54.0053674885467,0.876497021543102));
#46130=CARTESIAN_POINT('Ctrl Pts',(-1.13856971830611,54.00836784189,0.91950597961968));
#46131=CARTESIAN_POINT('Ctrl Pts',(-1.10382021305539,54.0113695411535,0.962534230964986));
#46132=CARTESIAN_POINT('Ctrl Pts',(-1.06665488468436,54.014371240417,1.00355686488468));
#46133=CARTESIAN_POINT('Ctrl Pts',(-1.02734317536112,54.0173729396805,1.04230429819652));
#46134=CARTESIAN_POINT('Ctrl Pts',(-0.987955827932152,54.0203804143949,
1.08112628391292));
#46135=CARTESIAN_POINT('Ctrl Pts',(-0.946414247093647,54.0233878891092,
1.11766397294946));
#46136=CARTESIAN_POINT('Ctrl Pts',(-0.903022262819839,54.0263953638236,
1.15168704206123));
#46137=CARTESIAN_POINT('Ctrl Pts',(-0.867725264986005,54.0288417794521,
1.1793629415813));
#46138=CARTESIAN_POINT('Ctrl Pts',(-0.831204594011595,54.0312881950806,
1.20537564955582));
#46139=CARTESIAN_POINT('Ctrl Pts',(-0.793636730561745,54.033734610709,1.2296231088847));
#46140=CARTESIAN_POINT('Ctrl Pts',(-0.747439914276172,54.0367429429103,
1.25943996087319));
#46141=CARTESIAN_POINT('Ctrl Pts',(-0.69946191794101,54.0397512751115,1.28671336006666));
#46142=CARTESIAN_POINT('Ctrl Pts',(-0.650013825152869,54.0427596073127,
1.31122624939792));
#46143=CARTESIAN_POINT('Ctrl Pts',(-0.600654576570762,54.0457625343937,
1.33569509601555));
#46144=CARTESIAN_POINT('Ctrl Pts',(-0.549830942972984,54.0487654614747,
1.35741304220325));
#46145=CARTESIAN_POINT('Ctrl Pts',(-0.497881347329851,54.0517683885557,
1.37620725691337));
#46146=CARTESIAN_POINT('Ctrl Pts',(-0.445983770009828,54.0547683087368,
1.39498265254469));
#46147=CARTESIAN_POINT('Ctrl Pts',(-0.392962958728821,54.057768228918,1.41083993669034));
#46148=CARTESIAN_POINT('Ctrl Pts',(-0.339178497152869,54.0607681490992,
1.42365381925141));
#46149=CARTESIAN_POINT('Ctrl Pts',(-0.285426572291352,54.0637662544895,
1.43645995010082));
#46150=CARTESIAN_POINT('Ctrl Pts',(-0.230912426129334,54.0667643598799,
1.44622620590558));
#46151=CARTESIAN_POINT('Ctrl Pts',(-0.176009798460427,54.0697624652702,
1.4528774211357));
#46152=CARTESIAN_POINT('Ctrl Pts',(-0.121118623008082,54.0727599452815,
1.45952724897945));
#46153=CARTESIAN_POINT('Ctrl Pts',(-0.0658396516920146,54.0757574252928,
1.46306326283564));
#46154=CARTESIAN_POINT('Ctrl Pts',(-0.0105534703801381,54.0787549053042,
1.46346194834814));
#46155=CARTESIAN_POINT('Ctrl Pts',(0.0447838433034418,54.0817551575862,
1.46386100259177));
#46156=CARTESIAN_POINT('Ctrl Pts',(0.100127850262098,54.0847554098682,1.46111692700126));
#46157=CARTESIAN_POINT('Ctrl Pts',(0.155097734339402,54.0877556621503,1.45525837664752));
#46158=CARTESIAN_POINT('Ctrl Pts',(0.210092295193867,54.090757261289,1.44939719630567));
#46159=CARTESIAN_POINT('Ctrl Pts',(0.264711875505141,54.0937588604278,1.44041883993959));
#46160=CARTESIAN_POINT('Ctrl Pts',(0.318583882175109,54.0967604595665,1.42840350042214));
#46161=CARTESIAN_POINT('Ctrl Pts',(0.372559514923604,54.0997678324636,1.41636504866899));
#46162=CARTESIAN_POINT('Ctrl Pts',(0.425784190889171,54.1027752053607,1.40127808736956));
#46163=CARTESIAN_POINT('Ctrl Pts',(0.477899657451986,54.1057825782578,1.38327299091946));
#46164=CARTESIAN_POINT('Ctrl Pts',(0.520221831142743,54.1082248198129,1.36865132734169));
#46165=CARTESIAN_POINT('Ctrl Pts',(0.561812711243729,54.110667061368,1.35210620685036));
#46166=CARTESIAN_POINT('Ctrl Pts',(0.602491761139594,54.1131093029232,1.33373008054813));
#46167=CARTESIAN_POINT('Ctrl Pts',(0.652599867060699,54.1161176351935,1.31109452525543));
#46168=CARTESIAN_POINT('Ctrl Pts',(0.701537431757105,54.1191259674638,1.28558293299416));
#46169=CARTESIAN_POINT('Ctrl Pts',(0.748953361756599,54.1221342997342,1.25733890097837));
#46170=CARTESIAN_POINT('Ctrl Pts',(0.796284098780793,54.1251372268848,1.22914561547586));
#46171=CARTESIAN_POINT('Ctrl Pts',(0.842098175770399,54.1281401540355,1.19822990093416));
#46172=CARTESIAN_POINT('Ctrl Pts',(0.886066823055248,54.1311430811861,1.16478231231453));
#46173=CARTESIAN_POINT('Ctrl Pts',(0.929991443528835,54.1341430014372,1.1313682155297));
#46174=CARTESIAN_POINT('Ctrl Pts',(0.972073875769551,54.1371429216883,1.09542758504222));
#46175=CARTESIAN_POINT('Ctrl Pts',(1.01201381034426,54.1401428419394,1.05719454107203));
#46176=CARTESIAN_POINT('Ctrl Pts',(1.05192958340331,54.1431409473998,1.01898462604034));
#46177=CARTESIAN_POINT('Ctrl Pts',(1.08970504626173,54.1461390528602,0.978485410964945));
#46178=CARTESIAN_POINT('Ctrl Pts',(1.12507431979167,54.1491371583206,0.935970098317945));
#46179=CARTESIAN_POINT('Ctrl Pts',(1.16043621559541,54.1521346384021,0.893463653999441));
#46180=CARTESIAN_POINT('Ctrl Pts',(1.19339258059246,54.1551321184835,0.84894235346802));
#46181=CARTESIAN_POINT('Ctrl Pts',(1.22371721374798,54.1581295985649,0.802713168433708));
#46182=CARTESIAN_POINT('Ctrl Pts',(1.25406989315387,54.1611298509165,0.756441227554957));
#46183=CARTESIAN_POINT('Ctrl Pts',(1.28178568664402,54.1641301032681,0.708458689278313));
#46184=CARTESIAN_POINT('Ctrl Pts',(1.30668209535494,54.1671303556197,0.659101017810481));
#46185=CARTESIAN_POINT('Ctrl Pts',(1.3315896804226,54.1701319548279,0.609721188972472));
#46186=CARTESIAN_POINT('Ctrl Pts',(1.35367514617084,54.173133554036,0.558965482172848));
#46187=CARTESIAN_POINT('Ctrl Pts',(1.3728037507583,54.1761351532441,0.507190409909275));
#46188=CARTESIAN_POINT('Ctrl Pts',(1.39196915037071,54.1791425262094,0.455315745170632));
#46189=CARTESIAN_POINT('Ctrl Pts',(1.40816617043101,54.1821498991748,0.402418304684393));
#46190=CARTESIAN_POINT('Ctrl Pts',(1.42131000508393,54.1851572721401,0.348869774340397));
#46191=CARTESIAN_POINT('Ctrl Pts',(1.43198390959968,54.1875995131392,0.305383842346905));
#46192=CARTESIAN_POINT('Ctrl Pts',(1.44064524891602,54.1900417541383,0.261468894889259));
#46193=CARTESIAN_POINT('Ctrl Pts',(1.44727375927812,54.1924839951374,0.217326748710252));
#46194=CARTESIAN_POINT('Ctrl Pts',(1.45543870299328,54.1954923272071,0.162952821639372));
#46195=CARTESIAN_POINT('Ctrl Pts',(1.46055255904921,54.1985006592768,0.108002164972088));
#46196=CARTESIAN_POINT('Ctrl Pts',(1.46254551339752,54.2015089913464,0.0528476228488291));
#46197=CARTESIAN_POINT('Ctrl Pts',(1.46453488697223,54.2045119182968,-0.00220782220849207));
#46198=CARTESIAN_POINT('Ctrl Pts',(1.46341446723391,54.2075148452472,-0.0574659016324648));
#46199=CARTESIAN_POINT('Ctrl Pts',(1.45916599836584,54.2105177721975,-0.112547053328953));
#46200=CARTESIAN_POINT('Ctrl Pts',(1.4549217835865,54.2135176922487,-0.167573051012567));
#46201=CARTESIAN_POINT('Ctrl Pts',(1.44755576439947,54.2165176122998,-0.222421947242493));
#46202=CARTESIAN_POINT('Ctrl Pts',(1.43710172189686,54.219517532351,-0.276714457376353));
#46203=CARTESIAN_POINT('Ctrl Pts',(1.42665400352655,54.2225156376122,-0.330974123467612));
#46204=CARTESIAN_POINT('Ctrl Pts',(1.41312206399171,54.2255137428734,-0.384677552264548));
#46205=CARTESIAN_POINT('Ctrl Pts',(1.39659119359043,54.2285118481346,-0.43745318376445));
#46206=CARTESIAN_POINT('Ctrl Pts',(1.38006377138099,54.2315093280178,-0.490217806739235));
#46207=CARTESIAN_POINT('Ctrl Pts',(1.36053881836953,54.234506807901,-0.542054512266186));
#46208=CARTESIAN_POINT('Ctrl Pts',(1.33815151727725,54.2375042877842,-0.592606755621791));
#46209=CARTESIAN_POINT('Ctrl Pts',(1.31574351088537,54.2405045399409,-0.643205753132372));
#46210=CARTESIAN_POINT('Ctrl Pts',(1.29046808152626,54.2435047920975,-0.692517430171096));
#46211=CARTESIAN_POINT('Ctrl Pts',(1.26250805423934,54.2465050442541,-0.74020650022868));
#46212=CARTESIAN_POINT('Ctrl Pts',(1.23453547527884,54.2495066432687,-0.78791697862163));
#46213=CARTESIAN_POINT('Ctrl Pts',(1.20387618937576,54.2525082422833,-0.834002956764934));
#46214=CARTESIAN_POINT('Ctrl Pts',(1.17075660960583,54.2555098412979,-0.878157850881181));
#46215=CARTESIAN_POINT('Ctrl Pts',(1.13757332226858,54.2585172140745,-0.922397679676829));
#46216=CARTESIAN_POINT('Ctrl Pts',(1.10192062801555,54.2615245868511,-0.964698597828198));
#46217=CARTESIAN_POINT('Ctrl Pts',(1.06406477447401,54.2645319596277,-1.00478774162684));
#46218=CARTESIAN_POINT('Ctrl Pts',(1.03332260046163,54.2669742022023,-1.03734353734581));
#46219=CARTESIAN_POINT('Ctrl Pts',(1.00112830682736,54.2694164447769,-1.06844130958447));
#46220=CARTESIAN_POINT('Ctrl Pts',(0.967640446453791,54.2718586873516,-1.09795456025589));
#46221=CARTESIAN_POINT('Ctrl Pts',(0.926390404078387,54.2748670195821,-1.13430871448525));
#46222=CARTESIAN_POINT('Ctrl Pts',(0.883000809343282,54.2778753518127,-1.16841251976987));
#46223=CARTESIAN_POINT('Ctrl Pts',(0.837747015186586,54.2808836840433,-1.20000507855007));
#46224=CARTESIAN_POINT('Ctrl Pts',(0.792574529298209,54.2838866111517,-1.23154087443793));
#46225=CARTESIAN_POINT('Ctrl Pts',(0.745544920711969,54.2868895382602,-1.260574077247));
#46226=CARTESIAN_POINT('Ctrl Pts',(0.696967153554221,54.2898924653686,-1.28688345892957));
#46227=CARTESIAN_POINT('Ctrl Pts',(0.648438028449004,54.292892385576,-1.31316649641394));
#46228=CARTESIAN_POINT('Ctrl Pts',(0.598364278136964,54.2958923057834,-1.33673086467611));
#46229=CARTESIAN_POINT('Ctrl Pts',(0.54708286080914,54.2988922259909,-1.3573992019332));
#46230=CARTESIAN_POINT('Ctrl Pts',(0.495832466008745,54.3018903314063,-1.37805503594656));
#46231=CARTESIAN_POINT('Ctrl Pts',(0.443376341644131,54.3048884368216,-1.39581811383031));
#46232=CARTESIAN_POINT('Ctrl Pts',(0.390072897403153,54.307886542237,-1.41055853643566));
#46233=CARTESIAN_POINT('Ctrl Pts',(0.336780571824872,54.3108840222722,-1.42529588430936));
#46234=CARTESIAN_POINT('Ctrl Pts',(0.282641786766773,54.3138815023073,-1.43701168791634));
#46235=CARTESIAN_POINT('Ctrl Pts',(0.228029401594911,54.3168789823424,-1.44562610726573));
#46236=CARTESIAN_POINT('Ctrl Pts',(0.173366507261933,54.3198792346461,-1.45424849380229));
#46237=CARTESIAN_POINT('Ctrl Pts',(0.118229661204808,54.3228794869499,-1.45976368225195));
#46238=CARTESIAN_POINT('Ctrl Pts',(0.0629997072737128,54.3258797392536,
-1.46214338793547));
#46239=CARTESIAN_POINT('Ctrl Pts',(0.00774495983722705,54.3288813384129,
-1.46452416190245));
#46240=CARTESIAN_POINT('Ctrl Pts',(-0.0476024489784899,54.3318829375723,
-1.46376665434922));
#46241=CARTESIAN_POINT('Ctrl Pts',(-0.102662144137076,54.3348845367316,
-1.45989476818063));
#46242=CARTESIAN_POINT('Ctrl Pts',(-0.157827749925949,54.3378919096471,
-1.45601543420647));
#46243=CARTESIAN_POINT('Ctrl Pts',(-0.212704010310351,54.3408992825627,
-1.44900982032604));
#46244=CARTESIAN_POINT('Ctrl Pts',(-0.266917270148343,54.3439066554783,
-1.43895358538646));
#46245=CARTESIAN_POINT('Ctrl Pts',(-0.310943025945519,54.3463488968408,
-1.43078707141899));
#46246=CARTESIAN_POINT('Ctrl Pts',(-0.354531603814856,54.3487911382033,
-1.42060974891572));
#46247=CARTESIAN_POINT('Ctrl Pts',(-0.397490727899304,54.3512333795657,
-1.40848619845353));
#46248=CARTESIAN_POINT('Ctrl Pts',(-0.450407420777729,54.3542417122277,
-1.39355250950907));
#46249=CARTESIAN_POINT('Ctrl Pts',(-0.502594203267989,54.3572500448897,
-1.37560071000914));
#46250=CARTESIAN_POINT('Ctrl Pts',(-0.553682533718253,54.3602583775517,
-1.35472059918469));
#46251=CARTESIAN_POINT('Ctrl Pts',(-0.604679072979523,54.3632613050962,
-1.33387800397647));
#46252=CARTESIAN_POINT('Ctrl Pts',(-0.654580591136171,54.3662642326406,
-1.31011773653688));
#46253=CARTESIAN_POINT('Ctrl Pts',(-0.703033640352132,54.369267160185,-1.28357935108556));
#46254=CARTESIAN_POINT('Ctrl Pts',(-0.751438172445503,54.3722670808309,
-1.25706753911354));
#46255=CARTESIAN_POINT('Ctrl Pts',(-0.798396647012399,54.3752670014768,
-1.2277833720989));
#46256=CARTESIAN_POINT('Ctrl Pts',(-0.843577282665841,54.3782669221226,
-1.19591371685842));
#46257=CARTESIAN_POINT('Ctrl Pts',(-0.888730586469374,54.3812650279782,
-1.16406334104198));
#46258=CARTESIAN_POINT('Ctrl Pts',(-0.932107751592581,54.3842631338337,
-1.12963088107265));
#46259=CARTESIAN_POINT('Ctrl Pts',(-0.973405233355805,54.3872612396893,
-1.09284697084063));
#46260=CARTESIAN_POINT('Ctrl Pts',(-1.01469410081568,54.3902587201654,-1.05607073341933));
#46261=CARTESIAN_POINT('Ctrl Pts',(-1.05390375154847,54.3932562006416,-1.01694437120819));
#46262=CARTESIAN_POINT('Ctrl Pts',(-1.09076485699683,54.3962536811178,-0.975737811474319));
#46263=CARTESIAN_POINT('Ctrl Pts',(-1.12766005401229,54.3992539338604,-0.9344931412123));
#46264=CARTESIAN_POINT('Ctrl Pts',(-1.16220201232692,54.4022541866031,-0.891164824363979));
#46265=CARTESIAN_POINT('Ctrl Pts',(-1.19416038342083,54.4052544393457,-0.846057461800444));
#46266=CARTESIAN_POINT('Ctrl Pts',(-1.22613310107108,54.4082560389435,-0.800929849915821));
#46267=CARTESIAN_POINT('Ctrl Pts',(-1.25551963809301,54.4112576385412,-0.754022049243226));
#46268=CARTESIAN_POINT('Ctrl Pts',(-1.28213374261602,54.4142592381389,-0.70566657568956));
#46269=CARTESIAN_POINT('Ctrl Pts',(-1.30879904090305,54.4172666114865,-0.657218087595426));
#46270=CARTESIAN_POINT('Ctrl Pts',(-1.3326810233957,54.4202739848341,-0.607316841650005));
#46271=CARTESIAN_POINT('Ctrl Pts',(-1.3536405631197,54.4232813581817,-0.55631778317521));
#46272=CARTESIAN_POINT('Ctrl Pts',(-1.37066145665484,54.4257235960478,-0.514902296188243));
#46273=CARTESIAN_POINT('Ctrl Pts',(-1.38575594771885,54.4281658339138,-0.472763328227954));
#46274=CARTESIAN_POINT('Ctrl Pts',(-1.39887399106228,54.4306080717799,-0.430097439110576));
#46275=CARTESIAN_POINT('Ctrl Pts',(-1.41857703393164,54.4342762649786,-0.366014113546658));
#46276=CARTESIAN_POINT('Ctrl Pts',(-1.43388913296348,54.4379444581773,-0.300521302854243));
#46277=CARTESIAN_POINT('Ctrl Pts',(-1.44464494335243,54.441612651376,-0.234164979547004));
#46278=CARTESIAN_POINT('Ctrl Pts',(-1.45524603995122,54.4452280805288,-0.168763139250205));
#46279=CARTESIAN_POINT('Ctrl Pts',(-1.46142092106582,54.4488435096816,-0.10252243931409));
#46280=CARTESIAN_POINT('Ctrl Pts',(-1.46305749085711,54.4524589388344,-0.0359865036769872));
#46281=CARTESIAN_POINT('Ctrl Pts',(-1.46334206291177,54.4530876013625,-0.0244170197394469));
#46282=CARTESIAN_POINT('Ctrl Pts',(-1.46348953364981,54.4537162638907,-0.0128386611170273));
#46283=CARTESIAN_POINT('Ctrl Pts',(-1.46349946245349,54.4543449264188,-0.00125435176163375));
#46284=CARTESIAN_POINT('Ctrl Pts',(-1.46349941614739,54.5256550458061,-0.00130726288314757));
#46285=CARTESIAN_POINT('Ctrl Pts',(-1.46343776422637,54.5219065796245,-0.0703274665285052));
#46286=CARTESIAN_POINT('Ctrl Pts',(-1.45848961851053,54.5181581134429,-0.13913082750592));
#46287=CARTESIAN_POINT('Ctrl Pts',(-1.44876956711919,54.5144096472613,-0.207120716948527));
#46288=CARTESIAN_POINT('Ctrl Pts',(-1.43955953911841,54.5108578678414,-0.271543090897566));
#46289=CARTESIAN_POINT('Ctrl Pts',(-1.42606575562852,54.5073060884214,-0.335235472021534));
#46290=CARTESIAN_POINT('Ctrl Pts',(-1.40842466851716,54.5037543090015,-0.39770869127081));
#46291=CARTESIAN_POINT('Ctrl Pts',(-1.39348277695714,54.5007459738234,-0.45062312117727));
#46292=CARTESIAN_POINT('Ctrl Pts',(-1.37552288279277,54.4977376386452,-0.502807170500935));
#46293=CARTESIAN_POINT('Ctrl Pts',(-1.35463484295704,54.4947293034671,-0.553892311055827));
#46294=CARTESIAN_POINT('Ctrl Pts',(-1.33378433265413,54.4917263733636,-0.604885666959094));
#46295=CARTESIAN_POINT('Ctrl Pts',(-1.3100163151661,54.48872344326,-0.654783546654793));
#46296=CARTESIAN_POINT('Ctrl Pts',(-1.28347040005656,54.4857205131565,-0.703232523550111));
#46297=CARTESIAN_POINT('Ctrl Pts',(-1.25695106572798,54.4827205899272,-0.751632987834817));
#46298=CARTESIAN_POINT('Ctrl Pts',(-1.22765959633201,54.4797206666979,-0.798586961608401));
#46299=CARTESIAN_POINT('Ctrl Pts',(-1.19578291064711,54.4767207434685,-0.843762692114504));
#46300=CARTESIAN_POINT('Ctrl Pts',(-1.16392550841339,54.4737226350098,-0.888911094058218));
#46301=CARTESIAN_POINT('Ctrl Pts',(-1.12948629366787,54.4707245265512,-0.932282953475559));
#46302=CARTESIAN_POINT('Ctrl Pts',(-1.09269594786137,54.4677264180925,-0.973574761139249));
#46303=CARTESIAN_POINT('Ctrl Pts',(-1.05591327601637,54.4647289349981,-1.01485795589823));
#46304=CARTESIAN_POINT('Ctrl Pts',(-1.01678079848737,54.4617314519037,-1.05406156572294));
#46305=CARTESIAN_POINT('Ctrl Pts',(-0.97556848477783,54.4587339688093,-1.090916303622));
#46306=CARTESIAN_POINT('Ctrl Pts',(-0.934318055219737,54.4557337134461,
-1.12780512719794));
#46307=CARTESIAN_POINT('Ctrl Pts',(-0.890984341139564,54.4527334580829,
-1.16234038489046));
#46308=CARTESIAN_POINT('Ctrl Pts',(-0.845871979587388,54.4497332027197,
-1.19429177513241));
#46309=CARTESIAN_POINT('Ctrl Pts',(-0.800739366405015,54.4467316004959,
-1.22625750884291));
#46310=CARTESIAN_POINT('Ctrl Pts',(-0.753826963071888,54.4437299982722,
-1.2556367815072));
#46311=CARTESIAN_POINT('Ctrl Pts',(-0.705467314835336,54.4407283960484,
-1.28224339253475));
#46312=CARTESIAN_POINT('Ctrl Pts',(-0.657014644503662,54.4377210200992,
-1.30890118265049));
#46313=CARTESIAN_POINT('Ctrl Pts',(-0.607109646006053,54.4347136441501,
-1.33277542708262));
#46314=CARTESIAN_POINT('Ctrl Pts',(-0.556107286701153,54.4317062682009,
-1.35372705361084));
#46315=CARTESIAN_POINT('Ctrl Pts',(-0.514689506526157,54.4292640510631,
-1.37074136184444));
#46316=CARTESIAN_POINT('Ctrl Pts',(-0.472548556674602,54.4268218339252,
-1.38582918825657));
#46317=CARTESIAN_POINT('Ctrl Pts',(-0.42988099944998,54.4243796167873,-1.3989405192187));
#46318=CARTESIAN_POINT('Ctrl Pts',(-0.377322935550869,54.4213712841633,
-1.41509110798764));
#46319=CARTESIAN_POINT('Ctrl Pts',(-0.323741358591926,54.4183629515393,
-1.42831011315973));
#46320=CARTESIAN_POINT('Ctrl Pts',(-0.269494607687241,54.4153546189152,
-1.43847311633812));
#46321=CARTESIAN_POINT('Ctrl Pts',(-0.215345322320914,54.4123516913846,
-1.44861785957357));
#46322=CARTESIAN_POINT('Ctrl Pts',(-0.160533750147607,54.4093487638541,
-1.45571740011836));
#46323=CARTESIAN_POINT('Ctrl Pts',(-0.105432531682753,54.4063458363235,
-1.45969730809609));
#46324=CARTESIAN_POINT('Ctrl Pts',(-0.0503864870309643,54.4033459156767,
-1.4636732309224));
#46325=CARTESIAN_POINT('Ctrl Pts',(0.0049481045831354,54.40034599503,-1.46453567080183));
#46326=CARTESIAN_POINT('Ctrl Pts',(0.0601911479564839,54.3973460743832,
-1.46226169877614));
#46327=CARTESIAN_POINT('Ctrl Pts',(0.115400772536663,54.3943479685121,-1.45998910236983));
#46328=CARTESIAN_POINT('Ctrl Pts',(0.170518431290405,54.3913498626409,-1.45458387610775));
#46329=CARTESIAN_POINT('Ctrl Pts',(0.225164017286448,54.3883517567698,-1.44607517623374));
#46330=CARTESIAN_POINT('Ctrl Pts',(0.279798204946626,54.3853542762633,-1.43756825116032));
#46331=CARTESIAN_POINT('Ctrl Pts',(0.333959993074543,54.3823567957568,-1.42595921913628));
#46332=CARTESIAN_POINT('Ctrl Pts',(0.387276712919702,54.3793593152503,-1.41132880564031));
#46333=CARTESIAN_POINT('Ctrl Pts',(0.440642743967967,54.3763590624545,-1.39668486086759));
#46334=CARTESIAN_POINT('Ctrl Pts',(0.493161633905515,54.3733588096587,-1.37901409145004));
#46335=CARTESIAN_POINT('Ctrl Pts',(0.544474660054742,54.370358556863,-1.35844749422209));
#46336=CARTESIAN_POINT('Ctrl Pts',(0.595810721550143,54.3673569571994,-1.3378716642764));
#46337=CARTESIAN_POINT('Ctrl Pts',(0.645939360235003,54.3643553575359,-1.31439763967138));
#46338=CARTESIAN_POINT('Ctrl Pts',(0.694523763630163,54.3613537578723,-1.2882037850251));
#46339=CARTESIAN_POINT('Ctrl Pts',(0.743201622252027,54.3583463844386,-1.26195954481364));
#46340=CARTESIAN_POINT('Ctrl Pts',(0.790328859340506,54.355339011005,-1.23298530008649));
#46341=CARTESIAN_POINT('Ctrl Pts',(0.835596091803423,54.3523316375713,-1.20150381662434));
#46342=CARTESIAN_POINT('Ctrl Pts',(0.872356854175208,54.3498893999052,-1.17593823044428));
#46343=CARTESIAN_POINT('Ctrl Pts',(0.907891455234829,54.3474471622392,-1.14872007734812));
#46344=CARTESIAN_POINT('Ctrl Pts',(0.942051250991144,54.3450049245731,-1.11998736176174));
#46345=CARTESIAN_POINT('Ctrl Pts',(0.984129047428765,54.341996593373,-1.08459460455182));
#46346=CARTESIAN_POINT('Ctrl Pts',(1.02429924813557,54.3389882621728,-1.04675178230511));
#46347=CARTESIAN_POINT('Ctrl Pts',(1.06226295109496,54.3359799309727,-1.00669244197571));
#46348=CARTESIAN_POINT('Ctrl Pts',(1.1001584436897,54.3329770049189,-0.966705077296702));
#46349=CARTESIAN_POINT('Ctrl Pts',(1.13585494489424,54.329974078865,-0.92450947809802));
#46350=CARTESIAN_POINT('Ctrl Pts',(1.16908778985078,54.3269711528111,-0.880378321871802));
#46351=CARTESIAN_POINT('Ctrl Pts',(1.20228735781706,54.3239712336723,-0.836291355424049));
#46352=CARTESIAN_POINT('Ctrl Pts',(1.2330278394993,54.3209713145335,-0.790273091355688));
#46353=CARTESIAN_POINT('Ctrl Pts',(1.26108379172199,54.3179713953947,-0.742630406229155));
#46354=CARTESIAN_POINT('Ctrl Pts',(1.28912277146795,54.31497329106,-0.69501654259328));
#46355=CARTESIAN_POINT('Ctrl Pts',(1.31448017255231,54.3119751867253,-0.645780660293874));
#46356=CARTESIAN_POINT('Ctrl Pts',(1.33697430174022,54.3089770823906,-0.595257899138059));
#46357=CARTESIAN_POINT('Ctrl Pts',(1.35946373875826,54.3059796034464,-0.544745676793315));
#46358=CARTESIAN_POINT('Ctrl Pts',(1.37909087479105,54.3029821245022,-0.492947591473747));
#46359=CARTESIAN_POINT('Ctrl Pts',(1.39572137425979,54.299984645558,-0.440220507739433));
#46360=CARTESIAN_POINT('Ctrl Pts',(1.41236725468445,54.2969843943524,-0.387444658605611));
#46361=CARTESIAN_POINT('Ctrl Pts',(1.42601080144522,54.2939841431469,-0.333738599817354));
#46362=CARTESIAN_POINT('Ctrl Pts',(1.43656747646328,54.2909838919413,-0.279474749428162));
#46363=CARTESIAN_POINT('Ctrl Pts',(1.44712889050309,54.2879822938859,-0.225186539326533));
#46364=CARTESIAN_POINT('Ctrl Pts',(1.45460059878481,54.2849806958305,-0.170340563466602));
#46365=CARTESIAN_POINT('Ctrl Pts',(1.45894974156856,54.2819790977751,-0.115316527770419));
#46366=CARTESIAN_POINT('Ctrl Pts',(1.46330725019915,54.2789717259591,-0.060186649916865));
#46367=CARTESIAN_POINT('Ctrl Pts',(1.46453018168205,54.275964354143,-0.00487855816238617));
#46368=CARTESIAN_POINT('Ctrl Pts',(1.46263785624305,54.272956982327,0.0502269995594));
#46369=CARTESIAN_POINT('Ctrl Pts',(1.46110112182314,54.2705147323376,0.0949775512002204));
#46370=CARTESIAN_POINT('Ctrl Pts',(1.45751093409315,54.2680724823483,0.139594440919207));
#46371=CARTESIAN_POINT('Ctrl Pts',(1.45190259880462,54.265630232359,0.183877931205435));
#46372=CARTESIAN_POINT('Ctrl Pts',(1.44499432232729,54.2626218997103,0.238425774467192));
#46373=CARTESIAN_POINT('Ctrl Pts',(1.4349929986005,54.2596135670617,0.292700086311256));
#46374=CARTESIAN_POINT('Ctrl Pts',(1.42193269097772,54.256605234413,0.346323075074201));
#46375=CARTESIAN_POINT('Ctrl Pts',(1.40889584898746,54.2536023068766,0.399849718683207));
#46376=CARTESIAN_POINT('Ctrl Pts',(1.39281105377228,54.2505993793402,0.45272685185352));
#46377=CARTESIAN_POINT('Ctrl Pts',(1.37376381367828,54.2475964518038,0.504584219162773));
#46378=CARTESIAN_POINT('Ctrl Pts',(1.35473564599147,54.2445965311627,0.55638966058566));
#46379=CARTESIAN_POINT('Ctrl Pts',(1.33275109063391,54.2415966105216,0.60717686483264));
#46380=CARTESIAN_POINT('Ctrl Pts',(1.30794566188285,54.2385966898805,0.656589975221846));
#46381=CARTESIAN_POINT('Ctrl Pts',(1.28315523905266,54.2355985840264,0.705973193395472));
#46382=CARTESIAN_POINT('Ctrl Pts',(1.25554756167424,54.2326004781724,0.753983493472151));
#46383=CARTESIAN_POINT('Ctrl Pts',(1.22530561964596,54.2296023723184,0.800286441509554));
#46384=CARTESIAN_POINT('Ctrl Pts',(1.19506998579682,54.2266048918405,0.846579731195973));
#46385=CARTESIAN_POINT('Ctrl Pts',(1.16220146737196,54.2236074113626,0.891165933422689));
#46386=CARTESIAN_POINT('Ctrl Pts',(1.12692699394499,54.2206099308847,0.933738614558757));
#46387=CARTESIAN_POINT('Ctrl Pts',(1.09161989631333,54.2176096781353,0.976350669772697));
#46388=CARTESIAN_POINT('Ctrl Pts',(1.05390273574852,54.2146094253859,1.01694507482582));
#46389=CARTESIAN_POINT('Ctrl Pts',(1.01404252055877,54.2116091726365,1.05524879364954));
#46390=CARTESIAN_POINT('Ctrl Pts',(0.974164411528354,54.2086075730293,1.09356970757968));
#46391=CARTESIAN_POINT('Ctrl Pts',(0.932141732274421,54.205605973422,1.1295975404169));
#46392=CARTESIAN_POINT('Ctrl Pts',(0.888275646213262,54.2026043738148,1.16309871736857));
#46393=CARTESIAN_POINT('Ctrl Pts',(0.844325181142252,54.1995970004532,1.19666433581466));
#46394=CARTESIAN_POINT('Ctrl Pts',(0.798524664186527,54.1965896270917,1.22769329106748));
#46395=CARTESIAN_POINT('Ctrl Pts',(0.751204438885884,54.1935822537301,1.2559952790509));
#46396=CARTESIAN_POINT('Ctrl Pts',(0.712776471366623,54.1911400158683,1.27897885252392));
#46397=CARTESIAN_POINT('Ctrl Pts',(0.67334691764437,54.1886977780066,1.30016485093418));
#46398=CARTESIAN_POINT('Ctrl Pts',(0.63310272398115,54.1862555401448,1.31947458895109));
#46399=CARTESIAN_POINT('Ctrl Pts',(0.583530196150556,54.1832472079272,1.34326019472704));
#46400=CARTESIAN_POINT('Ctrl Pts',(0.532509652540926,54.1802388757095,1.36429898322371));
#46401=CARTESIAN_POINT('Ctrl Pts',(0.480376950062696,54.1772305434919,1.38241463962462));
#46402=CARTESIAN_POINT('Ctrl Pts',(0.428337915222931,54.1742276163916,1.40049774734353));
#46403=CARTESIAN_POINT('Ctrl Pts',(0.375191182263449,54.1712246892913,1.41566797300545));
#46404=CARTESIAN_POINT('Ctrl Pts',(0.321294183042467,54.1682217621909,1.42779630828178));
#46405=CARTESIAN_POINT('Ctrl Pts',(0.26745115209298,54.1652218419887,1.43991249918457));
#46406=CARTESIAN_POINT('Ctrl Pts',(0.212859856349481,54.1622219217865,1.44899271754237));
#46407=CARTESIAN_POINT('Ctrl Pts',(0.157892756878364,54.1592220015843,1.45495777510048));
#46408=CARTESIAN_POINT('Ctrl Pts',(0.102958909522796,54.1562238961712,1.46091922412213));
#46409=CARTESIAN_POINT('Ctrl Pts',(0.0476502337176695,54.1532257907581,
1.46376919029396));
#46410=CARTESIAN_POINT('Ctrl Pts',(-0.00765305361946869,54.150227685345,
1.46347998987697));
#46411=CARTESIAN_POINT('Ctrl Pts',(-0.0629448051966588,54.1472302053093,
1.46319084978455));
#46412=CARTESIAN_POINT('Ctrl Pts',(-0.118230641962594,54.1442327252736,
1.45976384601396));
#46413=CARTESIAN_POINT('Ctrl Pts',(-0.173130034968162,54.1412352452378,
1.45322339679484));
#46414=CARTESIAN_POINT('Ctrl Pts',(-0.22808020266123,54.138234992929,1.44667689852403));
#46415=CARTESIAN_POINT('Ctrl Pts',(-0.282642686123091,54.1352347406201,
1.43701126397151));
#46416=CARTESIAN_POINT('Ctrl Pts',(-0.336443272906292,54.1322344883113,
1.42430269750362));
#46417=CARTESIAN_POINT('Ctrl Pts',(-0.390268011576567,54.1292328891443,
1.41158842597041));
#46418=CARTESIAN_POINT('Ctrl Pts',(-0.443329663792386,54.1262312899774,
1.39582865019909));
#46419=CARTESIAN_POINT('Ctrl Pts',(-0.495268640925472,54.1232296908104,
1.37714967353438));
#46420=CARTESIAN_POINT('Ctrl Pts',(-0.547307525869696,54.1202223178832,
1.35843476671132));
#46421=CARTESIAN_POINT('Ctrl Pts',(-0.598218933261884,54.117214944956,1.33678964809974));
#46422=CARTESIAN_POINT('Ctrl Pts',(-0.647663797226496,54.1142075720288,
1.31238860699191));
#46423=CARTESIAN_POINT('Ctrl Pts',(-0.687817211863172,54.1117653306628,
1.29257289626671));
#46424=CARTESIAN_POINT('Ctrl Pts',(-0.727003801605313,54.1093230892967,
1.27094067101378));
#46425=CARTESIAN_POINT('Ctrl Pts',(-0.765056054817736,54.1068808479306,
1.24760630127726));
#46426=CARTESIAN_POINT('Ctrl Pts',(-0.811928495705812,54.1038725158504,
1.21886322369838));
#46427=CARTESIAN_POINT('Ctrl Pts',(-0.857278827777476,54.1008641837701,
1.18741368394173));
#46428=CARTESIAN_POINT('Ctrl Pts',(-0.900776746638556,54.0978558516899,
1.15344419141771));
#46429=CARTESIAN_POINT('Ctrl Pts',(-0.94419651202103,54.094852924733,1.11953573248052));
#46430=CARTESIAN_POINT('Ctrl Pts',(-0.985770055459424,54.0918499977761,
1.0831166283029));
#46431=CARTESIAN_POINT('Ctrl Pts',(-1.02519511111212,54.0888470708192,1.0444171743857));
#46432=CARTESIAN_POINT('Ctrl Pts',(-1.06458068952564,54.0858471507639,1.00575647114553));
#46433=CARTESIAN_POINT('Ctrl Pts',(-1.10182166599974,54.0828472307087,0.964820309688656));
#46434=CARTESIAN_POINT('Ctrl Pts',(-1.13664947559035,54.0798473106535,0.921878636068854));
#46435=CARTESIAN_POINT('Ctrl Pts',(-1.17145621620474,54.0768492053906,0.878962939882364));
#46436=CARTESIAN_POINT('Ctrl Pts',(-1.20385235072037,54.0738511001278,0.834044545944874));
#46437=CARTESIAN_POINT('Ctrl Pts',(-1.23360837557169,54.070852994865,0.787427854294844));
#46438=CARTESIAN_POINT('Ctrl Pts',(-1.26335819355787,54.0678555149826,0.740820886508129));
#46439=CARTESIAN_POINT('Ctrl Pts',(-1.29046871093687,54.0648580351001,0.692516769945924));
#46440=CARTESIAN_POINT('Ctrl Pts',(-1.31475402529904,54.0618605552177,0.642848429227278));
#46441=CARTESIAN_POINT('Ctrl Pts',(-1.33906180034197,54.0588603030657,0.593134151909713));
#46442=CARTESIAN_POINT('Ctrl Pts',(-1.36053891866768,54.0558600509137,0.542053605584976));
#46443=CARTESIAN_POINT('Ctrl Pts',(-1.37904640930907,54.0528597987617,0.489962499556597));
#46444=CARTESIAN_POINT('Ctrl Pts',(-1.39756220822633,54.0498581997538,0.437848009089597));
#46445=CARTESIAN_POINT('Ctrl Pts',(-1.41310557308966,54.0468566007459,0.384722563097819));
#46446=CARTESIAN_POINT('Ctrl Pts',(-1.42558755326905,54.043855001738,0.33095676147248));
#46447=CARTESIAN_POINT('Ctrl Pts',(-1.43809354329804,54.0408476289715,0.277087538050962));
#46448=CARTESIAN_POINT('Ctrl Pts',(-1.44752629341353,54.0378402562049,0.222576020707));
#46449=CARTESIAN_POINT('Ctrl Pts',(-1.45384829802984,54.0348328834384,0.167801598072695));
#46450=CARTESIAN_POINT('Ctrl Pts',(-1.45898230369712,54.0323906408644,0.123320106315844));
#46451=CARTESIAN_POINT('Ctrl Pts',(-1.46206581984142,54.0299483982904,0.0786654767993697));
#46452=CARTESIAN_POINT('Ctrl Pts',(-1.46310406195348,54.0275061557164,0.0340404743685822));
#46453=CARTESIAN_POINT('Ctrl Pts',(-1.46336637553979,54.0268891190919,0.0227658937181583));
#46454=CARTESIAN_POINT('Ctrl Pts',(-1.46349836980657,54.0262720824674,0.0114882693004367));
#46455=CARTESIAN_POINT('Ctrl Pts',(-1.4634999849931,54.0256550458429,0.000209583410763473));
#46456=CARTESIAN_POINT('Origin',(0.,55.715,0.));
#46457=CARTESIAN_POINT('',(-1.46349946337466,53.4543449820144,0.00125327654337655));
#46458=CARTESIAN_POINT('',(-1.46349952908363,53.5256550458752,0.00117404088105176));
#46459=CARTESIAN_POINT('',(-1.4635,55.715,-1.79227059055215E-16));
#46460=CARTESIAN_POINT('Ctrl Pts',(-1.46349946337466,53.4543449820144,0.00125327654337655));
#46461=CARTESIAN_POINT('Ctrl Pts',(-1.46344247146976,53.457956593816,0.0678049268389159));
#46462=CARTESIAN_POINT('Ctrl Pts',(-1.45884204417911,53.4615682056176,0.134158530349188));
#46463=CARTESIAN_POINT('Ctrl Pts',(-1.44980166704424,53.4651798174191,0.199768306384531));
#46464=CARTESIAN_POINT('Ctrl Pts',(-1.44062889273595,53.4688443216152,0.266338943760728));
#46465=CARTESIAN_POINT('Ctrl Pts',(-1.42688524973019,53.4725088258113,0.332143813274635));
#46466=CARTESIAN_POINT('Ctrl Pts',(-1.40872749801776,53.4761733300074,0.396634701367167));
#46467=CARTESIAN_POINT('Ctrl Pts',(-1.40552582568331,53.4768194750748,0.408006081232914));
#46468=CARTESIAN_POINT('Ctrl Pts',(-1.40218703503298,53.4774656201422,0.419336662599626));
#46469=CARTESIAN_POINT('Ctrl Pts',(-1.39871213746661,53.4781117652096,0.430623509000147));
#46470=CARTESIAN_POINT('Ctrl Pts',(-1.3825336556066,53.4811200974129,0.4831729831241));
#46471=CARTESIAN_POINT('Ctrl Pts',(-1.36335513237752,53.4841284296161,0.534921516347173));
#46472=CARTESIAN_POINT('Ctrl Pts',(-1.34127504032735,53.4871367618194,0.585502789228946));
#46473=CARTESIAN_POINT('Ctrl Pts',(-1.31923461994155,53.4901396889028,0.635993181906195));
#46474=CARTESIAN_POINT('Ctrl Pts',(-1.2943031858894,53.4931426159861,0.685319995328997));
#46475=CARTESIAN_POINT('Ctrl Pts',(-1.2666285956018,53.4961455430694,0.733133173989421));
#46476=CARTESIAN_POINT('Ctrl Pts',(-1.23898171651536,53.4991454632531,0.780898476218864));
#46477=CARTESIAN_POINT('Ctrl Pts',(-1.20859738564374,53.5021453834368,0.827152690447797));
#46478=CARTESIAN_POINT('Ctrl Pts',(-1.17567024846075,53.5051453036205,0.871568538259749));
#46479=CARTESIAN_POINT('Ctrl Pts',(-1.14276303042778,53.5081434090135,0.915957516868622));
#46480=CARTESIAN_POINT('Ctrl Pts',(-1.107316369079,53.5111415144066,0.958509909163623));
#46481=CARTESIAN_POINT('Ctrl Pts',(-1.06956799832171,53.5141396197996,0.99892769856786));
#46482=CARTESIAN_POINT('Ctrl Pts',(-1.03182750154829,53.5171370998138,1.03933705717058));
#46483=CARTESIAN_POINT('Ctrl Pts',(-0.991786609455625,53.520134579828,1.07761231066859));
#46484=CARTESIAN_POINT('Ctrl Pts',(-0.949721530805348,53.5231320598421,
1.11349057648673));
#46485=CARTESIAN_POINT('Ctrl Pts',(-0.907617547543504,53.5261323121273,
1.14940202493617));
#46486=CARTESIAN_POINT('Ctrl Pts',(-0.863486040390983,53.5291325644124,
1.18291171218449));
#46487=CARTESIAN_POINT('Ctrl Pts',(-0.817636962037858,53.5321328166975,
1.21379654321039));
#46488=CARTESIAN_POINT('Ctrl Pts',(-0.771767301367409,53.5351344158395,
1.24469523888562));
#46489=CARTESIAN_POINT('Ctrl Pts',(-0.724178987950642,53.5381360149815,
1.27296645867143));
#46490=CARTESIAN_POINT('Ctrl Pts',(-0.675208840953914,53.5411376141234,
1.29843185077141));
#46491=CARTESIAN_POINT('Ctrl Pts',(-0.626144496900949,53.5441449870239,
1.32394622710197));
#46492=CARTESIAN_POINT('Ctrl Pts',(-0.575693492577419,53.5471523599244,
1.34664377545156));
#46493=CARTESIAN_POINT('Ctrl Pts',(-0.524213958059398,53.5501597328249,
1.36639378517897));
#46494=CARTESIAN_POINT('Ctrl Pts',(-0.482408215485274,53.5526019743579,
1.38243246599126));
#46495=CARTESIAN_POINT('Ctrl Pts',(-0.439924658865493,53.555044215891,1.39652819935841));
#46496=CARTESIAN_POINT('Ctrl Pts',(-0.396960975376122,53.557486457424,1.40863559305749));
#46497=CARTESIAN_POINT('Ctrl Pts',(-0.34403867802658,53.5604947896273,1.42354937691938));
#46498=CARTESIAN_POINT('Ctrl Pts',(-0.290161887486237,53.5635031218305,
1.43550838544453));
#46499=CARTESIAN_POINT('Ctrl Pts',(-0.235691761507292,53.5665114540337,
1.44439663650868));
#46500=CARTESIAN_POINT('Ctrl Pts',(-0.181319502899288,53.569514381117,1.453268917906));
#46501=CARTESIAN_POINT('Ctrl Pts',(-0.126356541991729,53.5725173082003,
1.45908130592402));
#46502=CARTESIAN_POINT('Ctrl Pts',(-0.0711771619183304,53.5755202352836,
1.46176812854202));
#46503=CARTESIAN_POINT('Ctrl Pts',(-0.0160530342221854,53.5785201554673,
1.46445226078299));
#46504=CARTESIAN_POINT('Ctrl Pts',(0.0392865578033683,53.5815200756509,
1.46401700136158));
#46505=CARTESIAN_POINT('Ctrl Pts',(0.0944610859346182,53.5845199958345,
1.46044833980667));
#46506=CARTESIAN_POINT('Ctrl Pts',(0.149602236438777,53.5875181012275,1.45688183710039));
#46507=CARTESIAN_POINT('Ctrl Pts',(0.20457799425863,53.5905162066205,1.4501857230921));
#46508=CARTESIAN_POINT('Ctrl Pts',(0.259009040695779,53.5935143120135,1.44039805846782));
#46509=CARTESIAN_POINT('Ctrl Pts',(0.313428733287042,53.5965117920276,1.43061243546579));
#46510=CARTESIAN_POINT('Ctrl Pts',(0.367303419860547,53.5995092720417,1.41773663582437));
#46511=CARTESIAN_POINT('Ctrl Pts',(0.42026242700844,53.6025067520558,1.40186010088203));
#46512=CARTESIAN_POINT('Ctrl Pts',(0.473270414204989,53.6055070043408,1.38596888225327));
#46513=CARTESIAN_POINT('Ctrl Pts',(0.525360522100424,53.6085072566259,1.36707153528687));
#46514=CARTESIAN_POINT('Ctrl Pts',(0.576177198252906,53.6115075089109,1.3453074318584));
#46515=CARTESIAN_POINT('Ctrl Pts',(0.627016686749469,53.6145091080528,1.32353355820775));
#46516=CARTESIAN_POINT('Ctrl Pts',(0.67658112942205,53.6175107071947,1.29889059847301));
#46517=CARTESIAN_POINT('Ctrl Pts',(0.724537988649745,53.6205123063366,1.27156476555596));
#46518=CARTESIAN_POINT('Ctrl Pts',(0.772587095812953,53.623519679237,1.2441863697373));
#46519=CARTESIAN_POINT('Ctrl Pts',(0.819021996490471,53.6265270521374,1.21411507882206));
#46520=CARTESIAN_POINT('Ctrl Pts',(0.863538615996965,53.6295344250378,1.1815808515214));
#46521=CARTESIAN_POINT('Ctrl Pts',(0.899689881798259,53.6319766665712,1.15516030315487));
#46522=CARTESIAN_POINT('Ctrl Pts',(0.934576570746223,53.6344189081046,1.12711638728839));
#46523=CARTESIAN_POINT('Ctrl Pts',(0.968053314844246,53.6368611496381,1.09759055645494));
#46524=CARTESIAN_POINT('Ctrl Pts',(1.00928968151939,53.6398694818428,1.0612208909023));
#46525=CARTESIAN_POINT('Ctrl Pts',(1.04856152653202,53.6428778140476,1.02244656129843));
#46526=CARTESIAN_POINT('Ctrl Pts',(1.08557550615083,53.6458861462524,0.981508059287019));
#46527=CARTESIAN_POINT('Ctrl Pts',(1.12252298214399,53.6488890733373,0.940643112155147));
#46528=CARTESIAN_POINT('Ctrl Pts',(1.15722029123299,53.6518920004221,0.897622097857804));
#46529=CARTESIAN_POINT('Ctrl Pts',(1.1894092349799,53.654894927507,0.852723825012847));
#46530=CARTESIAN_POINT('Ctrl Pts',(1.22156594720012,53.6578948476922,0.807870509836911));
#46531=CARTESIAN_POINT('Ctrl Pts',(1.25121896263647,53.6608947678774,0.761144087175086));
#46532=CARTESIAN_POINT('Ctrl Pts',(1.27815009566093,53.6638946880625,0.71285663563016));
#46533=CARTESIAN_POINT('Ctrl Pts',(1.3050649367959,53.6668927934571,0.664598395400761));
#46534=CARTESIAN_POINT('Ctrl Pts',(1.32926090181372,53.6698908988516,0.61478145881872));
#46535=CARTESIAN_POINT('Ctrl Pts',(1.35056420572131,53.6728890042462,0.563745134102613));
#46536=CARTESIAN_POINT('Ctrl Pts',(1.37186306594379,53.6758864842619,0.512719455122817));
#46537=CARTESIAN_POINT('Ctrl Pts',(1.3902702594988,53.6788839642775,0.460475380835802));
#46538=CARTESIAN_POINT('Ctrl Pts',(1.40565985543317,53.6818814442932,0.407372827792434));
#46539=CARTESIAN_POINT('Ctrl Pts',(1.42106368469994,53.6848816965798,0.354221161939852));
#46540=CARTESIAN_POINT('Ctrl Pts',(1.43344419239104,53.6878819488664,0.300209940002899));
#46541=CARTESIAN_POINT('Ctrl Pts',(1.44272559606006,53.690882201153,0.245713460097595));
#46542=CARTESIAN_POINT('Ctrl Pts',(1.452011166286,53.6938838002965,0.191192515930983));
#46543=CARTESIAN_POINT('Ctrl Pts',(1.45819479984448,53.6968853994399,0.13618640608039));
#46544=CARTESIAN_POINT('Ctrl Pts',(1.46125254930464,53.6998869985833,0.0810755027778488));
#46545=CARTESIAN_POINT('Ctrl Pts',(1.46431618053183,53.7028943714852,0.0258585903015235));
#46546=CARTESIAN_POINT('Ctrl Pts',(1.46424191570225,53.7059017443871,-0.0294629880018957));
#46547=CARTESIAN_POINT('Ctrl Pts',(1.46105799743672,53.708909117289,-0.0845090416831317));
#46548=CARTESIAN_POINT('Ctrl Pts',(1.45847238612692,53.7113513588101,-0.12921109967839));
#46549=CARTESIAN_POINT('Ctrl Pts',(1.45383703455088,53.7137936003313,-0.173731384701363));
#46550=CARTESIAN_POINT('Ctrl Pts',(1.4471919216604,53.7162358418524,-0.21787104415427));
#46551=CARTESIAN_POINT('Ctrl Pts',(1.43900652848005,53.719244174054,-0.272241898859626));
#46552=CARTESIAN_POINT('Ctrl Pts',(1.42773535304935,53.7222525062556,-0.326266773180041));
#46553=CARTESIAN_POINT('Ctrl Pts',(1.41342130756537,53.7252608384572,-0.379568778115642));
#46554=CARTESIAN_POINT('Ctrl Pts',(1.39913298036218,53.7282637655389,-0.432775014462888));
#46555=CARTESIAN_POINT('Ctrl Pts',(1.38181276825587,53.7312666926206,-0.48526045221439));
#46556=CARTESIAN_POINT('Ctrl Pts',(1.3615548375873,53.7342696197023,-0.536656942788047));
#46557=CARTESIAN_POINT('Ctrl Pts',(1.34131719164868,53.7372695398843,-0.588001968878557));
#46558=CARTESIAN_POINT('Ctrl Pts',(1.31814784685433,53.7402694600663,-0.638259718085283));
#46559=CARTESIAN_POINT('Ctrl Pts',(1.2921906241153,53.7432693802484,-0.687077609115968));
#46560=CARTESIAN_POINT('Ctrl Pts',(1.26624910410221,53.7462674856398,-0.735865967943945));
#46561=CARTESIAN_POINT('Ctrl Pts',(1.23752329643222,53.7492655910312,-0.783215728889403));
#46562=CARTESIAN_POINT('Ctrl Pts',(1.20620398227689,53.7522636964226,-0.828796840690991));
#46563=CARTESIAN_POINT('Ctrl Pts',(1.17489120105964,53.7552611764351,-0.874368444666847));
#46564=CARTESIAN_POINT('Ctrl Pts',(1.14098628685266,53.7582586564477,-0.918171696367938));
#46565=CARTESIAN_POINT('Ctrl Pts',(1.1047232918858,53.7612561364602,-0.959905567420563));
#46566=CARTESIAN_POINT('Ctrl Pts',(1.06842675846383,53.7642563887437,-1.00167803676223));
#46567=CARTESIAN_POINT('Ctrl Pts',(1.02976813429827,53.7672566410273,-1.04137690120061));
#46568=CARTESIAN_POINT('Ctrl Pts',(0.989020756245025,53.7702568933108,-1.07873546048905));
#46569=CARTESIAN_POINT('Ctrl Pts',(0.948255086101592,53.7732584924512,-1.11611079057768));
#46570=CARTESIAN_POINT('Ctrl Pts',(0.905399203044032,53.7762600915916,-1.15114338577598));
#46571=CARTESIAN_POINT('Ctrl Pts',(0.860759664375077,53.779261690732,-1.18360679711841));
#46572=CARTESIAN_POINT('Ctrl Pts',(0.81603425883766,53.7822690636309,-1.2161326538076));
#46573=CARTESIAN_POINT('Ctrl Pts',(0.76951878908108,53.7852764365298,-1.24607916626769));
#46574=CARTESIAN_POINT('Ctrl Pts',(0.72154796991533,53.7882838094288,-1.27326382855678));
#46575=CARTESIAN_POINT('Ctrl Pts',(0.682591601186528,53.7907260509747,-1.29534007712453));
#46576=CARTESIAN_POINT('Ctrl Pts',(0.642676067438844,53.7931682925206,-1.31559575457021));
#46577=CARTESIAN_POINT('Ctrl Pts',(0.601990109420668,53.7956105340664,-1.33395658031275));
#46578=CARTESIAN_POINT('Ctrl Pts',(0.551873495075722,53.7986188662688,-1.35657328808163));
#46579=CARTESIAN_POINT('Ctrl Pts',(0.50037366940323,53.8016271984713,-1.37640998129086));
#46580=CARTESIAN_POINT('Ctrl Pts',(0.447830531129377,53.8046355306737,-1.39329826863755));
#46581=CARTESIAN_POINT('Ctrl Pts',(0.395381797976556,53.8076384577561,-1.41015621252049));
#46582=CARTESIAN_POINT('Ctrl Pts',(0.341893971407634,53.8106413848386,-1.4240761023605));
#46583=CARTESIAN_POINT('Ctrl Pts',(0.287727409941581,53.813644311921,-1.43493734621701));
#46584=CARTESIAN_POINT('Ctrl Pts',(0.233615086694667,53.8166442321038,-1.44578771446117));
#46585=CARTESIAN_POINT('Ctrl Pts',(0.17882589070928,53.8196441522865,-1.4535853998682));
#46586=CARTESIAN_POINT('Ctrl Pts',(0.123734037419925,53.8226440724693,-1.45825996927289));
#46587=CARTESIAN_POINT('Ctrl Pts',(0.0686755117441382,53.8256421778614,
-1.46293171081404));
#46588=CARTESIAN_POINT('Ctrl Pts',(0.0133152175354595,53.8286402832535,
-1.46448403616265));
#46589=CARTESIAN_POINT('Ctrl Pts',(-0.0419660837095952,53.8316383886456,
-1.46289818436489));
#46590=CARTESIAN_POINT('Ctrl Pts',(-0.0972358537526679,53.8346358686588,
-1.46131266336211));
#46591=CARTESIAN_POINT('Ctrl Pts',(-0.152426135183783,53.837633348672,-1.45659028011005));
#46592=CARTESIAN_POINT('Ctrl Pts',(-0.207157076226368,53.8406308286852,
-1.44876436861532));
#46593=CARTESIAN_POINT('Ctrl Pts',(-0.261938636120848,53.8436310809694,
-1.44093121919178));
#46594=CARTESIAN_POINT('Ctrl Pts',(-0.31625948206119,53.8466313332535,-1.42998888134765));
#46595=CARTESIAN_POINT('Ctrl Pts',(-0.369747291296459,53.8496315855377,
-1.41602231288173));
#46596=CARTESIAN_POINT('Ctrl Pts',(-0.423259111986075,53.8526331846786,
-1.40204947462041));
#46597=CARTESIAN_POINT('Ctrl Pts',(-0.475936646207775,53.8556347838196,
-1.38504986202171));
#46598=CARTESIAN_POINT('Ctrl Pts',(-0.52742336570976,53.8586363829606,-1.3651581751956));
#46599=CARTESIAN_POINT('Ctrl Pts',(-0.579009123048124,53.86164375586,-1.34522822550008));
#46600=CARTESIAN_POINT('Ctrl Pts',(-0.629399006339953,53.8646511287595,
-1.32239530631913));
#46601=CARTESIAN_POINT('Ctrl Pts',(-0.67825812959912,53.867658501659,-1.29684160930805));
#46602=CARTESIAN_POINT('Ctrl Pts',(-0.717935876406113,53.8701007431995,
-1.2760898427524));
#46603=CARTESIAN_POINT('Ctrl Pts',(-0.756604471036526,53.8725429847401,
-1.25354473055454));
#46604=CARTESIAN_POINT('Ctrl Pts',(-0.794099129575007,53.8749852262807,
-1.22932453908975));
#46605=CARTESIAN_POINT('Ctrl Pts',(-0.840283151242524,53.8779934557358,
-1.19949133374789));
#46606=CARTESIAN_POINT('Ctrl Pts',(-0.884882167445745,53.881001685191,-1.16698825815757));
#46607=CARTESIAN_POINT('Ctrl Pts',(-0.927570350766358,53.8840099146462,
-1.13200949394392));
#46608=CARTESIAN_POINT('Ctrl Pts',(-0.970181836005141,53.8870127391998,
-1.09709357625854));
#46609=CARTESIAN_POINT('Ctrl Pts',(-1.01088889550785,53.8900155637534,-1.05971112920328));
#46610=CARTESIAN_POINT('Ctrl Pts',(-1.04939475798609,53.893018388307,-1.0200994519709));
#46611=CARTESIAN_POINT('Ctrl Pts',(-1.08786206595882,53.8960182062427,-0.980527436455715));
#46612=CARTESIAN_POINT('Ctrl Pts',(-1.12413217573949,53.8990180241783,-0.93873098934721));
#46613=CARTESIAN_POINT('Ctrl Pts',(-1.15794293658584,53.902017842114,-0.894986260012392));
#46614=CARTESIAN_POINT('Ctrl Pts',(-1.19173324829453,53.9050158457253,-0.851267987993812));
#46615=CARTESIAN_POINT('Ctrl Pts',(-1.22306683623055,53.9080138493365,-0.805604186729965));
#46616=CARTESIAN_POINT('Ctrl Pts',(-1.25172140781955,53.9110118529477,-0.758304534607467));
#46617=CARTESIAN_POINT('Ctrl Pts',(-1.28037000832997,53.9140092318309,-0.711014738850777));
#46618=CARTESIAN_POINT('Ctrl Pts',(-1.30634042704404,53.9170066107141,-0.662090221203661));
#46619=CARTESIAN_POINT('Ctrl Pts',(-1.32945462939384,53.9200039895973,-0.611868154411794));
#46620=CARTESIAN_POINT('Ctrl Pts',(-1.35259021151039,53.923004140943,-0.561599634099379));
#46621=CARTESIAN_POINT('Ctrl Pts',(-1.37286407693083,53.9260042922888,-0.510031648127808));
#46622=CARTESIAN_POINT('Ctrl Pts',(-1.3901456441654,53.9290044436346,-0.457523046422747));
#46623=CARTESIAN_POINT('Ctrl Pts',(-1.40743497500246,53.9320059427737,-0.404990855658612));
#46624=CARTESIAN_POINT('Ctrl Pts',(-1.42172919100888,53.9350074419129,-0.351517718710409));
#46625=CARTESIAN_POINT('Ctrl Pts',(-1.43294806662417,53.9380089410521,-0.297476197968935));
#46626=CARTESIAN_POINT('Ctrl Pts',(-1.44418851681402,53.9410162122552,-0.24333075212318));
#46627=CARTESIAN_POINT('Ctrl Pts',(-1.45234173314682,53.9440234834582,-0.188615263369206));
#46628=CARTESIAN_POINT('Ctrl Pts',(-1.45737912717119,53.9470307546613,-0.133709871309992));
#46629=CARTESIAN_POINT('Ctrl Pts',(-1.46146306265128,53.9494688211507,-0.089196760444808));
#46630=CARTESIAN_POINT('Ctrl Pts',(-1.46350005182781,53.95190688764,-0.0445590499666518));
#46631=CARTESIAN_POINT('Ctrl Pts',(-1.46349999999901,53.9543449541294,1.70220316559402E-6));
#46632=CARTESIAN_POINT('Ctrl Pts',(-1.46349998499324,54.0256550457892,0.000209582428625436));
#46633=CARTESIAN_POINT('Ctrl Pts',(-1.46350782863152,54.0226585901551,-0.054562015460591));
#46634=CARTESIAN_POINT('Ctrl Pts',(-1.46043663080279,54.019662134521,-0.109454800121881));
#46635=CARTESIAN_POINT('Ctrl Pts',(-1.45427163563079,54.0166656788869,-0.164092229553177));
#46636=CARTESIAN_POINT('Ctrl Pts',(-1.44811761703811,54.0136745583475,-0.218632378765915));
#46637=CARTESIAN_POINT('Ctrl Pts',(-1.43888078854372,54.010683437808,-0.272917549034307));
#46638=CARTESIAN_POINT('Ctrl Pts',(-1.42659838444462,54.0076923172686,-0.326572043353398));
#46639=CARTESIAN_POINT('Ctrl Pts',(-1.41432808282349,54.0047041440325,-0.380173669168011));
#46640=CARTESIAN_POINT('Ctrl Pts',(-1.39901826673936,54.0017159707964,-0.433145332152493));
#46641=CARTESIAN_POINT('Ctrl Pts',(-1.38075760625046,53.9987277975603,-0.485119245940098));
#46642=CARTESIAN_POINT('Ctrl Pts',(-1.36250755088441,53.9957413597458,-0.537062975182055));
#46643=CARTESIAN_POINT('Ctrl Pts',(-1.34131022339059,53.9927549219313,-0.588009601014911));
#46644=CARTESIAN_POINT('Ctrl Pts',(-1.31730409443323,53.9897684841168,-0.637606597197248));
#46645=CARTESIAN_POINT('Ctrl Pts',(-1.29330219526639,53.9867825725015,-0.687194854573563));
#46646=CARTESIAN_POINT('Ctrl Pts',(-1.2664927100556,53.9837966608862,-0.735433474673621));
#46647=CARTESIAN_POINT('Ctrl Pts',(-1.23706120277647,53.9808107492709,-0.781992219005559));
#46648=CARTESIAN_POINT('Ctrl Pts',(-1.2076019815707,53.9778220259975,-0.828594804980147));
#46649=CARTESIAN_POINT('Ctrl Pts',(-1.17551609341556,53.9748333027241,-0.873513904364883));
#46650=CARTESIAN_POINT('Ctrl Pts',(-1.14103298148957,53.9718445794507,-0.916447480848212));
#46651=CARTESIAN_POINT('Ctrl Pts',(-1.10653286838508,53.9688543826497,-0.95940222483518));
#46652=CARTESIAN_POINT('Ctrl Pts',(-1.06963353541908,53.9658641858487,-1.00036909962799));
#46653=CARTESIAN_POINT('Ctrl Pts',(-1.03060314573366,53.9628739890477,-1.03908103918987));
#46654=CARTESIAN_POINT('Ctrl Pts',(-0.991500095299347,53.9598782255603,
-1.07786504665939));
#46655=CARTESIAN_POINT('Ctrl Pts',(-0.950258467416528,53.956882462073,-1.11438538372738));
#46656=CARTESIAN_POINT('Ctrl Pts',(-0.907180510680163,53.9538866985856,
-1.14841445961033));
#46657=CARTESIAN_POINT('Ctrl Pts',(-0.879594469150748,53.9519682868911,
-1.17020582511681));
#46658=CARTESIAN_POINT('Ctrl Pts',(-0.851256028304565,53.9500498751967,
-1.19097642150542));
#46659=CARTESIAN_POINT('Ctrl Pts',(-0.822250282559253,53.9481314635023,
-1.21067614283558));
#46660=CARTESIAN_POINT('Ctrl Pts',(-0.776765301853876,53.9451231313024,
-1.24156800310599));
#46661=CARTESIAN_POINT('Ctrl Pts',(-0.729439992864939,53.9421147991026,
-1.26995887430848));
#46662=CARTESIAN_POINT('Ctrl Pts',(-0.680580264189124,53.9391064669027,
-1.29562446488026));
#46663=CARTESIAN_POINT('Ctrl Pts',(-0.631808322587715,53.9361035398226,
-1.32124394166528));
#46664=CARTESIAN_POINT('Ctrl Pts',(-0.581507896484375,53.9331006127424,
-1.34414761068936));
#46665=CARTESIAN_POINT('Ctrl Pts',(-0.530013263328142,53.9300976856623,
-1.36415475320663));
#46666=CARTESIAN_POINT('Ctrl Pts',(-0.478570192925391,53.9270977654817,
-1.38414186211469));
#46667=CARTESIAN_POINT('Ctrl Pts',(-0.425935774579324,53.9240978453011,
-1.40123799899503));
#46668=CARTESIAN_POINT('Ctrl Pts',(-0.372466555339235,53.9210979251205,
-1.41530947681195));
#46669=CARTESIAN_POINT('Ctrl Pts',(-0.3190296821035,53.9180998197304,-1.42937244214095));
#46670=CARTESIAN_POINT('Ctrl Pts',(-0.264759519264145,53.9151017143403,
-1.44041424046975));
#46671=CARTESIAN_POINT('Ctrl Pts',(-0.210027941408102,53.9121036089502,
-1.44835096362307));
#46672=CARTESIAN_POINT('Ctrl Pts',(-0.155307780083542,53.9091061289389,
-1.45628603124492));
#46673=CARTESIAN_POINT('Ctrl Pts',(-0.100126917957422,53.9061086489275,
-1.46111723386381));
#46674=CARTESIAN_POINT('Ctrl Pts',(-0.0448652849060839,53.9031111689161,
-1.46281213975353));
#46675=CARTESIAN_POINT('Ctrl Pts',(0.0104474578217938,53.9001109166336,
-1.46450861320626));
#46676=CARTESIAN_POINT('Ctrl Pts',(0.0658405909274442,53.897110664351,-1.46306297791753));
#46677=CARTESIAN_POINT('Ctrl Pts',(0.120932731060135,53.8941104120684,-1.45849495184534));
#46678=CARTESIAN_POINT('Ctrl Pts',(0.17604960285729,53.8911088129289,-1.45392487511968));
#46679=CARTESIAN_POINT('Ctrl Pts',(0.230864687593562,53.8881072137894,-1.44622968698154));
#46680=CARTESIAN_POINT('Ctrl Pts',(0.285003614276744,53.8851056146498,-1.4354808218326));
#46681=CARTESIAN_POINT('Ctrl Pts',(0.339246680482899,53.8820982417515,-1.42471128058685));
#46682=CARTESIAN_POINT('Ctrl Pts',(0.392810476690926,53.8790908688532,-1.41087645977689));
#46683=CARTESIAN_POINT('Ctrl Pts',(0.445333791806705,53.8760834959549,-1.39409829778071));
#46684=CARTESIAN_POINT('Ctrl Pts',(0.487987173063869,53.8736412543993,-1.38047300891918));
#46685=CARTESIAN_POINT('Ctrl Pts',(0.529954562293615,53.8711990128437,-1.36490764486807));
#46686=CARTESIAN_POINT('Ctrl Pts',(0.57105330475754,53.8687567712881,-1.34749039815707));
#46687=CARTESIAN_POINT('Ctrl Pts',(0.621678383013754,53.8657484390993,-1.32603598313388));
#46688=CARTESIAN_POINT('Ctrl Pts',(0.671200678228524,53.8627401069105,-1.30167887558553));
#46689=CARTESIAN_POINT('Ctrl Pts',(0.719265826454129,53.8597317747218,-1.27455440091636));
#46690=CARTESIAN_POINT('Ctrl Pts',(0.76724461523034,53.8567288476533,-1.24747866124093));
#46691=CARTESIAN_POINT('Ctrl Pts',(0.813770995584772,53.8537259205849,-1.21764567905283));
#46692=CARTESIAN_POINT('Ctrl Pts',(0.858511820184278,53.8507229935165,-1.18523824803449));
#46693=CARTESIAN_POINT('Ctrl Pts',(0.903207844767272,53.847723073348,-1.15286326732207));
#46694=CARTESIAN_POINT('Ctrl Pts',(0.946121428957106,53.8447231531795,-1.11791925269181));
#46695=CARTESIAN_POINT('Ctrl Pts',(0.986946856329365,53.841723233011,-1.08063321843333));
#46696=CARTESIAN_POINT('Ctrl Pts',(1.0277475865069,53.8387251276333,-1.04336974022651));
#46697=CARTESIAN_POINT('Ctrl Pts',(1.06646227372821,53.8357270222557,-1.00376740626566));
#46698=CARTESIAN_POINT('Ctrl Pts',(1.10281870602089,53.832728916878,-0.962093109657488));
#46699=CARTESIAN_POINT('Ctrl Pts',(1.13916755467355,53.8297314368795,-0.920427505950224));
#46700=CARTESIAN_POINT('Ctrl Pts',(1.17315877763142,53.8267339568809,-0.876691196053912));
#46701=CARTESIAN_POINT('Ctrl Pts',(1.20455903829702,53.8237364768823,-0.831185763386839));
#46702=CARTESIAN_POINT('Ctrl Pts',(1.235988340032,53.820736224613,-0.785638244240252));
#46703=CARTESIAN_POINT('Ctrl Pts',(1.26482159042764,53.8177359723437,-0.738318769322307));
#46704=CARTESIAN_POINT('Ctrl Pts',(1.29086847496074,53.8147357200743,-0.689558431427348));
#46705=CARTESIAN_POINT('Ctrl Pts',(1.31692705231761,53.8117341209483,-0.640776204310375));
#46706=CARTESIAN_POINT('Ctrl Pts',(1.34019654748639,53.8087325218223,-0.590552305532093));
#46707=CARTESIAN_POINT('Ctrl Pts',(1.36053389630347,53.8057309226962,-0.539239990179977));
#46708=CARTESIAN_POINT('Ctrl Pts',(1.38091036524808,53.8027235498117,-0.487828972468046));
#46709=CARTESIAN_POINT('Ctrl Pts',(1.39834325257721,53.7997161769272,-0.435325858756278));
#46710=CARTESIAN_POINT('Ctrl Pts',(1.41273906060424,53.7967088040426,-0.382100244233165));
#46711=CARTESIAN_POINT('Ctrl Pts',(1.42442967676295,53.7942665623864,-0.338876534384224));
#46712=CARTESIAN_POINT('Ctrl Pts',(1.43411833936465,53.7918243207301,-0.295176736857024));
#46713=CARTESIAN_POINT('Ctrl Pts',(1.4417800580858,53.7893820790739,-0.251202137940935));
#46714=CARTESIAN_POINT('Ctrl Pts',(1.45121769713886,53.7863737468613,-0.197034606192844));
#46715=CARTESIAN_POINT('Ctrl Pts',(1.45761861003363,53.7833654146488,-0.14221896263965));
#46716=CARTESIAN_POINT('Ctrl Pts',(1.46090425961526,53.7803570824363,-0.0871263119728763));
#46717=CARTESIAN_POINT('Ctrl Pts',(1.46418400581649,53.7773541553435,-0.0321326471735748));
#46718=CARTESIAN_POINT('Ctrl Pts',(1.46435956471138,53.7743512282507,0.0231365135285706));
#46719=CARTESIAN_POINT('Ctrl Pts',(1.46140378568201,53.7713483011579,0.0783021404196221));
#46720=CARTESIAN_POINT('Ctrl Pts',(1.45845096634177,53.7683483809647,0.133412528706947));
#46721=CARTESIAN_POINT('Ctrl Pts',(1.45237304800998,53.7653484607715,0.188419063081002));
#46722=CARTESIAN_POINT('Ctrl Pts',(1.44319490917644,53.7623485405783,0.242941771062965));
#46723=CARTESIAN_POINT('Ctrl Pts',(1.4340223226238,53.7593504351756,0.297431495735774));
#46724=CARTESIAN_POINT('Ctrl Pts',(1.42175332016554,53.756352329773,0.351437453626223));
#46725=CARTESIAN_POINT('Ctrl Pts',(1.40646445646018,53.7533542243703,0.404586187003662));
#46726=CARTESIAN_POINT('Ctrl Pts',(1.39117878187926,53.7503567443464,0.457723834016046));
#46727=CARTESIAN_POINT('Ctrl Pts',(1.37287464291517,53.7473592643226,0.510004103570024));
#46728=CARTESIAN_POINT('Ctrl Pts',(1.35167882500509,53.7443617842987,0.561067379227193));
#46729=CARTESIAN_POINT('Ctrl Pts',(1.33046340377805,53.7413615320039,0.612177881633607));
#46730=CARTESIAN_POINT('Ctrl Pts',(1.30635116309793,53.738361279709,0.662068651624444));
#46731=CARTESIAN_POINT('Ctrl Pts',(1.27951701607627,53.7353610274142,0.710400208031552));
#46732=CARTESIAN_POINT('Ctrl Pts',(1.25267082281594,53.7323594282625,0.758753461176909));
#46733=CARTESIAN_POINT('Ctrl Pts',(1.22310057038838,53.7293578291107,0.805545657443051));
#46734=CARTESIAN_POINT('Ctrl Pts',(1.19102542096925,53.726356229959,0.850464988465146));
#46735=CARTESIAN_POINT('Ctrl Pts',(1.15888857305027,53.7233488570489,0.895470724551247));
#46736=CARTESIAN_POINT('Ctrl Pts',(1.12423753408622,53.7203414841387,0.938595984611326));
#46737=CARTESIAN_POINT('Ctrl Pts',(1.08733208050887,53.7173341112285,0.979561737051965));
#46738=CARTESIAN_POINT('Ctrl Pts',(1.05736172718687,53.7148918697723,1.01282939686202));
#46739=CARTESIAN_POINT('Ctrl Pts',(1.0259054676592,53.712449628316,1.04467348410061));
#46740=CARTESIAN_POINT('Ctrl Pts',(0.993118844906541,53.7100073868598,1.07496381794528));
#46741=CARTESIAN_POINT('Ctrl Pts',(0.952732562551795,53.7069990546575,1.11227519290754));
#46742=CARTESIAN_POINT('Ctrl Pts',(0.910154550746728,53.7039907224552,1.14738700506166));
#46743=CARTESIAN_POINT('Ctrl Pts',(0.865653969298483,53.7009823902529,1.18003197220998));
#46744=CARTESIAN_POINT('Ctrl Pts',(0.821233342776419,53.6979794631706,1.21261828560922));
#46745=CARTESIAN_POINT('Ctrl Pts',(0.774897424288765,53.6949765360882,1.24274623911318));
#46746=CARTESIAN_POINT('Ctrl Pts',(0.726949905745565,53.6919736090058,1.27018742102751));
#46747=CARTESIAN_POINT('Ctrl Pts',(0.679050398150856,53.6889736888231,1.29760112545789));
#46748=CARTESIAN_POINT('Ctrl Pts',(0.629542943692324,53.6859737686404,1.32233312593508));
#46749=CARTESIAN_POINT('Ctrl Pts',(0.57876024920718,53.6829738484577,1.34419820857552));
#46750=CARTESIAN_POINT('Ctrl Pts',(0.528008275525374,53.6799757430656,1.36605006401503));
#46751=CARTESIAN_POINT('Ctrl Pts',(0.475983075522737,53.6769776376736,1.3850382301616));
#46752=CARTESIAN_POINT('Ctrl Pts',(0.423039914520692,53.6739795322815,1.40102443973056));
#46753=CARTESIAN_POINT('Ctrl Pts',(0.370107797004325,53.6709820522683,1.4170073147144));
#46754=CARTESIAN_POINT('Ctrl Pts',(0.316258604698278,53.6679845722551,1.42998932364978));
#46755=CARTESIAN_POINT('Ctrl Pts',(0.261863222396774,53.6649870922418,1.43988190583672));
#46756=CARTESIAN_POINT('Ctrl Pts',(0.207417531589752,53.6619868399577,1.44978363734855));
#46757=CARTESIAN_POINT('Ctrl Pts',(0.15242516295222,53.6589865876735,1.45659013812067));
#46758=CARTESIAN_POINT('Ctrl Pts',(0.0972661924160646,53.6559863353893,
1.46026420137346));
#46759=CARTESIAN_POINT('Ctrl Pts',(0.0420824602165115,53.6529847362482,
1.46393991396664));
#46760=CARTESIAN_POINT('Ctrl Pts',(-0.0132674931339486,53.6499831371072,
1.46448038058406));
#46761=CARTESIAN_POINT('Ctrl Pts',(-0.0684028367148747,53.6469815379662,
1.46190057867468));
#46762=CARTESIAN_POINT('Ctrl Pts',(-0.123644236483194,53.6439741650666,
1.45931581435939));
#46763=CARTESIAN_POINT('Ctrl Pts',(-0.178669674239935,53.640966792167,1.45359884523322));
#46764=CARTESIAN_POINT('Ctrl Pts',(-0.233103823558772,53.6379594192674,
1.44481654802341));
#46765=CARTESIAN_POINT('Ctrl Pts',(-0.277308963770685,53.6355171777268,
1.43768457876514));
#46766=CARTESIAN_POINT('Ctrl Pts',(-0.321124194878841,53.6330749361862,
1.42853210273926));
#46767=CARTESIAN_POINT('Ctrl Pts',(-0.364355779586917,53.6306326946455,
1.41741917437348));
#46768=CARTESIAN_POINT('Ctrl Pts',(-0.417608075171855,53.6276243624437,
1.40373036444101));
#46769=CARTESIAN_POINT('Ctrl Pts',(-0.470201429048979,53.624616030242,1.38700715994846));
#46770=CARTESIAN_POINT('Ctrl Pts',(-0.52176529539383,53.6216076980402,1.36733069391519));
#46771=CARTESIAN_POINT('Ctrl Pts',(-0.573236516091384,53.6186047709584,
1.34768958091227));
#46772=CARTESIAN_POINT('Ctrl Pts',(-0.623681429787296,53.6156018438765,
1.32510592298748));
#46773=CARTESIAN_POINT('Ctrl Pts',(-0.672743413675605,53.6125989167947,
1.29971094838664));
#46774=CARTESIAN_POINT('Ctrl Pts',(-0.721756270675137,53.6095989966126,
1.27434140235581));
#46775=CARTESIAN_POINT('Ctrl Pts',(-0.769388473490375,53.6065990764305,
1.24616635757713));
#46776=CARTESIAN_POINT('Ctrl Pts',(-0.815303950431102,53.6035991562484,
1.21536484991604));
#46777=CARTESIAN_POINT('Ctrl Pts',(-0.861191650973091,53.600601050857,1.18458197551362));
#46778=CARTESIAN_POINT('Ctrl Pts',(-0.905364245588497,53.5976029454656,
1.15117608123266));
#46779=CARTESIAN_POINT('Ctrl Pts',(-0.947512865291517,53.5946048400741,
1.11537062006629));
#46780=CARTESIAN_POINT('Ctrl Pts',(-0.9896526931564,53.5916073600616,1.07957262760996));
#46781=CARTESIAN_POINT('Ctrl Pts',(-1.02976898153332,53.5886098800491,1.04137640431734));
#46782=CARTESIAN_POINT('Ctrl Pts',(-1.06758614681198,53.5856124000365,1.00104548804495));
#46783=CARTESIAN_POINT('Ctrl Pts',(-1.10543828794615,53.5826121477531,0.960677271031219));
#46784=CARTESIAN_POINT('Ctrl Pts',(-1.14098669472224,53.5796118954696,0.91817080286692));
#46785=CARTESIAN_POINT('Ctrl Pts',(-1.17399393983496,53.5766116431861,0.873825199471148));
#46786=CARTESIAN_POINT('Ctrl Pts',(-1.20701600237928,53.5736100440459,0.82945968869011));
#46787=CARTESIAN_POINT('Ctrl Pts',(-1.2374943373654,53.5706084449056,0.78325383910798));
#46788=CARTESIAN_POINT('Ctrl Pts',(-1.26523494747296,53.5676068457653,0.735535707966041));
#46789=CARTESIAN_POINT('Ctrl Pts',(-1.29302891833125,53.5645994728665,0.687725788096614));
#46790=CARTESIAN_POINT('Ctrl Pts',(-1.31807440322412,53.5615920999678,0.638398247899321));
#46791=CARTESIAN_POINT('Ctrl Pts',(-1.34022399085555,53.558584727069,0.587904672829887));
#46792=CARTESIAN_POINT('Ctrl Pts',(-1.3582113322855,53.5561424855231,0.546899612604587));
#46793=CARTESIAN_POINT('Ctrl Pts',(-1.3742897590747,53.5537002439772,0.505126098320758));
#46794=CARTESIAN_POINT('Ctrl Pts',(-1.38840463064804,53.5512580024313,0.46277946323825));
#46795=CARTESIAN_POINT('Ctrl Pts',(-1.4090478451279,53.5476861870038,0.400846864987792));
#46796=CARTESIAN_POINT('Ctrl Pts',(-1.42556244976633,53.5441143715763,0.337473458473622));
#46797=CARTESIAN_POINT('Ctrl Pts',(-1.43777994548423,53.5405425561488,0.273168589635323));
#46798=CARTESIAN_POINT('Ctrl Pts',(-1.44985697291845,53.5370118069753,0.209603053534845));
#46799=CARTESIAN_POINT('Ctrl Pts',(-1.45773505299724,53.5334810578018,0.145127443764852));
#46800=CARTESIAN_POINT('Ctrl Pts',(-1.46129787737112,53.5299503086283,0.0802543680472647));
#46801=CARTESIAN_POINT('Ctrl Pts',(-1.46274263843805,53.5285185543773,0.0539476842892827));
#46802=CARTESIAN_POINT('Ctrl Pts',(-1.46347834914557,53.5270868001262,0.0275758722661284));
#46803=CARTESIAN_POINT('Ctrl Pts',(-1.46349952908363,53.5256550458752,0.00117404088105226));
#46804=CARTESIAN_POINT('Origin',(0.,55.715,0.));
#46805=CARTESIAN_POINT('',(-1.46345008434496,52.9543449205092,-0.000748272696638112));
#46806=CARTESIAN_POINT('',(-1.46349972639677,53.0256550458429,-0.000894894726806227));
#46807=CARTESIAN_POINT('',(-1.4635,55.715,-1.79227059055215E-16));
#46808=CARTESIAN_POINT('Ctrl Pts',(-1.4614949149962,52.9543449541571,-0.000746652183517826));
#46809=CARTESIAN_POINT('Ctrl Pts',(-1.46014398544565,52.9701845067463,0.291491935245273));
#46810=CARTESIAN_POINT('Ctrl Pts',(-1.23353547905525,53.0124822900733,1.07381215251494));
#46811=CARTESIAN_POINT('Ctrl Pts',(0.0411507811327844,53.081238304139,1.72924034556294));
#46812=CARTESIAN_POINT('Ctrl Pts',(1.47504206610459,53.160612996353,0.903446989440327));
#46813=CARTESIAN_POINT('Ctrl Pts',(1.55910697444425,53.2399876885673,-0.749100127985283));
#46814=CARTESIAN_POINT('Ctrl Pts',(0.216416831887046,53.3193623807813,-1.71613790657862));
#46815=CARTESIAN_POINT('Ctrl Pts',(-1.17054009011867,53.3908148026447,-1.17294623829698));
#46816=CARTESIAN_POINT('Ctrl Pts',(-1.4597932078458,53.4358089937699,-0.340099651390323));
#46817=CARTESIAN_POINT('Ctrl Pts',(-1.46257561148105,53.4543449541571,0.00125197239151345));
#46818=CARTESIAN_POINT('Ctrl Pts',(-1.46349952908411,53.5256550458429,0.00117404028541898));
#46819=CARTESIAN_POINT('Ctrl Pts',(-1.46354376834028,53.5226644905813,-0.0539723898429259));
#46820=CARTESIAN_POINT('Ctrl Pts',(-1.46046671848057,53.5196739353198,-0.109161561176566));
#46821=CARTESIAN_POINT('Ctrl Pts',(-1.45428048852627,53.5166833800582,-0.164013751532615));
#46822=CARTESIAN_POINT('Ctrl Pts',(-1.44809574892989,53.5136935452674,-0.218852727152532));
#46823=CARTESIAN_POINT('Ctrl Pts',(-1.43880337509673,53.5107037104765,-0.273354355238613));
#46824=CARTESIAN_POINT('Ctrl Pts',(-1.42646732953524,53.5077138756857,-0.327144016861991));
#46825=CARTESIAN_POINT('Ctrl Pts',(-1.41411960847097,53.504721211153,-0.380984587939385));
#46826=CARTESIAN_POINT('Ctrl Pts',(-1.39872257657072,53.5017285466204,-0.434111326458504));
#46827=CARTESIAN_POINT('Ctrl Pts',(-1.38039106058168,53.4987358820877,-0.486161259116953));
#46828=CARTESIAN_POINT('Ctrl Pts',(-1.36205174102466,53.4957419436036,-0.538233348982043));
#46829=CARTESIAN_POINT('Ctrl Pts',(-1.34077565159835,53.4927480051194,-0.589227227488573));
#46830=CARTESIAN_POINT('Ctrl Pts',(-1.31672591829994,53.4897540666353,-0.638799738632687));
#46831=CARTESIAN_POINT('Ctrl Pts',(-1.29262661862144,53.4867539576589,-0.688474418474416));
#46832=CARTESIAN_POINT('Ctrl Pts',(-1.26574251017182,53.4837538486826,-0.736721410432874));
#46833=CARTESIAN_POINT('Ctrl Pts',(-1.23628238045958,53.4807537397062,-0.783222909372043));
#46834=CARTESIAN_POINT('Ctrl Pts',(-1.20724743479485,53.4777969298765,-0.829053274282686));
#46835=CARTESIAN_POINT('Ctrl Pts',(-1.17571072582716,53.4748401200468,-0.873187873684522));
#46836=CARTESIAN_POINT('Ctrl Pts',(-1.14190992569338,53.4718833102171,-0.915354560595474));
#46837=CARTESIAN_POINT('Ctrl Pts',(-1.1075201470487,53.4688749780139,-0.958256001487645));
#46838=CARTESIAN_POINT('Ctrl Pts',(-1.07063596092685,53.4658666458107,-0.999308203109229));
#46839=CARTESIAN_POINT('Ctrl Pts',(-1.03148379480124,53.4628583136074,-1.03820683443254));
#46840=CARTESIAN_POINT('Ctrl Pts',(-0.992401974016205,53.4598553865241,
-1.07703557594542));
#46841=CARTESIAN_POINT('Ctrl Pts',(-0.951060631611375,53.4568524594408,
-1.11371805588311));
#46842=CARTESIAN_POINT('Ctrl Pts',(-0.907726122749242,53.4538495323575,
-1.14798324729877));
#46843=CARTESIAN_POINT('Ctrl Pts',(-0.864435005723443,53.4508496121739,
-1.1822141281934));
#46844=CARTESIAN_POINT('Ctrl Pts',(-0.819155088302014,53.4478496919903,
-1.21403218870371));
#46845=CARTESIAN_POINT('Ctrl Pts',(-0.772187840886459,53.4448497718067,
-1.24320480548746));
#46846=CARTESIAN_POINT('Ctrl Pts',(-0.725249006133795,53.4418516664137,
-1.27235977440441));
#46847=CARTESIAN_POINT('Ctrl Pts',(-0.676625312742512,53.4388535610207,
-1.29887219284699));
#46848=CARTESIAN_POINT('Ctrl Pts',(-0.62664751905947,53.4358554556277,-1.32255250816616));
#46849=CARTESIAN_POINT('Ctrl Pts',(-0.576680150312218,53.4328579756136,
-1.34622788397624));
#46850=CARTESIAN_POINT('Ctrl Pts',(-0.525359719776652,53.4298604955995,
-1.36707210330548));
#46851=CARTESIAN_POINT('Ctrl Pts',(-0.473039822227728,53.4268630155854,
-1.38494244522535));
#46852=CARTESIAN_POINT('Ctrl Pts',(-0.420671535721616,53.4238627633003,
-1.40282931483832));
#46853=CARTESIAN_POINT('Ctrl Pts',(-0.367302436829406,53.4208625110152,
-1.4177366400966));
#46854=CARTESIAN_POINT('Ctrl Pts',(-0.313302844803723,53.4178622587302,
-1.42957111660732));
#46855=CARTESIAN_POINT('Ctrl Pts',(-0.25927901157679,53.4148606595883,-1.44141090578645));
#46856=CARTESIAN_POINT('Ctrl Pts',(-0.204624644159727,53.4118590604464,
-1.45017501236716));
#46857=CARTESIAN_POINT('Ctrl Pts',(-0.14971856735692,53.4088574613045,-1.45582162389099));
#46858=CARTESIAN_POINT('Ctrl Pts',(-0.0947068753758562,53.4058500884041,
-1.46147909701553));
#46859=CARTESIAN_POINT('Ctrl Pts',(-0.0394430364872446,53.4028427155037,
-1.46400707041701));
#46860=CARTESIAN_POINT('Ctrl Pts',(0.0156918512274061,53.3998353426032,
-1.46341587247271));
#46861=CARTESIAN_POINT('Ctrl Pts',(0.0604660502298152,53.3973931010698,
-1.46293576966476));
#46862=CARTESIAN_POINT('Ctrl Pts',(0.105155090899535,53.3949508595364,-1.46039964528197));
#46863=CARTESIAN_POINT('Ctrl Pts',(0.149558460248952,53.392508618003,-1.45583808061472));
#46864=CARTESIAN_POINT('Ctrl Pts',(0.204254150302647,53.3895002857997,-1.45021918432701));
#46865=CARTESIAN_POINT('Ctrl Pts',(0.25874938857528,53.3864919535964,-1.44150164742992));
#46866=CARTESIAN_POINT('Ctrl Pts',(0.312665684768387,53.3834836213931,-1.42971060693006));
#46867=CARTESIAN_POINT('Ctrl Pts',(0.366485108665576,53.3804806943098,-1.41794075158654));
#46868=CARTESIAN_POINT('Ctrl Pts',(0.41972714227277,53.3774777672264,-1.40310846303509));
#46869=CARTESIAN_POINT('Ctrl Pts',(0.472019615198521,53.374474840143,-1.38529048681778));
#46870=CARTESIAN_POINT('Ctrl Pts',(0.524259726473268,53.3714749199594,-1.36749035214821));
#46871=CARTESIAN_POINT('Ctrl Pts',(0.575551662363499,53.3684749997757,-1.34671062142189));
#46872=CARTESIAN_POINT('Ctrl Pts',(0.625536466939525,53.365475079592,-1.32307837202821));
#46873=CARTESIAN_POINT('Ctrl Pts',(0.67549103339254,53.362476974199,-1.29946041887657));
#46874=CARTESIAN_POINT('Ctrl Pts',(0.724139558553897,53.3594788688059,-1.27299359265179));
#46875=CARTESIAN_POINT('Ctrl Pts',(0.77114338272203,53.3564807634129,-1.2438529387689));
#46876=CARTESIAN_POINT('Ctrl Pts',(0.818137402298552,53.3534832833987,-1.21471836337463));
#46877=CARTESIAN_POINT('Ctrl Pts',(0.863486952817407,53.3504858033846,-1.18291134626145));
#46878=CARTESIAN_POINT('Ctrl Pts',(0.906880330003941,53.3474883233704,-1.14865152115511));
#46879=CARTESIAN_POINT('Ctrl Pts',(0.950313840301762,53.3444880710853,-1.11436001026022));
#46880=CARTESIAN_POINT('Ctrl Pts',(0.99178714630534,53.3414878188002,-1.07761148713108));
#46881=CARTESIAN_POINT('Ctrl Pts',(1.03102098604369,53.3384875665151,-1.03866644132633));
#46882=CARTESIAN_POINT('Ctrl Pts',(1.07027243842259,53.3354859673732,-0.99970391252482));
#46883=CARTESIAN_POINT('Ctrl Pts',(1.10728206611334,53.3324843682312,-0.958543289348735));
#46884=CARTESIAN_POINT('Ctrl Pts',(1.14180925128689,53.3294827690893,-0.915480138329427));
#46885=CARTESIAN_POINT('Ctrl Pts',(1.17640285160107,53.3264753961889,-0.872334152720036));
#46886=CARTESIAN_POINT('Ctrl Pts',(1.20850416171198,53.3234680232884,-0.827278759840527));
#46887=CARTESIAN_POINT('Ctrl Pts',(1.23791513373388,53.320460650388,-0.780639719507421));
#46888=CARTESIAN_POINT('Ctrl Pts',(1.26179933425598,53.3180184088549,-0.742764868222509));
#46889=CARTESIAN_POINT('Ctrl Pts',(1.28391009492697,53.3155761673219,-0.703846279542525));
#46890=CARTESIAN_POINT('Ctrl Pts',(1.30416433960299,53.3131339257888,-0.664068991376574));
#46891=CARTESIAN_POINT('Ctrl Pts',(1.32911334472593,53.3101255935852,-0.615071668489279));
#46892=CARTESIAN_POINT('Ctrl Pts',(1.35135047432382,53.3071172613816,-0.56456190198843));
#46893=CARTESIAN_POINT('Ctrl Pts',(1.37069153569222,53.3041089291779,-0.512871293778182));
#46894=CARTESIAN_POINT('Ctrl Pts',(1.38999784665771,53.3011060020942,-0.46127355893344));
#46895=CARTESIAN_POINT('Ctrl Pts',(1.40641823129796,53.2981030750105,-0.40849968381212));
#46896=CARTESIAN_POINT('Ctrl Pts',(1.41981528099887,53.2951001479268,-0.354903955799443));
#46897=CARTESIAN_POINT('Ctrl Pts',(1.43319891592706,53.2921002277427,-0.301361894416825));
#46898=CARTESIAN_POINT('Ctrl Pts',(1.44356508487175,53.2891003075587,-0.247000120728342));
#46899=CARTESIAN_POINT('Ctrl Pts',(1.45082583068964,53.2861003873746,-0.192189123010937));
#46900=CARTESIAN_POINT('Ctrl Pts',(1.45808218414616,53.2831022819812,-0.137411283004198));
#46901=CARTESIAN_POINT('Ctrl Pts',(1.46223676838547,53.2801041765878,-0.0821852807834841));
#46902=CARTESIAN_POINT('Ctrl Pts',(1.46325293337584,53.2771060711944,-0.0268905739432862));
#46903=CARTESIAN_POINT('Ctrl Pts',(1.46426888640298,53.2741085911799,0.0283925988989668));
#46904=CARTESIAN_POINT('Ctrl Pts',(1.46214771030909,53.2711111111653,0.0837439194122856));
#46905=CARTESIAN_POINT('Ctrl Pts',(1.45690483515211,53.2681136311508,0.138782388329361));
#46906=CARTESIAN_POINT('Ctrl Pts',(1.45165711103186,53.2651133788653,0.193871760521138));
#46907=CARTESIAN_POINT('Ctrl Pts',(1.44328196932721,53.2621131265798,0.248647175308659));
#46908=CARTESIAN_POINT('Ctrl Pts',(1.43184676089073,53.2591128742943,0.3027327258932));
#46909=CARTESIAN_POINT('Ctrl Pts',(1.42040641902306,53.256111275152,0.356842556267067));
#46910=CARTESIAN_POINT('Ctrl Pts',(1.40590341073846,53.2531096760097,0.410261393706924));
#46911=CARTESIAN_POINT('Ctrl Pts',(1.38845551706784,53.2501080768673,0.462626768706566));
#46912=CARTESIAN_POINT('Ctrl Pts',(1.37097406131256,53.2471007039665,0.51509287168989));
#46913=CARTESIAN_POINT('Ctrl Pts',(1.35053659899753,53.2440933310657,0.566500970985331));
#46914=CARTESIAN_POINT('Ctrl Pts',(1.32730936811835,53.2410859581648,0.616507981542214));
#46915=CARTESIAN_POINT('Ctrl Pts',(1.30844688921991,53.2386437166348,0.657117909876322));
#46916=CARTESIAN_POINT('Ctrl Pts',(1.28774558225792,53.2362014751047,0.696804156453991));
#46917=CARTESIAN_POINT('Ctrl Pts',(1.26531583177733,53.2337592335746,0.73539655686823));
#46918=CARTESIAN_POINT('Ctrl Pts',(1.2376870572049,53.2307509013712,0.782934345225549));
#46919=CARTESIAN_POINT('Ctrl Pts',(1.20731664893692,53.2277425691678,0.829014327277459));
#46920=CARTESIAN_POINT('Ctrl Pts',(1.17438326852762,53.2247342369643,0.873301888582852));
#46921=CARTESIAN_POINT('Ctrl Pts',(1.14150906006434,53.2217313098808,0.917509877698758));
#46922=CARTESIAN_POINT('Ctrl Pts',(1.10608133051636,53.2187283827973,0.959931415927525));
#46923=CARTESIAN_POINT('Ctrl Pts',(1.06832317710263,53.2157254557138,1.00025888612166));
#46924=CARTESIAN_POINT('Ctrl Pts',(1.03060283179282,53.21272553553,1.04054597549612));
#46925=CARTESIAN_POINT('Ctrl Pts',(0.990557044489343,53.2097256153462,1.07874276614619));
#46926=CARTESIAN_POINT('Ctrl Pts',(0.94844934733431,53.2067256951623,1.11457439659321));
#46927=CARTESIAN_POINT('Ctrl Pts',(0.906367123075159,53.2037275897691,1.15038435082773));
#46928=CARTESIAN_POINT('Ctrl Pts',(0.862225863030327,53.2007294843759,1.18383163850145));
#46929=CARTESIAN_POINT('Ctrl Pts',(0.816324465664141,53.1977313789828,1.21467963544227));
#46930=CARTESIAN_POINT('Ctrl Pts',(0.7704326429328,53.1947338989684,1.24552119775748));
#46931=CARTESIAN_POINT('Ctrl Pts',(0.722781850590871,53.1917364189541,1.27376425105146));
#46932=CARTESIAN_POINT('Ctrl Pts',(0.673700532821939,53.1887389389398,1.29921508691803));
#46933=CARTESIAN_POINT('Ctrl Pts',(0.624573821351992,53.1857386866545,1.32468946142796));
#46934=CARTESIAN_POINT('Ctrl Pts',(0.574014411452842,53.1827384343693,1.34736621458981));
#46935=CARTESIAN_POINT('Ctrl Pts',(0.522374633333037,53.179738182084,1.36709801859639));
#46936=CARTESIAN_POINT('Ctrl Pts',(0.470711673366742,53.1767365829419,1.38683868049641));
#46937=CARTESIAN_POINT('Ctrl Pts',(0.417967883231469,53.1737349837998,1.40363159699367));
#46938=CARTESIAN_POINT('Ctrl Pts',(0.364511660168443,53.1707333846577,1.4173790952322));
#46939=CARTESIAN_POINT('Ctrl Pts',(0.31095261080908,53.1677260117571,1.43115303761973));
#46940=CARTESIAN_POINT('Ctrl Pts',(0.256678910962631,53.1647186388565,1.4418697555694));
#46941=CARTESIAN_POINT('Ctrl Pts',(0.202068958382688,53.1617112659559,1.44948279950406));
#46942=CARTESIAN_POINT('Ctrl Pts',(0.157721051206288,53.1592690244241,1.45566523603429));
#46943=CARTESIAN_POINT('Ctrl Pts',(0.113151658485708,53.1568267828922,1.45980184246395));
#46944=CARTESIAN_POINT('Ctrl Pts',(0.0685636114066627,53.1543845413604,
1.46189304711079));
#46945=CARTESIAN_POINT('Ctrl Pts',(0.0136404368681237,53.151376209157,1.46446897508563));
#46946=CARTESIAN_POINT('Ctrl Pts',(-0.0415452319520151,53.1483678769535,
1.46395090058842));
#46947=CARTESIAN_POINT('Ctrl Pts',(-0.0966153742922227,53.1453595447501,
1.46030740580549));
#46948=CARTESIAN_POINT('Ctrl Pts',(-0.151586571202367,53.1423566176665,
1.45667045734954));
#46949=CARTESIAN_POINT('Ctrl Pts',(-0.206442130184051,53.139353690583,1.44991926667887));
#46950=CARTESIAN_POINT('Ctrl Pts',(-0.260802606776823,53.1363507634995,
1.44007439054322));
#46951=CARTESIAN_POINT('Ctrl Pts',(-0.315108650979167,53.1333508433156,
1.43023937230755));
#46952=CARTESIAN_POINT('Ctrl Pts',(-0.368920076967387,53.1303509231318,
1.41731689847776));
#46953=CARTESIAN_POINT('Ctrl Pts',(-0.421863024325294,53.1273510029479,
1.40137926297884));
#46954=CARTESIAN_POINT('Ctrl Pts',(-0.47477394404273,53.1243528975547,1.38545126889365));
#46955=CARTESIAN_POINT('Ctrl Pts',(-0.526816920995354,53.1213547921615,
1.36651188028076));
#46956=CARTESIAN_POINT('Ctrl Pts',(-0.57763103332442,53.1183566867683,1.34468384363781));
#46957=CARTESIAN_POINT('Ctrl Pts',(-0.628434546268866,53.1153592067539,
1.32286036013464));
#46958=CARTESIAN_POINT('Ctrl Pts',(-0.678009217880427,53.1123617267396,
1.29814963362067));
#46959=CARTESIAN_POINT('Ctrl Pts',(-0.726014152547299,53.1093642467252,
1.27072251113334));
#46960=CARTESIAN_POINT('Ctrl Pts',(-0.774063485403634,53.1063639944399,
1.24327002220006));
#46961=CARTESIAN_POINT('Ctrl Pts',(-0.820539720261415,53.1033637421546,
1.21309638044427));
#46962=CARTESIAN_POINT('Ctrl Pts',(-0.865127968604045,53.1003634898693,
1.18041765826297));
#46963=CARTESIAN_POINT('Ctrl Pts',(-0.909736233259117,53.0973618907272,
1.14772426612854));
#46964=CARTESIAN_POINT('Ctrl Pts',(-0.952454412876865,53.0943602915851,
1.11252388867989));
#46965=CARTESIAN_POINT('Ctrl Pts',(-0.993000618162861,53.091358692443,1.07507303116029));
#46966=CARTESIAN_POINT('Ctrl Pts',(-1.03362481654068,53.0883513195423,1.03755013463855));
#46967=CARTESIAN_POINT('Ctrl Pts',(-1.07206832522004,53.0853439466417,0.997768490892899));
#46968=CARTESIAN_POINT('Ctrl Pts',(-1.10808686241959,53.0823365737411,0.956020792312128));
#46969=CARTESIAN_POINT('Ctrl Pts',(-1.1373369655372,53.0798943322095,0.922118124870501));
#46970=CARTESIAN_POINT('Ctrl Pts',(-1.16498852794603,53.0774520906778,0.886919639444868));
#46971=CARTESIAN_POINT('Ctrl Pts',(-1.19093188475308,53.0750098491462,0.850595965120026));
#46972=CARTESIAN_POINT('Ctrl Pts',(-1.22317500899146,53.0719745635543,0.805451894028509));
#46973=CARTESIAN_POINT('Ctrl Pts',(-1.25291514808135,53.0689392779623,0.758377611385144));
#46974=CARTESIAN_POINT('Ctrl Pts',(-1.27991741444354,53.0659039923703,0.709678562593066));
#46975=CARTESIAN_POINT('Ctrl Pts',(-1.30687456070399,53.0628737786635,0.661060888675478));
#46976=CARTESIAN_POINT('Ctrl Pts',(-1.33110265731129,53.0598435649568,0.610824279516039));
#46977=CARTESIAN_POINT('Ctrl Pts',(-1.35240949428086,53.05681335125,0.559303861759417));
#46978=CARTESIAN_POINT('Ctrl Pts',(-1.37368565050044,53.0537875008952,0.507857630756016));
#46979=CARTESIAN_POINT('Ctrl Pts',(-1.39204870241039,53.0507616505403,0.455131736075086));
#46980=CARTESIAN_POINT('Ctrl Pts',(-1.40735296774861,53.0477358001855,0.401484587710638));
#46981=CARTESIAN_POINT('Ctrl Pts',(-1.42264437592381,53.0447124918574,0.34788250848977));
#46982=CARTESIAN_POINT('Ctrl Pts',(-1.43488195380794,53.0416891835293,0.293361205924596));
#46983=CARTESIAN_POINT('Ctrl Pts',(-1.44396929253368,53.0386658752012,0.238295892158849));
#46984=CARTESIAN_POINT('Ctrl Pts',(-1.45305339393419,53.0356436439137,0.183250195173629));
#46985=CARTESIAN_POINT('Ctrl Pts',(-1.45898939495832,53.0326214126261,0.127661379838728));
#46986=CARTESIAN_POINT('Ctrl Pts',(-1.46173203743927,53.0295991813386,0.0719145376376866));
#46987=CARTESIAN_POINT('Ctrl Pts',(-1.46292512432683,53.0282844695067,0.047663900919573));
#46988=CARTESIAN_POINT('Ctrl Pts',(-1.46351457201552,53.0269697576748,0.0233834458729815));
#46989=CARTESIAN_POINT('Ctrl Pts',(-1.46349972639677,53.0256550458429,-0.000894894726806227));
#46990=CARTESIAN_POINT('Origin',(0.,55.715,0.));
#46991=CARTESIAN_POINT('',(-1.46349975751718,52.4543449541929,-0.000842464927107473));
#46992=CARTESIAN_POINT('',(-1.46356159323047,52.5256550654528,-0.000674754275529077));
#46993=CARTESIAN_POINT('',(-1.4635,55.715,-1.79227059055215E-16));
#46994=CARTESIAN_POINT('Ctrl Pts',(-1.46349975751718,52.4543449541929,-0.000842464927105523));
#46995=CARTESIAN_POINT('Ctrl Pts',(-1.46353104926595,52.4573145585449,0.053516435090471));
#46996=CARTESIAN_POINT('Ctrl Pts',(-1.46052950171535,52.4602841628968,0.10799664215151));
#46997=CARTESIAN_POINT('Ctrl Pts',(-1.45448095535421,52.4632537672487,0.162226386608034));
#46998=CARTESIAN_POINT('Ctrl Pts',(-1.44844398843846,52.466217686537,0.216352312671336));
#46999=CARTESIAN_POINT('Ctrl Pts',(-1.43937166570992,52.4691816058252,0.270228191471467));
#47000=CARTESIAN_POINT('Ctrl Pts',(-1.427301866151,52.4721455251134,0.323483589818531));
#47001=CARTESIAN_POINT('Ctrl Pts',(-1.41524210424932,52.4751069795052,0.376694699158753));
#47002=CARTESIAN_POINT('Ctrl Pts',(-1.40018991934944,52.478068433897,0.429285821314699));
#47003=CARTESIAN_POINT('Ctrl Pts',(-1.3822345951345,52.4810298882888,0.48089476396959));
#47004=CARTESIAN_POINT('Ctrl Pts',(-1.3642866557656,52.4839901246639,0.532482480380307));
#47005=CARTESIAN_POINT('Ctrl Pts',(-1.34343812148758,52.486950361039,0.583088304963121));
#47006=CARTESIAN_POINT('Ctrl Pts',(-1.31982794369632,52.4899105974141,0.63236575574452));
#47007=CARTESIAN_POINT('Ctrl Pts',(-1.29609678355886,52.4928860025162,0.68189571210479));
#47008=CARTESIAN_POINT('Ctrl Pts',(-1.26957580844062,52.4958614076184,0.73008312987647));
#47009=CARTESIAN_POINT('Ctrl Pts',(-1.24045377280016,52.4988368127205,0.776599438285822));
#47010=CARTESIAN_POINT('Ctrl Pts',(-1.21144935669503,52.5018002006075,0.822927874300251));
#47011=CARTESIAN_POINT('Ctrl Pts',(-1.1798651988766,52.5047635884946,0.867598248163093));
#47012=CARTESIAN_POINT('Ctrl Pts',(-1.14593065596066,52.5077269763816,0.910315979058679));
#47013=CARTESIAN_POINT('Ctrl Pts',(-1.11178969455546,52.5107083900913,0.953293555195093));
#47014=CARTESIAN_POINT('Ctrl Pts',(-1.07527002533709,52.513689803801,0.994294235726321));
#47015=CARTESIAN_POINT('Ctrl Pts',(-1.0366434733955,52.5166712175106,1.03305496420399));
#47016=CARTESIAN_POINT('Ctrl Pts',(-0.998016921453907,52.5196526312203,
1.07181569268167));
#47017=CARTESIAN_POINT('Ctrl Pts',(-0.957283944973365,52.5226340449299,
1.10833615314451));
#47018=CARTESIAN_POINT('Ctrl Pts',(-0.914748300344012,52.5256154586396,
1.14239563944272));
#47019=CARTESIAN_POINT('Ctrl Pts',(-0.871828611231862,52.528623790843,1.1767626409535));
#47020=CARTESIAN_POINT('Ctrl Pts',(-0.826877950761343,52.5316321230465,
1.20878083215128));
#47021=CARTESIAN_POINT('Ctrl Pts',(-0.780183677225224,52.53464045525,1.23820260046219));
#47022=CARTESIAN_POINT('Ctrl Pts',(-0.733573300058009,52.5376433823335,
1.26757150619829));
#47023=CARTESIAN_POINT('Ctrl Pts',(-0.685225970294237,52.540646309417,1.29435296678914));
#47024=CARTESIAN_POINT('Ctrl Pts',(-0.635460747905163,52.5436492365005,
1.31834058113668));
#47025=CARTESIAN_POINT('Ctrl Pts',(-0.585745356573187,52.5466491566844,
1.34230417613653));
#47026=CARTESIAN_POINT('Ctrl Pts',(-0.534615358916831,52.5496490768682,
1.36347923779956));
#47027=CARTESIAN_POINT('Ctrl Pts',(-0.482415707669257,52.5526489970521,
1.38170450350065));
#47028=CARTESIAN_POINT('Ctrl Pts',(-0.430247634407936,52.5556471024453,
1.39991874389455));
#47029=CARTESIAN_POINT('Ctrl Pts',(-0.377011688301272,52.5586452078385,
1.41518655098178));
#47030=CARTESIAN_POINT('Ctrl Pts',(-0.323072009847727,52.5616433132318,
1.42739508421913));
#47031=CARTESIAN_POINT('Ctrl Pts',(-0.269143582744988,52.5646407932461,
1.43960107086196));
#47032=CARTESIAN_POINT('Ctrl Pts',(-0.214512230302412,52.5676382732604,
1.44874893402928));
#47033=CARTESIAN_POINT('Ctrl Pts',(-0.159554164232267,52.5706357532748,
1.45477651846466));
#47034=CARTESIAN_POINT('Ctrl Pts',(-0.104545269249389,52.5736360055601,
1.46080967761517));
#47035=CARTESIAN_POINT('Ctrl Pts',(-0.0492095837828533,52.5766362578454,
1.46371673408402));
#47036=CARTESIAN_POINT('Ctrl Pts',(0.00607113783769222,52.5796365101307,
1.46348740728622));
#47037=CARTESIAN_POINT('Ctrl Pts',(0.0613766757771898,52.5826381092728,
1.4632579775403));
#47038=CARTESIAN_POINT('Ctrl Pts',(0.116626671796092,52.5856397084149,1.45988938996001));
#47039=CARTESIAN_POINT('Ctrl Pts',(0.171442302665545,52.588641307557,1.45342347127626));
#47040=CARTESIAN_POINT('Ctrl Pts',(0.226363374734846,52.5916486804577,1.44694511500467));
#47041=CARTESIAN_POINT('Ctrl Pts',(0.280847890085497,52.5946560533583,1.43735761659836));
#47042=CARTESIAN_POINT('Ctrl Pts',(0.334526180335395,52.5976634262589,1.4247541839455));
#47043=CARTESIAN_POINT('Ctrl Pts',(0.378117498780343,52.6001056677905,1.41451912907113));
#47044=CARTESIAN_POINT('Ctrl Pts',(0.421177233326342,52.6025479093222,1.40229613677227));
#47045=CARTESIAN_POINT('Ctrl Pts',(0.463516369951613,52.6049901508538,1.38815878947146));
#47046=CARTESIAN_POINT('Ctrl Pts',(0.515669355857966,52.6079984830573,1.37074452613733));
#47047=CARTESIAN_POINT('Ctrl Pts',(0.566950816112585,52.6110068152608,1.35034996121041));
#47048=CARTESIAN_POINT('Ctrl Pts',(0.616996857500184,52.6140151474643,1.32708218578764));
#47049=CARTESIAN_POINT('Ctrl Pts',(0.666952980342508,52.6170180745478,1.30385621595947));
#47050=CARTESIAN_POINT('Ctrl Pts',(0.715677613505122,52.6200210016314,1.27776750096769));
#47051=CARTESIAN_POINT('Ctrl Pts',(0.762824288771276,52.623023928715,1.24897211916864));
#47052=CARTESIAN_POINT('Ctrl Pts',(0.809923754991525,52.6260238488989,1.22020557084498));
#47053=CARTESIAN_POINT('Ctrl Pts',(0.855447944005862,52.6290237690828,1.18873799846579));
#47054=CARTESIAN_POINT('Ctrl Pts',(0.899074262649257,52.6320236892667,1.15477171780473));
#47055=CARTESIAN_POINT('Ctrl Pts',(0.94267418971227,52.6350217946599,1.12082598491974));
#47056=CARTESIAN_POINT('Ctrl Pts',(0.98437810538599,52.6380199000532,1.08438486379709));
#47057=CARTESIAN_POINT('Ctrl Pts',(1.02389368717946,52.6410180054464,1.04569305599399));
#47058=CARTESIAN_POINT('Ctrl Pts',(1.06340102636414,52.6440154854608,1.00700931896755));
#47059=CARTESIAN_POINT('Ctrl Pts',(1.10072056033147,52.6470129654752,0.96607619723495));
#47060=CARTESIAN_POINT('Ctrl Pts',(1.13559599889987,52.6500104454896,0.923176027246491));
#47061=CARTESIAN_POINT('Ctrl Pts',(1.17050369261746,52.6530106977749,0.880236180297959));
#47062=CARTESIAN_POINT('Ctrl Pts',(1.2029624399759,52.6560109500603,0.835326061356269));
#47063=CARTESIAN_POINT('Ctrl Pts',(1.23275652369796,52.6590112023456,0.788760802322296));
#47064=CARTESIAN_POINT('Ctrl Pts',(1.26256398241702,52.6620128014878,0.742174639467111));
#47065=CARTESIAN_POINT('Ctrl Pts',(1.28970413303551,52.66501440063,0.693932317105381));
#47066=CARTESIAN_POINT('Ctrl Pts',(1.31400662314741,52.6680159997721,0.644374770087052));
#47067=CARTESIAN_POINT('Ctrl Pts',(1.33835586057712,52.6710233726728,0.594721896112934));
#47068=CARTESIAN_POINT('Ctrl Pts',(1.35985632634852,52.6740307455735,0.543749231768453));
#47069=CARTESIAN_POINT('Ctrl Pts',(1.37838579892566,52.6770381184742,0.491817892435872));
#47070=CARTESIAN_POINT('Ctrl Pts',(1.39343330017515,52.6794803600054,0.449645246115749));
#47071=CARTESIAN_POINT('Ctrl Pts',(1.4065223972658,52.6819226015367,0.406840832596735));
#47072=CARTESIAN_POINT('Ctrl Pts',(1.41761237649152,52.684364843068,0.363603355344911));
#47073=CARTESIAN_POINT('Ctrl Pts',(1.43127291792989,52.6873731752715,0.310343801141272));
#47074=CARTESIAN_POINT('Ctrl Pts',(1.44195697891875,52.6903815074749,0.256199759131709));
#47075=CARTESIAN_POINT('Ctrl Pts',(1.44955713379634,52.6933898396784,0.201535023904365));
#47076=CARTESIAN_POINT('Ctrl Pts',(1.45714363335072,52.6963927667619,0.146968505705502));
#47077=CARTESIAN_POINT('Ctrl Pts',(1.46165714999721,52.6993956938455,0.0918836702770846));
#47078=CARTESIAN_POINT('Ctrl Pts',(1.46304086395174,52.702398620929,0.036656246498318));
#47079=CARTESIAN_POINT('Ctrl Pts',(1.4644231923618,52.7053985411129,-0.018515876795996));
#47080=CARTESIAN_POINT('Ctrl Pts',(1.46268191263403,52.7083984612968,-0.0738297795846173));
#47081=CARTESIAN_POINT('Ctrl Pts',(1.45781199954093,52.7113983814806,-0.128904708969369));
#47082=CARTESIAN_POINT('Ctrl Pts',(1.45294503248377,52.7143964868739,-0.183946320978928));
#47083=CARTESIAN_POINT('Ctrl Pts',(1.44495322959695,52.7173945922671,-0.238748720358541));
#47084=CARTESIAN_POINT('Ctrl Pts',(1.43388359375688,52.7203926976603,-0.292933592397393));
#47085=CARTESIAN_POINT('Ctrl Pts',(1.42281626694719,52.7233901776747,-0.347107161940224));
#47086=CARTESIAN_POINT('Ctrl Pts',(1.40867248773217,52.726387657689,-0.400662942018325));
#47087=CARTESIAN_POINT('Ctrl Pts',(1.3915504212787,52.7293851377034,-0.453232473504558));
#47088=CARTESIAN_POINT('Ctrl Pts',(1.37441251918756,52.7323853899887,-0.505850624826231));
#47089=CARTESIAN_POINT('Ctrl Pts',(1.35429099024574,52.735385642274,-0.557480201005298));
#47090=CARTESIAN_POINT('Ctrl Pts',(1.33133355935835,52.7383858945593,-0.607769038143786));
#47091=CARTESIAN_POINT('Ctrl Pts',(1.30836582254677,52.7413874937014,-0.658080450671743));
#47092=CARTESIAN_POINT('Ctrl Pts',(1.2825598929126,52.7443890928436,-0.707049455543295));
#47093=CARTESIAN_POINT('Ctrl Pts',(1.25410978013588,52.7473906919857,-0.754348002825965));
#47094=CARTESIAN_POINT('Ctrl Pts',(1.2256049418369,52.7503980648863,-0.801737531741041));
#47095=CARTESIAN_POINT('Ctrl Pts',(1.19444605759191,52.753405437787,-0.847449745331225));
#47096=CARTESIAN_POINT('Ctrl Pts',(1.16087019891324,52.7564128106876,-0.89118608117224));
#47097=CARTESIAN_POINT('Ctrl Pts',(1.13360375766034,52.7588550522191,-0.926703690512898));
#47098=CARTESIAN_POINT('Ctrl Pts',(1.10474424805654,52.7612972937506,-0.960918760075315));
#47099=CARTESIAN_POINT('Ctrl Pts',(1.07443651424841,52.7637395352821,-0.993689300963699));
#47100=CARTESIAN_POINT('Ctrl Pts',(1.03710370729502,52.7667478674856,-1.03405577258739));
#47101=CARTESIAN_POINT('Ctrl Pts',(0.997413273392782,52.7697561996891,-1.07240151421543));
#47102=CARTESIAN_POINT('Ctrl Pts',(0.955612560776801,52.7727645318925,-1.10843893998975));
#47103=CARTESIAN_POINT('Ctrl Pts',(0.913886952188335,52.7757674589761,-1.14441161672877));
#47104=CARTESIAN_POINT('Ctrl Pts',(0.87005898616825,52.7787703860596,-1.17808386526148));
#47105=CARTESIAN_POINT('Ctrl Pts',(0.824413487742079,52.7817733131432,-1.20920413960131));
#47106=CARTESIAN_POINT('Ctrl Pts',(0.778813695199047,52.7847732333271,-1.24029325249759));
#47107=CARTESIAN_POINT('Ctrl Pts',(0.731400409966574,52.7877731535109,-1.26883515643326));
#47108=CARTESIAN_POINT('Ctrl Pts',(0.682490773392749,52.7907730736948,-1.29461909233325));
#47109=CARTESIAN_POINT('Ctrl Pts',(0.633610724522977,52.793771179088,-1.32038743033642));
#47110=CARTESIAN_POINT('Ctrl Pts',(0.583236585237063,52.7967692844813,-1.34340086081427));
#47111=CARTESIAN_POINT('Ctrl Pts',(0.531711670956427,52.7997673898745,-1.36349365563934));
#47112=CARTESIAN_POINT('Ctrl Pts',(0.480197504327599,52.8027648698889,-1.38358225928106));
#47113=CARTESIAN_POINT('Ctrl Pts',(0.427533531783183,52.8057623499032,-1.40075124486874));
#47114=CARTESIAN_POINT('Ctrl Pts',(0.374082541870647,52.8087598299176,-1.41488321138799));
#47115=CARTESIAN_POINT('Ctrl Pts',(0.320582116890717,52.8117600822029,-1.42902824809955));
#47116=CARTESIAN_POINT('Ctrl Pts',(0.266293732613245,52.8147603344882,-1.44013051795475));
#47117=CARTESIAN_POINT('Ctrl Pts',(0.211593371524531,52.8177605867735,-1.44812309391394));
#47118=CARTESIAN_POINT('Ctrl Pts',(0.15686845464912,52.8207621859156,-1.45611925785659));
#47119=CARTESIAN_POINT('Ctrl Pts',(0.101731720078069,52.8237637850578,-1.46100289822506));
#47120=CARTESIAN_POINT('Ctrl Pts',(0.046563999296092,52.8267653841999,-1.46275905191852));
#47121=CARTESIAN_POINT('Ctrl Pts',(-0.00870983995210641,52.8297727571006,
-1.46451858368041));
#47122=CARTESIAN_POINT('Ctrl Pts',(-0.0640142543121039,52.8327801300012,
-1.46313862316723));
#47123=CARTESIAN_POINT('Ctrl Pts',(-0.118969825836467,52.8357875029019,
-1.45865637850058));
#47124=CARTESIAN_POINT('Ctrl Pts',(-0.163598404864021,52.8382297444333,
-1.45501641616779));
#47125=CARTESIAN_POINT('Ctrl Pts',(-0.207996882973535,52.8406719859648,
-1.44933157481369));
#47126=CARTESIAN_POINT('Ctrl Pts',(-0.251967406554764,52.8431142274963,
-1.44164651563206));
#47127=CARTESIAN_POINT('Ctrl Pts',(-0.30612992094532,52.8461225596997,-1.4321801255458));
#47128=CARTESIAN_POINT('Ctrl Pts',(-0.35987371977749,52.8491308919032,-1.41963697875378));
#47129=CARTESIAN_POINT('Ctrl Pts',(-0.412823031868646,52.8521392241067,
-1.40406887094572));
#47130=CARTESIAN_POINT('Ctrl Pts',(-0.465677209060325,52.8551421511902,
-1.38852873461288));
#47131=CARTESIAN_POINT('Ctrl Pts',(-0.517739228997993,52.8581450782738,
-1.36997457047864));
#47132=CARTESIAN_POINT('Ctrl Pts',(-0.568643268197576,52.8611480053573,
-1.34850920780452));
#47133=CARTESIAN_POINT('Ctrl Pts',(-0.619496336016655,52.8641479255412,
-1.32706533888976));
#47134=CARTESIAN_POINT('Ctrl Pts',(-0.669193235005333,52.8671478457251,
-1.30271625004196));
#47135=CARTESIAN_POINT('Ctrl Pts',(-0.717384876594728,52.870147765909,-1.2756140438366));
#47136=CARTESIAN_POINT('Ctrl Pts',(-0.765547364828624,52.8731458713022,
-1.24852823301074));
#47137=CARTESIAN_POINT('Ctrl Pts',(-0.812205940344729,52.8761439766955,
-1.21869286436914));
#47138=CARTESIAN_POINT('Ctrl Pts',(-0.8570351466989,52.8791420820887,-1.18630645590538));
#47139=CARTESIAN_POINT('Ctrl Pts',(-0.901855002067964,52.8821395621031,
-1.15392680296661));
#47140=CARTESIAN_POINT('Ctrl Pts',(-0.944845817479181,52.8851370421174,
-1.11899747631191));
#47141=CARTESIAN_POINT('Ctrl Pts',(-0.985712172587482,52.8881345221318,
-1.0817595679322));
#47142=CARTESIAN_POINT('Ctrl Pts',(-1.02661632364724,52.8911347744171,-1.0444872194324));
#47143=CARTESIAN_POINT('Ctrl Pts',(-1.06539169668125,52.8941350267024,-1.00490238004313));
#47144=CARTESIAN_POINT('Ctrl Pts',(-1.10177811711606,52.8971352789877,-0.963284605214991));
#47145=CARTESIAN_POINT('Ctrl Pts',(-1.13818087194359,52.9001368781299,-0.921648147563138));
#47146=CARTESIAN_POINT('Ctrl Pts',(-1.17219221067203,52.903138477272,-0.877977353199902));
#47147=CARTESIAN_POINT('Ctrl Pts',(-1.203592982875,52.9061400764142,-0.83258403874568));
#47148=CARTESIAN_POINT('Ctrl Pts',(-1.23505415637306,52.9091474493148,-0.787103407490333));
#47149=CARTESIAN_POINT('Ctrl Pts',(-1.26389445454505,52.9121548222155,-0.739894089129721));
#47150=CARTESIAN_POINT('Ctrl Pts',(-1.28993932232875,52.9151621951162,-0.691295012791242));
#47151=CARTESIAN_POINT('Ctrl Pts',(-1.31108996107004,52.9176044366476,-0.651828446274866));
#47152=CARTESIAN_POINT('Ctrl Pts',(-1.33039789737408,52.920046678179,-0.611445951610777));
#47153=CARTESIAN_POINT('Ctrl Pts',(-1.3477933260689,52.9224889197105,-0.57033797015815));
#47154=CARTESIAN_POINT('Ctrl Pts',(-1.37157131759644,52.9258272449372,-0.514147044838465));
#47155=CARTESIAN_POINT('Ctrl Pts',(-1.39186134356342,52.929165570164,-0.456396611155354));
#47156=CARTESIAN_POINT('Ctrl Pts',(-1.40848026768949,52.9325038953908,-0.397511742630756));
#47157=CARTESIAN_POINT('Ctrl Pts',(-1.4250404108123,52.9358304129877,-0.338835149420643));
#47158=CARTESIAN_POINT('Ctrl Pts',(-1.43795520456422,52.9391569305845,-0.279032416728898));
#47159=CARTESIAN_POINT('Ctrl Pts',(-1.44709009425181,52.9424834481814,-0.218546354621345));
#47160=CARTESIAN_POINT('Ctrl Pts',(-1.45617431336866,52.9457915138263,-0.158395804314613));
#47161=CARTESIAN_POINT('Ctrl Pts',(-1.46152030885999,52.9490995794712,-0.0975697894002547));
#47162=CARTESIAN_POINT('Ctrl Pts',(-1.46304423604721,52.9524076451162,-0.0365214097352111));
#47163=CARTESIAN_POINT('Ctrl Pts',(-1.46334171758207,52.9530534032953,-0.0246043274519001));
#47164=CARTESIAN_POINT('Ctrl Pts',(-1.46349370840455,52.9536991614744,-0.0126788176551808));
#47165=CARTESIAN_POINT('Ctrl Pts',(-1.4634998086868,52.9543449196535,-0.000748313909921448));
#47166=CARTESIAN_POINT('Ctrl Pts',(-1.46168684698443,53.0256544778977,-0.000904261258610456));
#47167=CARTESIAN_POINT('Ctrl Pts',(-1.4627153019643,53.0156480375759,-0.185461603358528));
#47168=CARTESIAN_POINT('Ctrl Pts',(-1.34465214268998,52.9791833665158,-0.856740950372973));
#47169=CARTESIAN_POINT('Ctrl Pts',(-0.337036094537274,52.9162604647181,
-1.69657654331278));
#47170=CARTESIAN_POINT('Ctrl Pts',(1.24245598610379,52.8368857725037,-1.20344024319159));
#47171=CARTESIAN_POINT('Ctrl Pts',(1.6849636373595,52.7575110802896,0.390976773113176));
#47172=CARTESIAN_POINT('Ctrl Pts',(0.58554349303632,52.6781363880753,1.62760686718302));
#47173=CARTESIAN_POINT('Ctrl Pts',(-1.00666498239691,52.600851258045,1.38145223997477));
#47174=CARTESIAN_POINT('Ctrl Pts',(-1.46296296025439,52.5500243587529,0.445771649118409));
#47175=CARTESIAN_POINT('Ctrl Pts',(-1.46552883361008,52.5256556901986,-0.000664216367255248));
#47176=CARTESIAN_POINT('Origin',(0.,55.715,0.));
#47177=CARTESIAN_POINT('',(-1.4634994347896,51.9543449541571,0.00128622335730389));
#47178=CARTESIAN_POINT('',(-1.4634993993698,52.025655045799,0.00132591260086994));
#47179=CARTESIAN_POINT('',(-1.4635,55.715,-1.79227059055215E-16));
#47180=CARTESIAN_POINT('Ctrl Pts',(-1.4634994347896,51.9543449541571,0.00128622335730389));
#47181=CARTESIAN_POINT('Ctrl Pts',(-1.46342941742781,51.9586837643365,0.0809538555928721));
#47182=CARTESIAN_POINT('Ctrl Pts',(-1.45685072552131,51.9630225745159,0.160344782218165));
#47183=CARTESIAN_POINT('Ctrl Pts',(-1.44391791303884,51.9673613846953,0.238607020863936));
#47184=CARTESIAN_POINT('Ctrl Pts',(-1.44130358770758,51.9682384608437,0.254427473936301));
#47185=CARTESIAN_POINT('Ctrl Pts',(-1.43842975380386,51.969115536992,0.27020190040974));
#47186=CARTESIAN_POINT('Ctrl Pts',(-1.43529790189955,51.9699926131404,0.285923386246649));
#47187=CARTESIAN_POINT('Ctrl Pts',(-1.42455578908048,51.9730009453427,0.339847383837681));
#47188=CARTESIAN_POINT('Ctrl Pts',(-1.41074765930891,51.976009277545,0.393280163984652));
#47189=CARTESIAN_POINT('Ctrl Pts',(-1.39393416290903,51.9790176097473,0.445847282682202));
#47190=CARTESIAN_POINT('Ctrl Pts',(-1.3771508755945,51.9820205368297,0.498319953173532));
#47191=CARTESIAN_POINT('Ctrl Pts',(-1.35737309683935,51.9850234639121,0.5499295491025));
#47192=CARTESIAN_POINT('Ctrl Pts',(-1.33471226153445,51.9880263909945,0.600312775900695));
#47193=CARTESIAN_POINT('Ctrl Pts',(-1.31207411704297,51.9910263111772,0.650645552819918));
#47194=CARTESIAN_POINT('Ctrl Pts',(-1.2865588501779,51.9940262313599,0.699753913120156));
#47195=CARTESIAN_POINT('Ctrl Pts',(-1.25832676043541,51.9970261515426,0.747292455449752));
#47196=CARTESIAN_POINT('Ctrl Pts',(-1.23011174959128,52.0000242569346,0.794802239513849));
#47197=CARTESIAN_POINT('Ctrl Pts',(-1.19918344268237,52.0030223623267,0.840743633927565));
#47198=CARTESIAN_POINT('Ctrl Pts',(-1.16574798392042,52.0060204677188,0.884795958391238));
#47199=CARTESIAN_POINT('Ctrl Pts',(-1.13231949950606,52.009017947732,0.928839093920941));
#47200=CARTESIAN_POINT('Ctrl Pts',(-1.09638522119433,52.0120154277452,0.970993520856203));
#47201=CARTESIAN_POINT('Ctrl Pts',(-1.05819314641334,52.0150129077584,1.01096959147337));
#47202=CARTESIAN_POINT('Ctrl Pts',(-1.01996574903474,52.0180131600426,1.0509826346474));
#47203=CARTESIAN_POINT('Ctrl Pts',(-0.979476749019557,52.0210134123268,
1.08881291271801));
#47204=CARTESIAN_POINT('Ctrl Pts',(-0.937011764659512,52.0240136646109,
1.12420692174069));
#47205=CARTESIAN_POINT('Ctrl Pts',(-0.894527717150933,52.0270152637519,
1.15961681964832));
#47206=CARTESIAN_POINT('Ctrl Pts',(-0.850066342559578,52.030016862893,1.19258795262113));
#47207=CARTESIAN_POINT('Ctrl Pts',(-0.803944543095699,52.033018462034,1.22290859087123));
#47208=CARTESIAN_POINT('Ctrl Pts',(-0.757734025544826,52.0360258349336,
1.25328755271349));
#47209=CARTESIAN_POINT('Ctrl Pts',(-0.709857161136456,52.0390332078331,
1.28100556834841));
#47210=CARTESIAN_POINT('Ctrl Pts',(-0.660656904481931,52.0420405807327,
1.30589613084669));
#47211=CARTESIAN_POINT('Ctrl Pts',(-0.62070212846228,52.0444828222733,1.32610937600524));
#47212=CARTESIAN_POINT('Ctrl Pts',(-0.579875171453695,52.0469250638139,
1.34445881403067));
#47213=CARTESIAN_POINT('Ctrl Pts',(-0.538368069328275,52.0493673053545,
1.36087915404996));
#47214=CARTESIAN_POINT('Ctrl Pts',(-0.487239976610686,52.0523756375563,
1.38110558817741));
#47215=CARTESIAN_POINT('Ctrl Pts',(-0.434861406560966,52.0553839697581,
1.39848982932012));
#47216=CARTESIAN_POINT('Ctrl Pts',(-0.381579825840558,52.0583923019598,
1.41287971409865));
#47217=CARTESIAN_POINT('Ctrl Pts',(-0.328393977013189,52.0613952290417,
1.42724374433436));
#47218=CARTESIAN_POINT('Ctrl Pts',(-0.27430884348231,52.0643981561235,1.43862395760165));
#47219=CARTESIAN_POINT('Ctrl Pts',(-0.219690073186104,52.0674010832053,
1.44691690215557));
#47220=CARTESIAN_POINT('Ctrl Pts',(-0.16512599391629,52.0704010033874,1.45520154279407));
#47221=CARTESIAN_POINT('Ctrl Pts',(-0.11002985655561,52.0734009235695,1.46040495909979));
#47222=CARTESIAN_POINT('Ctrl Pts',(-0.0547787834541315,52.0764008437516,
1.46247445614728));
#47223=CARTESIAN_POINT('Ctrl Pts',(0.000438865714139876,52.079398949143,
1.46454270126016));
#47224=CARTESIAN_POINT('Ctrl Pts',(0.055810737441721,52.0823970545345,1.46348076474494));
#47225=CARTESIAN_POINT('Ctrl Pts',(0.110955609096121,52.0853951599259,1.45928787523576));
#47226=CARTESIAN_POINT('Ctrl Pts',(0.166088978006442,52.0883926399384,1.45509586032714));
#47227=CARTESIAN_POINT('Ctrl Pts',(0.220994913799366,52.091390119951,1.44777422924706));
#47228=CARTESIAN_POINT('Ctrl Pts',(0.275295560985323,52.0943875999635,1.43737420461819));
#47229=CARTESIAN_POINT('Ctrl Pts',(0.32964642905838,52.097387852247,1.42696456134775));
#47230=CARTESIAN_POINT('Ctrl Pts',(0.383390369377223,52.1003881045305,1.41347093547737));
#47231=CARTESIAN_POINT('Ctrl Pts',(0.43615948329097,52.1033883568139,1.39699576060035));
#47232=CARTESIAN_POINT('Ctrl Pts',(0.48895228602622,52.1063899559542,1.38051318977809));
#47233=CARTESIAN_POINT('Ctrl Pts',(0.540768893944325,52.1093915550945,1.36104658804578));
#47234=CARTESIAN_POINT('Ctrl Pts',(0.59125953270791,52.1123931542348,1.33874733052284));
#47235=CARTESIAN_POINT('Ctrl Pts',(0.641847293285998,52.1154005271336,1.31640517902181));
#47236=CARTESIAN_POINT('Ctrl Pts',(0.691103516856547,52.1184079000324,1.29121972736791));
#47237=CARTESIAN_POINT('Ctrl Pts',(0.738702288430127,52.1214152729312,1.26338876798399));
#47238=CARTESIAN_POINT('Ctrl Pts',(0.777356522999696,52.123857514477,1.24078767142713));
#47239=CARTESIAN_POINT('Ctrl Pts',(0.814918099146787,52.1262997560229,1.21644285060387));
#47240=CARTESIAN_POINT('Ctrl Pts',(0.851227997708145,52.1287419975687,1.19048021651676));
#47241=CARTESIAN_POINT('Ctrl Pts',(0.895954219558794,52.1317503297734,1.15849966636333));
#47242=CARTESIAN_POINT('Ctrl Pts',(0.938971054269809,52.1347586619781,1.12392686811807));
#47243=CARTESIAN_POINT('Ctrl Pts',(0.979962189207295,52.1377669941828,1.08697118532372));
#47244=CARTESIAN_POINT('Ctrl Pts',(1.02087967469914,52.1407699212677,1.05008190141183));
#47245=CARTESIAN_POINT('Ctrl Pts',(1.05977829334223,52.1437728483525,1.01081858014419));
#47246=CARTESIAN_POINT('Ctrl Pts',(1.09637279239192,52.1467757754373,0.96943228237084));
#47247=CARTESIAN_POINT('Ctrl Pts',(1.13293064853169,52.1497756956224,0.928087425645212));
#47248=CARTESIAN_POINT('Ctrl Pts',(1.16718860656678,52.1527756158076,0.884624197387474));
#47249=CARTESIAN_POINT('Ctrl Pts',(1.19889782988811,52.1557755359927,0.839330830775079));
#47250=CARTESIAN_POINT('Ctrl Pts',(1.23058787083203,52.1587736413873,0.794064864217351));
#47251=CARTESIAN_POINT('Ctrl Pts',(1.25973193015169,52.1617717467818,0.74697138590056));
#47252=CARTESIAN_POINT('Ctrl Pts',(1.28612256760004,52.1647698521763,0.698370239278483));
#47253=CARTESIAN_POINT('Ctrl Pts',(1.3125077001896,52.167767332192,0.649779230435358));
#47254=CARTESIAN_POINT('Ctrl Pts',(1.33614029905837,52.1707648122077,0.599681642236049));
#47255=CARTESIAN_POINT('Ctrl Pts',(1.35685843015397,52.1737622922233,0.548422693294248));
#47256=CARTESIAN_POINT('Ctrl Pts',(1.37759572276949,52.1767625445099,0.497116336631775));
#47257=CARTESIAN_POINT('Ctrl Pts',(1.39541296315079,52.1797627967966,0.444646964508727));
#47258=CARTESIAN_POINT('Ctrl Pts',(1.41019664017959,52.1827630490832,0.39137921000763));
#47259=CARTESIAN_POINT('Ctrl Pts',(1.42498695381579,52.1857646482267,0.338087542837671));
#47260=CARTESIAN_POINT('Ctrl Pts',(1.43674087678561,52.1887662473701,0.283997296585355));
#47261=CARTESIAN_POINT('Ctrl Pts',(1.44539584476812,52.1917678465136,0.229484426327902));
#47262=CARTESIAN_POINT('Ctrl Pts',(1.45406746110791,52.1947752194155,0.174866697249202));
#47263=CARTESIAN_POINT('Ctrl Pts',(1.45962815996977,52.1977825923175,0.119825247692324));
#47264=CARTESIAN_POINT('Ctrl Pts',(1.46206731419165,52.2007899652194,0.0647411675243254));
#47265=CARTESIAN_POINT('Ctrl Pts',(1.46404811401639,52.2032322067406,0.0200082288015758));
#47266=CARTESIAN_POINT('Ctrl Pts',(1.46397131916159,52.2056744482617,-0.0247526510507388));
#47267=CARTESIAN_POINT('Ctrl Pts',(1.46185644726803,52.2081166897829,-0.0693395816318449));
#47268=CARTESIAN_POINT('Ctrl Pts',(1.45925136617019,52.2111250219861,-0.124261381113747));
#47269=CARTESIAN_POINT('Ctrl Pts',(1.45354131146121,52.2141333541893,-0.179153290527361));
#47270=CARTESIAN_POINT('Ctrl Pts',(1.44473058552518,52.2171416863925,-0.233636010169793));
#47271=CARTESIAN_POINT('Ctrl Pts',(1.4359356899653,52.2201446134758,-0.28802083981412));
#47272=CARTESIAN_POINT('Ctrl Pts',(1.42405126211438,52.2231475405591,-0.341997420855086));
#47273=CARTESIAN_POINT('Ctrl Pts',(1.40913348218309,52.2261504676424,-0.395189928250392));
#47274=CARTESIAN_POINT('Ctrl Pts',(1.39423063976656,52.2291503878261,-0.448329172769607));
#47275=CARTESIAN_POINT('Ctrl Pts',(1.37630060379322,52.2321503080097,-0.500685392135842));
#47276=CARTESIAN_POINT('Ctrl Pts',(1.35545053637126,52.2351502281933,-0.551893190255918));
#47277=CARTESIAN_POINT('Ctrl Pts',(1.3346130821206,52.2381483335863,-0.603070010407611));
#47278=CARTESIAN_POINT('Ctrl Pts',(1.31085929640091,52.2411464389793,-0.653099297377025));
#47279=CARTESIAN_POINT('Ctrl Pts',(1.28434535208418,52.2441445443723,-0.701633284971403));
#47280=CARTESIAN_POINT('Ctrl Pts',(1.25783693834707,52.2471420243864,-0.750157148795457));
#47281=CARTESIAN_POINT('Ctrl Pts',(1.22856976260241,52.2501395044005,-0.797185868677385));
#47282=CARTESIAN_POINT('Ctrl Pts',(1.19674599977527,52.2531369844147,-0.842396143166551));
#47283=CARTESIAN_POINT('Ctrl Pts',(1.16489280419369,52.2561372366997,-0.887648231155727));
#47284=CARTESIAN_POINT('Ctrl Pts',(1.13047860215334,52.2591374889848,-0.93107807988732));
#47285=CARTESIAN_POINT('Ctrl Pts',(1.09374814527682,52.2621377412699,-0.972392536326513));
#47286=CARTESIAN_POINT('Ctrl Pts',(1.05700119956465,52.2651393404118,-1.01372553942536));
#47287=CARTESIAN_POINT('Ctrl Pts',(1.01793630010504,52.2681409395537,-1.0529408817308));
#47288=CARTESIAN_POINT('Ctrl Pts',(0.976835345856191,52.2711425386956,-1.08978206862015));
#47289=CARTESIAN_POINT('Ctrl Pts',(0.935655331421994,52.274149911596,-1.12669412177324));
#47290=CARTESIAN_POINT('Ctrl Pts',(0.892431852070245,52.2771572844964,-1.16122256470015));
#47291=CARTESIAN_POINT('Ctrl Pts',(0.847479293493252,52.2801646573968,-1.19315174940163));
#47292=CARTESIAN_POINT('Ctrl Pts',(0.810974008240795,52.2826068989302,-1.21908095192766));
#47293=CARTESIAN_POINT('Ctrl Pts',(0.773329118366619,52.2850491404637,-1.2432967432468));
#47294=CARTESIAN_POINT('Ctrl Pts',(0.734724817516778,52.2874913819971,-1.26570600556564));
#47295=CARTESIAN_POINT('Ctrl Pts',(0.687172370372218,52.2904997142004,-1.29330954295674));
#47296=CARTESIAN_POINT('Ctrl Pts',(0.637960756872752,52.2935080464037,-1.31828840483469));
#47297=CARTESIAN_POINT('Ctrl Pts',(0.587410957263806,52.296516378607,-1.34044045644945));
#47298=CARTESIAN_POINT('Ctrl Pts',(0.53695198131096,52.2995193056903,-1.36255270710886));
#47299=CARTESIAN_POINT('Ctrl Pts',(0.48516007083935,52.3025222327737,-1.38184801576162));
#47300=CARTESIAN_POINT('Ctrl Pts',(0.432381427918273,52.305525159857,-1.3981697145881));
#47301=CARTESIAN_POINT('Ctrl Pts',(0.379655633461367,52.3085250800407,-1.41447507012365));
#47302=CARTESIAN_POINT('Ctrl Pts',(0.325945566384239,52.3115250002244,-1.42781255830531));
#47303=CARTESIAN_POINT('Ctrl Pts',(0.271616322349622,52.3145249204081,-1.43807399789902));
#47304=CARTESIAN_POINT('Ctrl Pts',(0.21731994459062,52.3175230258011,-1.44832922987272));
#47305=CARTESIAN_POINT('Ctrl Pts',(0.162405650853886,52.3205211311942,-1.45551200330532));
#47306=CARTESIAN_POINT('Ctrl Pts',(0.107250311706722,52.3235192365872,-1.45956487373423));
#47307=CARTESIAN_POINT('Ctrl Pts',(0.0521064774866472,52.3265167166014,
-1.46361689876938));
#47308=CARTESIAN_POINT('Ctrl Pts',(-0.00327777514903709,52.3295141966155,
-1.4645402783775));
#47309=CARTESIAN_POINT('Ctrl Pts',(-0.0585211746800166,52.3325116766297,
-1.46232948479953));
#47310=CARTESIAN_POINT('Ctrl Pts',(-0.113815667019152,52.3355119289148,
-1.4601166465311));
#47311=CARTESIAN_POINT('Ctrl Pts',(-0.168968516327793,52.3385121811999,
-1.45476386443413));
#47312=CARTESIAN_POINT('Ctrl Pts',(-0.223600683004577,52.341512433485,-1.44631773292036));
#47313=CARTESIAN_POINT('Ctrl Pts',(-0.278257374854556,52.3445140326269,
-1.43786780981546));
#47314=CARTESIAN_POINT('Ctrl Pts',(-0.332392399889933,52.3475156317689,
-1.42632187951638));
#47315=CARTESIAN_POINT('Ctrl Pts',(-0.385637364549656,52.3505172309108,
-1.41177762875858));
#47316=CARTESIAN_POINT('Ctrl Pts',(-0.438984749137255,52.3535246038113,
-1.39720540124987));
#47317=CARTESIAN_POINT('Ctrl Pts',(-0.491438150029499,52.3565319767117,
-1.37962349938454));
#47318=CARTESIAN_POINT('Ctrl Pts',(-0.542645866305165,52.3595393496122,
-1.35917905876375));
#47319=CARTESIAN_POINT('Ctrl Pts',(-0.58423086944253,52.3619815911452,-1.34257644124454));
#47320=CARTESIAN_POINT('Ctrl Pts',(-0.624994623049939,52.3644238326782,
-1.32408702064475));
#47321=CARTESIAN_POINT('Ctrl Pts',(-0.664761154561096,52.3668660742113,
-1.30381166484527));
#47322=CARTESIAN_POINT('Ctrl Pts',(-0.713745227493257,52.3698744064149,
-1.2788366552212));
#47323=CARTESIAN_POINT('Ctrl Pts',(-0.761424339089982,52.3728827386186,
-1.25104405257105));
#47324=CARTESIAN_POINT('Ctrl Pts',(-0.807454563614266,52.3758910708222,
-1.2205938627154));
#47325=CARTESIAN_POINT('Ctrl Pts',(-0.853402084877471,52.3788939979059,
-1.19019838321642));
#47326=CARTESIAN_POINT('Ctrl Pts',(-0.89770616060824,52.3818969249896,-1.15715508131275));
#47327=CARTESIAN_POINT('Ctrl Pts',(-0.940047380002483,52.3848998520733,
-1.121669814763));
#47328=CARTESIAN_POINT('Ctrl Pts',(-0.982346202163917,52.3878997722574,
-1.08622008042345));
#47329=CARTESIAN_POINT('Ctrl Pts',(-1.02268565786927,52.3908996924414,-1.04833356289356));
#47330=CARTESIAN_POINT('Ctrl Pts',(-1.06077682074949,52.3938996126255,-1.00825829357393));
#47331=CARTESIAN_POINT('Ctrl Pts',(-1.09884494052139,52.3968977180189,-0.968207267640473));
#47332=CARTESIAN_POINT('Ctrl Pts',(-1.13466709942395,52.3998958234123,-0.925970496657785));
#47333=CARTESIAN_POINT('Ctrl Pts',(-1.16799060738075,52.4028939288057,-0.881833425920308));
#47334=CARTESIAN_POINT('Ctrl Pts',(-1.20130716434185,52.4058914088203,-0.83770556179425));
#47335=CARTESIAN_POINT('Ctrl Pts',(-1.23212578672651,52.4088888888348,-0.79167860681229));
#47336=CARTESIAN_POINT('Ctrl Pts',(-1.26023501196336,52.4118863688493,-0.744069865417023));
#47337=CARTESIAN_POINT('Ctrl Pts',(-1.28837023450064,52.4148866211348,-0.696417092258431));
#47338=CARTESIAN_POINT('Ctrl Pts',(-1.31379078353157,52.4178868734203,-0.647180066041529));
#47339=CARTESIAN_POINT('Ctrl Pts',(-1.33633019456792,52.4208871257058,-0.596702489592641));
#47340=CARTESIAN_POINT('Ctrl Pts',(-1.35887972387331,52.4238887248481,-0.546202253026419));
#47341=CARTESIAN_POINT('Ctrl Pts',(-1.37854534854324,52.4268903239904,-0.494460851334243));
#47342=CARTESIAN_POINT('Ctrl Pts',(-1.39520930120319,52.4298919231327,-0.441840758459538));
#47343=CARTESIAN_POINT('Ctrl Pts',(-1.41190530798958,52.4328992960336,-0.389119447635857));
#47344=CARTESIAN_POINT('Ctrl Pts',(-1.42558797626905,52.4359066689344,-0.335516582714291));
#47345=CARTESIAN_POINT('Ctrl Pts',(-1.43619013507206,52.4389140418352,-0.281407437573529));
#47346=CARTESIAN_POINT('Ctrl Pts',(-1.44479998605859,52.4413562833653,-0.237466228492767));
#47347=CARTESIAN_POINT('Ctrl Pts',(-1.45137926737774,52.4437985248953,-0.193191457633103));
#47348=CARTESIAN_POINT('Ctrl Pts',(-1.45591726187338,52.4462407664254,-0.148785673299232));
#47349=CARTESIAN_POINT('Ctrl Pts',(-1.46093679807477,52.4489421623359,-0.099667843335173));
#47350=CARTESIAN_POINT('Ctrl Pts',(-1.46347129195106,52.4516435582465,-0.0502917836747106));
#47351=CARTESIAN_POINT('Ctrl Pts',(-1.4634997575168,52.4543449541571,-0.000842465582414598));
#47352=CARTESIAN_POINT('Ctrl Pts',(-1.46349984429797,52.5256550458429,-0.000675085045776301));
#47353=CARTESIAN_POINT('Ctrl Pts',(-1.46348221233139,52.5235656984443,-0.0388989806992069));
#47354=CARTESIAN_POINT('Ctrl Pts',(-1.4619672098159,52.5214763510457,-0.0770868883956254));
#47355=CARTESIAN_POINT('Ctrl Pts',(-1.45896244675631,52.5193870036471,-0.115155672699358));
#47356=CARTESIAN_POINT('Ctrl Pts',(-1.45463605973137,52.5163786714437,-0.169968744878602));
#47357=CARTESIAN_POINT('Ctrl Pts',(-1.44720716417161,52.5133703392402,-0.224654556156892));
#47358=CARTESIAN_POINT('Ctrl Pts',(-1.43669195684029,52.5103620070367,-0.278834128381786));
#47359=CARTESIAN_POINT('Ctrl Pts',(-1.42619564235484,52.5073590799532,-0.332916355278562));
#47360=CARTESIAN_POINT('Ctrl Pts',(-1.41262412003453,52.5043561528696,-0.386493633192423));
#47361=CARTESIAN_POINT('Ctrl Pts',(-1.39604532996566,52.5013532257861,-0.439192084037346));
#47362=CARTESIAN_POINT('Ctrl Pts',(-1.37948314061905,52.4983533056022,-0.49183776671632));
#47363=CARTESIAN_POINT('Ctrl Pts',(-1.35991980613222,52.4953533854183,-0.5436058634614));
#47364=CARTESIAN_POINT('Ctrl Pts',(-1.33747389630939,52.4923534652344,-0.594134519019868));
#47365=CARTESIAN_POINT('Ctrl Pts',(-1.31504156505682,52.4893553598411,-0.644632607454754));
#47366=CARTESIAN_POINT('Ctrl Pts',(-1.28973032877393,52.4863572544478,-0.693892258377518));
#47367=CARTESIAN_POINT('Ctrl Pts',(-1.26170719096556,52.4833591490546,-0.741570774953939));
#47368=CARTESIAN_POINT('Ctrl Pts',(-1.23368989854155,52.4803616690402,-0.789239346203877));
#47369=CARTESIAN_POINT('Ctrl Pts',(-1.20296209561939,52.4773641890257,-0.835326982267059));
#47370=CARTESIAN_POINT('Ctrl Pts',(-1.16973599780358,52.4743667090113,-0.879516881840516));
#47371=CARTESIAN_POINT('Ctrl Pts',(-1.13647917025973,52.471366456726,-0.923747651202649));
#47372=CARTESIAN_POINT('Ctrl Pts',(-1.10071974961237,52.4683662044406,-0.966076753465806));
#47373=CARTESIAN_POINT('Ctrl Pts',(-1.0627115616305,52.4653659521553,-1.00621885630158));
#47374=CARTESIAN_POINT('Ctrl Pts',(-1.02468631122093,52.4623643530131,-1.04637897951043));
#47375=CARTESIAN_POINT('Ctrl Pts',(-0.984410666551524,52.4593627538709,
-1.08434978262169));
#47376=CARTESIAN_POINT('Ctrl Pts',(-0.942174432683029,52.4563611547287,
-1.11988373878649));
#47377=CARTESIAN_POINT('Ctrl Pts',(-0.89985695484988,52.453353781828,-1.15548604667716));
#47378=CARTESIAN_POINT('Ctrl Pts',(-0.85557177787915,52.4503464089273,-1.1886418250489));
#47379=CARTESIAN_POINT('Ctrl Pts',(-0.809639896454233,52.4473390360266,
-1.2191453925064));
#47380=CARTESIAN_POINT('Ctrl Pts',(-0.772339318132137,52.4448967944953,
-1.24391687305007));
#47381=CARTESIAN_POINT('Ctrl Pts',(-0.733953435917443,52.442454552964,-1.266940042379));
#47382=CARTESIAN_POINT('Ctrl Pts',(-0.694665275384337,52.4400123114327,
-1.28812748017236));
#47383=CARTESIAN_POINT('Ctrl Pts',(-0.646270455693958,52.4370039792292,
-1.31422598460214));
#47384=CARTESIAN_POINT('Ctrl Pts',(-0.596299607221141,52.4339956470258,
-1.33764906610797));
#47385=CARTESIAN_POINT('Ctrl Pts',(-0.545079892123478,52.4309873148223,
-1.35820475672951));
#47386=CARTESIAN_POINT('Ctrl Pts',(-0.493952204329986,52.4279843877388,
-1.37872351460377));
#47387=CARTESIAN_POINT('Ctrl Pts',(-0.441580589407029,52.4249814606553,
-1.39638490970809));
#47388=CARTESIAN_POINT('Ctrl Pts',(-0.388315992885773,52.4219785335717,
-1.41104320971016));
#47389=CARTESIAN_POINT('Ctrl Pts',(-0.335104731425083,52.4189786133879,
-1.42568683202067));
#47390=CARTESIAN_POINT('Ctrl Pts',(-0.281002766876122,52.415978693204,-1.43733317602712));
#47391=CARTESIAN_POINT('Ctrl Pts',(-0.226378408317006,52.4129787730202,
-1.44588556471384));
#47392=CARTESIAN_POINT('Ctrl Pts',(-0.171787094561888,52.409980667627,-1.4544327796646));
#47393=CARTESIAN_POINT('Ctrl Pts',(-0.116674534556434,52.4069825622338,
-1.45988966712609));
#47394=CARTESIAN_POINT('Ctrl Pts',(-0.0614192151634559,52.4039844568406,
-1.46221063120493));
#47395=CARTESIAN_POINT('Ctrl Pts',(-0.00617542155252979,52.4009869768262,
-1.46453111115072));
#47396=CARTESIAN_POINT('Ctrl Pts',(0.0492105442026703,52.3979894968119,
-1.46371694433711));
#47397=CARTESIAN_POINT('Ctrl Pts',(0.104357424786168,52.3949920167976,-1.45977456406529));
#47398=CARTESIAN_POINT('Ctrl Pts',(0.159555308910696,52.3919917645123,-1.45582853761526));
#47399=CARTESIAN_POINT('Ctrl Pts',(0.214513137333803,52.388991512227,-1.44874855467913));
#47400=CARTESIAN_POINT('Ctrl Pts',(0.268853518339394,52.3859912599417,-1.43859307508292));
#47401=CARTESIAN_POINT('Ctrl Pts',(0.32321829353139,52.3829896607996,-1.42843303654439));
#47402=CARTESIAN_POINT('Ctrl Pts',(0.376964554247815,52.3799880616575,-1.41519487574425));
#47403=CARTESIAN_POINT('Ctrl Pts',(0.429727152053714,52.3769864625154,-1.39898778578936));
#47404=CARTESIAN_POINT('Ctrl Pts',(0.482591241925535,52.3739790896148,-1.38274952051121));
#47405=CARTESIAN_POINT('Ctrl Pts',(0.534467391389492,52.3709717167142,-1.36353110081879));
#47406=CARTESIAN_POINT('Ctrl Pts',(0.585008687370433,52.3679643438135,-1.34149062080252));
#47407=CARTESIAN_POINT('Ctrl Pts',(0.626052500753326,52.3655221022819,-1.32359188411404));
#47408=CARTESIAN_POINT('Ctrl Pts',(0.666216290259966,52.3630798607503,-1.30383303059522));
#47409=CARTESIAN_POINT('Ctrl Pts',(0.705327333557285,52.3606376192187,-1.28232039776998));
#47410=CARTESIAN_POINT('Ctrl Pts',(0.753503981746238,52.3576292870153,-1.25582132088878));
#47411=CARTESIAN_POINT('Ctrl Pts',(0.800287938591522,52.3546209548119,-1.22654696647804));
#47412=CARTESIAN_POINT('Ctrl Pts',(0.845340466043305,52.3516126226084,-1.19466804865188));
#47413=CARTESIAN_POINT('Ctrl Pts',(0.890312046878343,52.3486096955249,-1.16284640820147));
#47414=CARTESIAN_POINT('Ctrl Pts',(0.933557943449558,52.3456067684414,-1.12842979366184));
#47415=CARTESIAN_POINT('Ctrl Pts',(0.9747653586962,52.3426038413579,-1.09163397963139));
#47416=CARTESIAN_POINT('Ctrl Pts',(1.01593151201406,52.3396039211741,-1.05487501009237));
#47417=CARTESIAN_POINT('Ctrl Pts',(1.05506283468393,52.3366040009902,-1.01574191051119));
#47418=CARTESIAN_POINT('Ctrl Pts',(1.09187832183192,52.3336040808064,-0.9744916522544));
#47419=CARTESIAN_POINT('Ctrl Pts',(1.12867153758691,52.3306059754132,-0.933266348189026));
#47420=CARTESIAN_POINT('Ctrl Pts',(1.16315134293306,52.32760787002,-0.88992681756898));
#47421=CARTESIAN_POINT('Ctrl Pts',(1.19507412492466,52.3246097646268,-0.844766290719245));
#47422=CARTESIAN_POINT('Ctrl Pts',(1.22699024809984,52.3216122846125,-0.799615183965102));
#47423=CARTESIAN_POINT('Ctrl Pts',(1.25635010185372,52.3186148045982,-0.752644266816934));
#47424=CARTESIAN_POINT('Ctrl Pts',(1.28295227970449,52.3156173245838,-0.70417731999905));
#47425=CARTESIAN_POINT('Ctrl Pts',(1.30957906103701,52.3126170722986,-0.655665547691769));
#47426=CARTESIAN_POINT('Ctrl Pts',(1.33344281533899,52.3096168200133,-0.60565544577297));
#47427=CARTESIAN_POINT('Ctrl Pts',(1.35438794004212,52.306616567728,-0.554495769026658));
#47428=CARTESIAN_POINT('Ctrl Pts',(1.37534246731598,52.3036149685859,-0.5033131259583));
#47429=CARTESIAN_POINT('Ctrl Pts',(1.39337558042551,52.3006133694438,-0.450980380244922));
#47430=CARTESIAN_POINT('Ctrl Pts',(1.40838093870219,52.2976117703017,-0.397863521198329));
#47431=CARTESIAN_POINT('Ctrl Pts',(1.42341516069815,52.2946043974011,-0.344644488642768));
#47432=CARTESIAN_POINT('Ctrl Pts',(1.43540987731051,52.2915970245004,-0.290638847159452));
#47433=CARTESIAN_POINT('Ctrl Pts',(1.44430972084507,52.2885896515998,-0.236223792773784));
#47434=CARTESIAN_POINT('Ctrl Pts',(1.45153714764747,52.286147410068,-0.192034159439937));
#47435=CARTESIAN_POINT('Ctrl Pts',(1.45672454183031,52.2837051685362,-0.147574815969591));
#47436=CARTESIAN_POINT('Ctrl Pts',(1.45986754430988,52.2812629270044,-0.103048547154441));
#47437=CARTESIAN_POINT('Ctrl Pts',(1.46373906784771,52.2782545948007,-0.0482014705485008));
#47438=CARTESIAN_POINT('Ctrl Pts',(1.46452364628708,52.2752462625971,0.00698105278430778));
#47439=CARTESIAN_POINT('Ctrl Pts',(1.46218094840775,52.2722379303934,0.0621218489214135));
#47440=CARTESIAN_POINT('Ctrl Pts',(1.45984245969221,52.2692350033097,0.117163572683595));
#47441=CARTESIAN_POINT('Ctrl Pts',(1.45438786698462,52.266232076226,0.172163194004425));
#47442=CARTESIAN_POINT('Ctrl Pts',(1.44582876554686,52.2632291491423,0.226740888939868));
#47443=CARTESIAN_POINT('Ctrl Pts',(1.43727823453342,52.2602292289582,0.281263933979221));
#47444=CARTESIAN_POINT('Ctrl Pts',(1.42562943388078,52.2572293087742,0.335365369639398));
#47445=CARTESIAN_POINT('Ctrl Pts',(1.41094581340977,52.2542293885901,0.38866973334883));
#47446=CARTESIAN_POINT('Ctrl Pts',(1.39627107574074,52.2512312831967,0.441941850780256));
#47447=CARTESIAN_POINT('Ctrl Pts',(1.378565296993,52.2482331778033,0.494417343063966));
#47448=CARTESIAN_POINT('Ctrl Pts',(1.35794267088501,52.2452350724099,0.54573249178483));
#47449=CARTESIAN_POINT('Ctrl Pts',(1.33732434647859,52.2422375923953,0.597036936609169));
#47450=CARTESIAN_POINT('Ctrl Pts',(1.31379057988949,52.2392401123808,0.647181027993167));
#47451=CARTESIAN_POINT('Ctrl Pts',(1.28750412464189,52.2362426323663,0.695819932906582));
#47452=CARTESIAN_POINT('Ctrl Pts',(1.26119335791405,52.2332423800808,0.744503822347745));
#47453=CARTESIAN_POINT('Ctrl Pts',(1.23212506767509,52.2302421277953,0.791679277473329));
#47454=CARTESIAN_POINT('Ctrl Pts',(1.2005078340374,52.2272418755098,0.837026397681));
#47455=CARTESIAN_POINT('Ctrl Pts',(1.16887640696426,52.2242402763675,0.882393874869642));
#47456=CARTESIAN_POINT('Ctrl Pts',(1.13469408260439,52.2212386772252,0.925930964162548));
#47457=CARTESIAN_POINT('Ctrl Pts',(1.09821064151044,52.2182370780829,0.967349800678757));
#47458=CARTESIAN_POINT('Ctrl Pts',(1.06165702229867,52.2152297051821,1.00884830884604));
#47459=CARTESIAN_POINT('Ctrl Pts',(1.02279381580018,52.2122223322812,1.04822004642159));
#47460=CARTESIAN_POINT('Ctrl Pts',(0.981907867256102,52.2092149593804,1.0852138914613));
#47461=CARTESIAN_POINT('Ctrl Pts',(0.948705013861077,52.2067727178504,1.11525602713653));
#47462=CARTESIAN_POINT('Ctrl Pts',(0.914168974229151,52.2043304763203,1.14373065169785));
#47463=CARTESIAN_POINT('Ctrl Pts',(0.878467741568595,52.2018882347902,1.1705241035636));
#47464=CARTESIAN_POINT('Ctrl Pts',(0.834491268894918,52.198879902587,1.20352804813355));
#47465=CARTESIAN_POINT('Ctrl Pts',(0.788558493019324,52.1958715703837,1.23412063783018));
#47466=CARTESIAN_POINT('Ctrl Pts',(0.740964397071321,52.1928632381805,1.2620633947123));
#47467=CARTESIAN_POINT('Ctrl Pts',(0.693455814217933,52.1898603110971,1.28995594638376));
#47468=CARTESIAN_POINT('Ctrl Pts',(0.64429228690314,52.1868573840138,1.31520784746683));
#47469=CARTESIAN_POINT('Ctrl Pts',(0.593799191766317,52.1838544569304,1.33762280552391));
#47470=CARTESIAN_POINT('Ctrl Pts',(0.543356656522229,52.1808545367468,1.36001531897007));
#47471=CARTESIAN_POINT('Ctrl Pts',(0.491587671504272,52.1778546165631,1.37957630275564));
#47472=CARTESIAN_POINT('Ctrl Pts',(0.438842077635214,52.1748546963794,1.39615539281873));
#47473=CARTESIAN_POINT('Ctrl Pts',(0.386128392018362,52.1718565909864,1.41272445342251));
#47474=CARTESIAN_POINT('Ctrl Pts',(0.332439771952628,52.1688584855933,1.42631503715667));
#47475=CARTESIAN_POINT('Ctrl Pts',(0.278143717957992,52.1658603802003,1.43682578003059));
#47476=CARTESIAN_POINT('Ctrl Pts',(0.223858989650928,52.1628629001861,1.44733433045439));
#47477=CARTESIAN_POINT('Ctrl Pts',(0.168967597944205,52.159865420172,1.4547642151376));
#47478=CARTESIAN_POINT('Ctrl Pts',(0.11384751892074,52.1568679401578,1.45906510904606));
#47479=CARTESIAN_POINT('Ctrl Pts',(0.058676461144021,52.1538676878727,1.46336998071023));
#47480=CARTESIAN_POINT('Ctrl Pts',(0.0032768218967902,52.1508674355876,
1.46454003810465));
#47481=CARTESIAN_POINT('Ctrl Pts',(-0.0519695098638592,52.1478671833025,
1.46257697918589));
#47482=CARTESIAN_POINT('Ctrl Pts',(-0.10724064250541,52.1448655841605,1.46061303902145));
#47483=CARTESIAN_POINT('Ctrl Pts',(-0.162357802847613,52.1418639850186,
1.45551322747208));
#47484=CARTESIAN_POINT('Ctrl Pts',(-0.216943665905202,52.1388623858766,
1.44733123224216));
#47485=CARTESIAN_POINT('Ctrl Pts',(-0.271634528190421,52.1358550129762,
1.43913349844677));
#47486=CARTESIAN_POINT('Ctrl Pts',(-0.325791532254495,52.1328476400757,
1.42784184448758));
#47487=CARTESIAN_POINT('Ctrl Pts',(-0.379048114992458,52.1298402671752,
1.4135610268116));
#47488=CARTESIAN_POINT('Ctrl Pts',(-0.422296971245356,52.1273980256422,
1.40196379320987));
#47489=CARTESIAN_POINT('Ctrl Pts',(-0.46495215472597,52.1249557841091,1.38839627300597));
#47490=CARTESIAN_POINT('Ctrl Pts',(-0.506827052270095,52.1225135425761,
1.37293794072682));
#47491=CARTESIAN_POINT('Ctrl Pts',(-0.558408192417141,52.1195052103728,
1.35389649942204));
#47492=CARTESIAN_POINT('Ctrl Pts',(-0.609024760409792,52.1164968781696,
1.33190355763431));
#47493=CARTESIAN_POINT('Ctrl Pts',(-0.658316400906693,52.1134885459664,
1.30707756705456));
#47494=CARTESIAN_POINT('Ctrl Pts',(-0.707519478302657,52.1104856188831,
1.28229618174027));
#47495=CARTESIAN_POINT('Ctrl Pts',(-0.755401883695639,52.1074826917997,
1.25469208458097));
#47496=CARTESIAN_POINT('Ctrl Pts',(-0.801622214624486,52.1044797647164,
1.22443214390204));
#47497=CARTESIAN_POINT('Ctrl Pts',(-0.847796264077206,52.1014798445328,
1.19420250319486));
#47498=CARTESIAN_POINT('Ctrl Pts',(-0.892311095418834,52.0984799243492,
1.1613225748655));
#47499=CARTESIAN_POINT('Ctrl Pts',(-0.934850619701237,52.0954800041656,
1.12600469308268));
#47500=CARTESIAN_POINT('Ctrl Pts',(-0.977364409855472,52.0924818987726,
1.09070817672205));
#47501=CARTESIAN_POINT('Ctrl Pts',(-1.01790485514864,52.0894837933796,1.05297696701299));
#47502=CARTESIAN_POINT('Ctrl Pts',(-1.05618745181737,52.0864856879866,1.01306481363412));
#47503=CARTESIAN_POINT('Ctrl Pts',(-1.09446206306729,52.0834882079725,0.973160985585508));
#47504=CARTESIAN_POINT('Ctrl Pts',(-1.13047939493121,52.0804907279584,0.93107749861966));
#47505=CARTESIAN_POINT('Ctrl Pts',(-1.16399213862248,52.0774932479443,0.887104588661938));
#47506=CARTESIAN_POINT('Ctrl Pts',(-1.19753587715117,52.0744929956592,0.843091009602121));
#47507=CARTESIAN_POINT('Ctrl Pts',(-1.22857007782311,52.0714927433742,0.797184937546463));
#47508=CARTESIAN_POINT('Ctrl Pts',(-1.2568890134035,52.0684924910891,0.749708115192558));
#47509=CARTESIAN_POINT('Ctrl Pts',(-1.28522066176543,52.0654908919472,0.702209979803454));
#47510=CARTESIAN_POINT('Ctrl Pts',(-1.31083436989937,52.0624892928053,0.65314015814533));
#47511=CARTESIAN_POINT('Ctrl Pts',(-1.33357056241619,52.0594876936634,0.602844760329691));
#47512=CARTESIAN_POINT('Ctrl Pts',(-1.35635048938215,52.056480320763,0.552452616257335));
#47513=CARTESIAN_POINT('Ctrl Pts',(-1.37624165184502,52.0534729478626,0.500830681054212));
#47514=CARTESIAN_POINT('Ctrl Pts',(-1.39313321455586,52.0504655749622,0.448343725841303));
#47515=CARTESIAN_POINT('Ctrl Pts',(-1.40685059426998,52.0480233334288,0.405719872322318));
#47516=CARTESIAN_POINT('Ctrl Pts',(-1.41859071834354,52.0455810918954,0.362525986532535));
#47517=CARTESIAN_POINT('Ctrl Pts',(-1.42831912530962,52.0431388503619,0.31896195113959));
#47518=CARTESIAN_POINT('Ctrl Pts',(-1.44470142292229,52.0390262009033,0.245601636803999));
#47519=CARTESIAN_POINT('Ctrl Pts',(-1.45543708182968,52.0349135514447,0.170937601088179));
#47520=CARTESIAN_POINT('Ctrl Pts',(-1.46036746516698,52.030800901986,0.0957032741434123));
#47521=CARTESIAN_POINT('Ctrl Pts',(-1.4624238073246,52.029085616605,0.0643248786693624));
#47522=CARTESIAN_POINT('Ctrl Pts',(-1.46347084113317,52.0273703312239,0.0328475503915992));
#47523=CARTESIAN_POINT('Ctrl Pts',(-1.46349939936907,52.0256550458429,0.00132591340718779));
#47524=CARTESIAN_POINT('Origin',(0.,55.715,0.));
#47525=CARTESIAN_POINT('',(-1.46326096487245,51.4543449563653,2.91466190404779E-5));
#47526=CARTESIAN_POINT('',(-1.46349999166114,51.5256550458102,-0.00015623008169786));
#47527=CARTESIAN_POINT('',(-1.4635,55.715,-1.79227059055215E-16));
#47528=CARTESIAN_POINT('Ctrl Pts',(-1.46111644255208,51.4543449761763,2.9469711106117E-5));
#47529=CARTESIAN_POINT('Ctrl Pts',(-1.46115932464248,51.4674781374027,0.242492190997025));
#47530=CARTESIAN_POINT('Ctrl Pts',(-1.28920392493414,51.5070695293669,0.973365973503329));
#47531=CARTESIAN_POINT('Ctrl Pts',(-0.135188693436253,51.5731191520696,
1.72443892271662));
#47532=CARTESIAN_POINT('Ctrl Pts',(1.37535400909208,51.6524938442836,1.04898375450915));
#47533=CARTESIAN_POINT('Ctrl Pts',(1.62729589757749,51.7318685364977,-0.586407376508306));
#47534=CARTESIAN_POINT('Ctrl Pts',(0.39008234965916,51.811243228712,-1.68517100717997));
#47535=CARTESIAN_POINT('Ctrl Pts',(-1.09934054493347,51.8854019417222,-1.27095135834563));
#47536=CARTESIAN_POINT('Ctrl Pts',(-1.46045977152297,51.9331024239943,-0.388908969420869));
#47537=CARTESIAN_POINT('Ctrl Pts',(-1.46404229631382,51.9543446755284,0.00128158248083468));
#47538=CARTESIAN_POINT('Ctrl Pts',(-1.4634993993698,52.025655045799,0.00132591260086507));
#47539=CARTESIAN_POINT('Ctrl Pts',(-1.46354869863678,52.0226939958363,-0.0530890221102393));
#47540=CARTESIAN_POINT('Ctrl Pts',(-1.46055891101372,52.0197329458736,-0.107594537808096));
#47541=CARTESIAN_POINT('Ctrl Pts',(-1.4545263530835,52.0167718959108,-0.161818843728488));
#47542=CARTESIAN_POINT('Ctrl Pts',(-1.44849874612696,52.013813276108,-0.215998647281014));
#47543=CARTESIAN_POINT('Ctrl Pts',(-1.43943337148726,52.0108546563052,-0.269897158612643));
#47544=CARTESIAN_POINT('Ctrl Pts',(-1.42737854950162,52.0078960365024,-0.323145054770552));
#47545=CARTESIAN_POINT('Ctrl Pts',(-1.4153285359981,52.0049385968473,-0.37637171116587));
#47546=CARTESIAN_POINT('Ctrl Pts',(-1.40029155813435,52.0019811571922,-0.428947736076216));
#47547=CARTESIAN_POINT('Ctrl Pts',(-1.38236704141599,51.9990237175371,-0.480513904904738));
#47548=CARTESIAN_POINT('Ctrl Pts',(-1.36442889580751,51.9960640291954,-0.532119282023224));
#47549=CARTESIAN_POINT('Ctrl Pts',(-1.3435989973952,51.9931043408537,-0.582712751097336));
#47550=CARTESIAN_POINT('Ctrl Pts',(-1.32002617989456,51.990144652512,-0.631951844995319));
#47551=CARTESIAN_POINT('Ctrl Pts',(-1.29644571658337,51.9871840041995,-0.681206909524852));
#47552=CARTESIAN_POINT('Ctrl Pts',(-1.27012082155683,51.984223355887,-0.729106243757953));
#47553=CARTESIAN_POINT('Ctrl Pts',(-1.24124631062107,51.9812627075745,-0.775332087798249));
#47554=CARTESIAN_POINT('Ctrl Pts',(-1.21231567244277,51.9782963042546,-0.821647787184175));
#47555=CARTESIAN_POINT('Ctrl Pts',(-1.18082583043793,51.9753299009347,-0.86628304977985));
#47556=CARTESIAN_POINT('Ctrl Pts',(-1.1470142439362,51.9723634976147,-0.908950259479294));
#47557=CARTESIAN_POINT('Ctrl Pts',(-1.11434198296482,51.9694970511257,-0.9501797418684));
#47558=CARTESIAN_POINT('Ctrl Pts',(-1.07950236031916,51.9666306046367,-0.989571445912857));
#47559=CARTESIAN_POINT('Ctrl Pts',(-1.04274147209032,51.9637641581477,-1.02689944609144));
#47560=CARTESIAN_POINT('Ctrl Pts',(-1.00416096335152,51.9607558259461,-1.06607513815108));
#47561=CARTESIAN_POINT('Ctrl Pts',(-0.963287366499095,51.9577474937445,
-1.10315714890105));
#47562=CARTESIAN_POINT('Ctrl Pts',(-0.920376928025628,51.9547391615429,
-1.13786579189204));
#47563=CARTESIAN_POINT('Ctrl Pts',(-0.877543587442246,51.9517362344612,
-1.1725120732937));
#47564=CARTESIAN_POINT('Ctrl Pts',(-0.832681075231708,51.9487333073795,
-1.20479311914918));
#47565=CARTESIAN_POINT('Ctrl Pts',(-0.78608196587128,51.9457303802978,-1.23446644058554));
#47566=CARTESIAN_POINT('Ctrl Pts',(-0.739529517266323,51.9427304601158,
-1.26411004944554));
#47567=CARTESIAN_POINT('Ctrl Pts',(-0.691244359782136,51.9397305399338,
-1.29115082347741));
#47568=CARTESIAN_POINT('Ctrl Pts',(-0.641550089063736,51.9367306197518,
-1.31538805423431));
#47569=CARTESIAN_POINT('Ctrl Pts',(-0.591885880710703,51.9337325143604,
-1.33961062276806));
#47570=CARTESIAN_POINT('Ctrl Pts',(-0.540814722945341,51.930734408969,-1.36103277794393));
#47571=CARTESIAN_POINT('Ctrl Pts',(-0.488684960241562,51.9277363035776,
-1.37949964104153));
#47572=CARTESIAN_POINT('Ctrl Pts',(-0.436566071355437,51.924738823565,-1.39796265211119));
#47573=CARTESIAN_POINT('Ctrl Pts',(-0.383389514216903,51.9217413435525,
-1.4134714185952));
#47574=CARTESIAN_POINT('Ctrl Pts',(-0.329521581096066,51.9187438635399,
-1.4259199758724));
#47575=CARTESIAN_POINT('Ctrl Pts',(-0.275603827290023,51.9157436112564,
-1.43838004641209));
#47576=CARTESIAN_POINT('Ctrl Pts',(-0.220993936311395,51.9127433589729,
-1.44777413324175));
#47577=CARTESIAN_POINT('Ctrl Pts',(-0.166069804793557,51.9097431066893,
-1.45404713470225));
#47578=CARTESIAN_POINT('Ctrl Pts',(-0.111121017034867,51.9067415075489,
-1.46032295220427));
#47579=CARTESIAN_POINT('Ctrl Pts',(-0.0558582365253506,51.9037399084086,
-1.46347486104163));
#47580=CARTESIAN_POINT('Ctrl Pts',(-0.000662576695014244,51.9007383092682,
-1.46349985001438));
#47581=CARTESIAN_POINT('Ctrl Pts',(0.0546392553450768,51.8977309363692,
-1.46352488705494));
#47582=CARTESIAN_POINT('Ctrl Pts',(0.109873179261047,51.8947235634703,-1.46041101743114));
#47583=CARTESIAN_POINT('Ctrl Pts',(0.164661130782233,51.8917161905713,-1.45420733116345));
#47584=CARTESIAN_POINT('Ctrl Pts',(0.209153588457817,51.8892739490254,-1.44916941240514));
#47585=CARTESIAN_POINT('Ctrl Pts',(0.253351922077775,51.8868317074795,-1.44209483761692));
#47586=CARTESIAN_POINT('Ctrl Pts',(0.297059776139041,51.8843894659336,-1.43303445157478));
#47587=CARTESIAN_POINT('Ctrl Pts',(0.350898736126536,51.8813811337312,-1.42187394570985));
#47588=CARTESIAN_POINT('Ctrl Pts',(0.404222686025515,51.8783728015288,-1.40765132960243));
#47589=CARTESIAN_POINT('Ctrl Pts',(0.456657664065666,51.8753644693263,-1.39043015928528));
#47590=CARTESIAN_POINT('Ctrl Pts',(0.508998431318031,51.8723615422439,-1.37323993052819));
#47591=CARTESIAN_POINT('Ctrl Pts',(0.560452897965904,51.8693586151614,-1.35306200233425));
#47592=CARTESIAN_POINT('Ctrl Pts',(0.610658645679146,51.866355688079,-1.33001062719713));
#47593=CARTESIAN_POINT('Ctrl Pts',(0.66081412122682,51.8633557678963,-1.30698233393012));
#47594=CARTESIAN_POINT('Ctrl Pts',(0.709722876371364,51.8603558477135,-1.28108651255609));
#47595=CARTESIAN_POINT('Ctrl Pts',(0.757040764890917,51.8573559275308,-1.25248613976099));
#47596=CARTESIAN_POINT('Ctrl Pts',(0.80433002862821,51.8543578221387,-1.22390306865599));
#47597=CARTESIAN_POINT('Ctrl Pts',(0.850029881403249,51.8513597167466,-1.19261896174547));
#47598=CARTESIAN_POINT('Ctrl Pts',(0.893821253282568,51.8483616113545,-1.15884244709123));
#47599=CARTESIAN_POINT('Ctrl Pts',(0.937603490659938,51.8453641313413,-1.12507297792621));
#47600=CARTESIAN_POINT('Ctrl Pts',(0.979477619030784,51.8423666513281,-1.08881245612636));
#47601=CARTESIAN_POINT('Ctrl Pts',(1.01915592509,51.8393691713149,-1.05031112074182));
#47602=CARTESIAN_POINT('Ctrl Pts',(1.05887092831282,51.8363689190307,-1.01177417673525));
#47603=CARTESIAN_POINT('Ctrl Pts',(1.09638567101698,51.8333686667466,-0.970992647325472));
#47604=CARTESIAN_POINT('Ctrl Pts',(1.1314488747108,51.8303684144625,-0.928254110637631));
#47605=CARTESIAN_POINT('Ctrl Pts',(1.16652781878599,51.8273668153215,-0.885496387999963));
#47606=CARTESIAN_POINT('Ctrl Pts',(1.19915271761295,51.8243652161806,-0.840780334767258));
#47607=CARTESIAN_POINT('Ctrl Pts',(1.2291143085151,51.8213636170396,-0.794424487666041));
#47608=CARTESIAN_POINT('Ctrl Pts',(1.25913353235958,51.8183562441401,-0.747979472273609));
#47609=CARTESIAN_POINT('Ctrl Pts',(1.28647895112592,51.8153488712407,-0.699888822361476));
#47610=CARTESIAN_POINT('Ctrl Pts',(1.31098672592821,51.8123414983412,-0.650496775118848));
#47611=CARTESIAN_POINT('Ctrl Pts',(1.33088911505348,51.8098992568006,-0.61038624889416));
#47612=CARTESIAN_POINT('Ctrl Pts',(1.34892098079718,51.80745701526,-0.569418040334823));
#47613=CARTESIAN_POINT('Ctrl Pts',(1.36501852540261,51.8050147737194,-0.52778468650357));
#47614=CARTESIAN_POINT('Ctrl Pts',(1.38484734297908,51.8020064415064,-0.476501077825916));
#47615=CARTESIAN_POINT('Ctrl Pts',(1.40182434334399,51.7989981092935,-0.423989098985121));
#47616=CARTESIAN_POINT('Ctrl Pts',(1.41580006576566,51.7959897770805,-0.370597387710631));
#47617=CARTESIAN_POINT('Ctrl Pts',(1.42975067777728,51.7929868499874,-0.31730160620087));
#47618=CARTESIAN_POINT('Ctrl Pts',(1.44071057985552,51.7899839228944,-0.263129736274374));
#47619=CARTESIAN_POINT('Ctrl Pts',(1.44857916261137,51.7869809958013,-0.208448218145759));
#47620=CARTESIAN_POINT('Ctrl Pts',(1.45643986637511,51.7839810756079,-0.153821453873512));
#47621=CARTESIAN_POINT('Ctrl Pts',(1.46121530727312,51.7809811554145,-0.0986865730917024));
#47622=CARTESIAN_POINT('Ctrl Pts',(1.46285572030392,51.7779812352211,-0.0434210959567612));
#47623=CARTESIAN_POINT('Ctrl Pts',(1.46449514097292,51.7749831298184,0.011810948531835));
#47624=CARTESIAN_POINT('Ctrl Pts',(1.46300327682994,51.7719850244156,0.0671729052360835));
#47625=CARTESIAN_POINT('Ctrl Pts',(1.45838231670623,51.7689869190129,0.122283557024521));
#47626=CARTESIAN_POINT('Ctrl Pts',(1.4537623204749,51.765989438989,0.177382713206783));
#47627=CARTESIAN_POINT('Ctrl Pts',(1.44601456840762,51.7629919589652,0.232230141822435));
#47628=CARTESIAN_POINT('Ctrl Pts',(1.43519321561095,51.7599944789413,0.28644839651201));
#47629=CARTESIAN_POINT('Ctrl Pts',(1.42436185450047,51.7569942266466,0.340716795884744));
#47630=CARTESIAN_POINT('Ctrl Pts',(1.41045131650601,51.7539939743519,0.394354338834923));
#47631=CARTESIAN_POINT('Ctrl Pts',(1.39356688884657,51.7509937220573,0.446993933192053));
#47632=CARTESIAN_POINT('Ctrl Pts',(1.37667488152258,51.7479921229058,0.499657158226818));
#47633=CARTESIAN_POINT('Ctrl Pts',(1.3568065133307,51.7449905237543,0.551321047025914));
#47634=CARTESIAN_POINT('Ctrl Pts',(1.33411587080629,51.7419889246029,0.601637011214214));
#47635=CARTESIAN_POINT('Ctrl Pts',(1.3113815814526,51.7389815516931,0.652049761216168));
#47636=CARTESIAN_POINT('Ctrl Pts',(1.28581441695944,51.7359741787833,0.701108936269424));
#47637=CARTESIAN_POINT('Ctrl Pts',(1.25761469449969,51.7329668058736,0.748490167055289));
#47638=CARTESIAN_POINT('Ctrl Pts',(1.23471413201236,51.7305245644174,0.78696773852383));
#47639=CARTESIAN_POINT('Ctrl Pts',(1.21007838239006,51.7280823229613,0.824339144666384));
#47640=CARTESIAN_POINT('Ctrl Pts',(1.18383458759932,51.7256400815051,0.860446348823416));
#47641=CARTESIAN_POINT('Ctrl Pts',(1.15150770510008,51.7226317493178,0.90492289482096));
#47642=CARTESIAN_POINT('Ctrl Pts',(1.11660192598051,51.7196234171304,0.94766997657345));
#47643=CARTESIAN_POINT('Ctrl Pts',(1.07932906361815,51.7166150849431,0.988372916681332));
#47644=CARTESIAN_POINT('Ctrl Pts',(1.04212317001952,51.7136121578756,1.02900272514849));
#47645=CARTESIAN_POINT('Ctrl Pts',(1.0025589870473,51.710609230808,1.06759529338764));
#47646=CARTESIAN_POINT('Ctrl Pts',(0.960889782951117,51.7076063037405,1.10386732672915));
#47647=CARTESIAN_POINT('Ctrl Pts',(0.919262303182719,51.7046063835726,1.14010304005348));
#47648=CARTESIAN_POINT('Ctrl Pts',(0.87553437434542,51.7016064634047,1.17402247559887));
#47649=CARTESIAN_POINT('Ctrl Pts',(0.829996153126448,51.6986065432367,1.20537904237435));
#47650=CARTESIAN_POINT('Ctrl Pts',(0.784485480084899,51.6956084378594,1.23671664011147));
#47651=CARTESIAN_POINT('Ctrl Pts',(0.737167119800396,51.692610332482,1.26549414248036));
#47652=CARTESIAN_POINT('Ctrl Pts',(0.688362516843125,51.6896122271046,1.29150659905608));
#47653=CARTESIAN_POINT('Ctrl Pts',(0.639568094102268,51.686614747106,1.31751362965921));
#47654=CARTESIAN_POINT('Ctrl Pts',(0.58928851070837,51.6836172671073,1.34075651104833));
#47655=CARTESIAN_POINT('Ctrl Pts',(0.537870232273453,51.6806197871087,1.36107599465794));
#47656=CARTESIAN_POINT('Ctrl Pts',(0.486404398753673,51.6776195348388,1.3814142710937));
#47657=CARTESIAN_POINT('Ctrl Pts',(0.433798258887482,51.6746192825689,1.39882355260789));
#47658=CARTESIAN_POINT('Ctrl Pts',(0.380417316169004,51.671619030299,1.4131931628616));
#47659=CARTESIAN_POINT('Ctrl Pts',(0.327012409967135,51.6686174311722,1.42756922384284));
#47660=CARTESIAN_POINT('Ctrl Pts',(0.272832526168473,51.6656158320453,1.43890278480729));
#47661=CARTESIAN_POINT('Ctrl Pts',(0.218254094321258,51.6626142329184,1.44713420259215));
#47662=CARTESIAN_POINT('Ctrl Pts',(0.163570677532388,51.6596068600326,1.45538145401103));
#47663=CARTESIAN_POINT('Ctrl Pts',(0.108487709142944,51.6565994871467,1.46051459160544));
#47664=CARTESIAN_POINT('Ctrl Pts',(0.0533863500468608,51.6535921142609,
1.46252594767706));
#47665=CARTESIAN_POINT('Ctrl Pts',(0.0086393766485887,51.6511498726043,
1.46415933926862));
#47666=CARTESIAN_POINT('Ctrl Pts',(-0.0361195599308845,51.6487076309477,
1.46373498102298));
#47667=CARTESIAN_POINT('Ctrl Pts',(-0.0806887268960853,51.6462653892911,
1.46127395766567));
#47668=CARTESIAN_POINT('Ctrl Pts',(-0.135588642225334,51.6432570570899,
1.45824249032761));
#47669=CARTESIAN_POINT('Ctrl Pts',(-0.190434558441944,51.6402487248887,
1.45210637508921));
#47670=CARTESIAN_POINT('Ctrl Pts',(-0.244847220686593,51.6372403926875,
1.44287285944467));
#47671=CARTESIAN_POINT('Ctrl Pts',(-0.299162118801187,51.6342374656065,
1.43365593381039));
#47672=CARTESIAN_POINT('Ctrl Pts',(-0.353044790576555,51.6312345385255,
1.42135273906261));
#47673=CARTESIAN_POINT('Ctrl Pts',(-0.406119858537471,51.6282316114445,
1.4060223719776));
#47674=CARTESIAN_POINT('Ctrl Pts',(-0.459141781213952,51.6252316912634,
1.39070735554121));
#47675=CARTESIAN_POINT('Ctrl Pts',(-0.511357196357732,51.6222317710822,
1.37237131696433));
#47676=CARTESIAN_POINT('Ctrl Pts',(-0.562401550999693,51.6192318509011,
1.35112425240358));
#47677=CARTESIAN_POINT('Ctrl Pts',(-0.613415026545028,51.6162337455108,
1.32989004117723));
#47678=CARTESIAN_POINT('Ctrl Pts',(-0.663258358355904,51.6132356401204,
1.30574849693959));
#47679=CARTESIAN_POINT('Ctrl Pts',(-0.711585003397819,51.6102375347301,
1.27885848823837));
#47680=CARTESIAN_POINT('Ctrl Pts',(-0.759901567916541,51.6072400547188,
1.25197408856207));
#47681=CARTESIAN_POINT('Ctrl Pts',(-0.806701611939131,51.6042425747075,
1.22234261976295));
#47682=CARTESIAN_POINT('Ctrl Pts',(-0.851663413638878,51.6012450946962,
1.19016876108768));
#47683=CARTESIAN_POINT('Ctrl Pts',(-0.896666799031075,51.5982448424141,
1.1579651458681));
#47684=CARTESIAN_POINT('Ctrl Pts',(-0.939828114034045,51.5952445901321,
1.12321475098883));
#47685=CARTESIAN_POINT('Ctrl Pts',(-0.980856114933589,51.5922443378501,
1.08616459700977));
#47686=CARTESIAN_POINT('Ctrl Pts',(-1.02190253389697,51.5892427387113,1.04909781067996));
#47687=CARTESIAN_POINT('Ctrl Pts',(-1.06081335713255,51.5862411395726,1.00972958400529));
#47688=CARTESIAN_POINT('Ctrl Pts',(-1.09733428667997,51.5832395404339,0.968343799110916));
#47689=CARTESIAN_POINT('Ctrl Pts',(-1.13392546645469,51.5802321675368,0.926878406144349));
#47690=CARTESIAN_POINT('Ctrl Pts',(-1.16811724047725,51.5772247946397,0.883388118469462));
#47691=CARTESIAN_POINT('Ctrl Pts',(-1.19969640843694,51.5742174217426,0.838188986794449));
#47692=CARTESIAN_POINT('Ctrl Pts',(-1.22534136797843,51.5717751801874,0.801483462931507));
#47693=CARTESIAN_POINT('Ctrl Pts',(-1.2492641189705,51.5693329386321,0.76365167332456));
#47694=CARTESIAN_POINT('Ctrl Pts',(-1.27137294561791,51.5668906970769,0.724874529246846));
#47695=CARTESIAN_POINT('Ctrl Pts',(-1.2997668503311,51.5637541772103,0.675073852279607));
#47696=CARTESIAN_POINT('Ctrl Pts',(-1.32528023419885,51.5606176573437,0.623516209451306));
#47697=CARTESIAN_POINT('Ctrl Pts',(-1.34770252112457,51.5574811374771,0.570552508148441));
#47698=CARTESIAN_POINT('Ctrl Pts',(-1.37006162486433,51.5543534559292,0.517738051898046));
#47699=CARTESIAN_POINT('Ctrl Pts',(-1.38934677995713,51.5512257743813,0.463525844821878));
#47700=CARTESIAN_POINT('Ctrl Pts',(-1.40539355836495,51.5480980928334,0.408290578027837));
#47701=CARTESIAN_POINT('Ctrl Pts',(-1.42141300606684,51.5449757383202,0.353149387365186));
#47702=CARTESIAN_POINT('Ctrl Pts',(-1.43420490088096,51.5418533838069,0.296989040883462));
#47703=CARTESIAN_POINT('Ctrl Pts',(-1.44365328872406,51.5387310292937,0.240202897476707));
#47704=CARTESIAN_POINT('Ctrl Pts',(-1.45308371483079,51.5356146104924,0.183524706638624));
#47705=CARTESIAN_POINT('Ctrl Pts',(-1.45918319990495,51.5324981916911,0.12622354192248));
#47706=CARTESIAN_POINT('Ctrl Pts',(-1.4618864308277,51.5293817728898,0.0687045366903423));
#47707=CARTESIAN_POINT('Ctrl Pts',(-1.46296397147466,51.5281395305409,0.0457767632662445));
#47708=CARTESIAN_POINT('Ctrl Pts',(-1.46350244379955,51.5268972881919,0.0228144961225602));
#47709=CARTESIAN_POINT('Ctrl Pts',(-1.46349999166121,51.5256550458429,-0.00015622947666356));
#47710=CARTESIAN_POINT('Origin',(0.,55.715,0.));
#47711=CARTESIAN_POINT('',(-1.46349942146382,50.9543449542045,-0.00130129745633658));
#47712=CARTESIAN_POINT('',(-1.46349947235337,51.0256550458841,-0.00124274752362485));
#47713=CARTESIAN_POINT('',(-1.4635,55.715,-1.79227059055215E-16));
#47714=CARTESIAN_POINT('Ctrl Pts',(-1.46349942146382,50.9543449542045,-0.00130129745634145));
#47715=CARTESIAN_POINT('Ctrl Pts',(-1.46354775243707,50.9573044486033,0.0530539547187437));
#47716=CARTESIAN_POINT('Ctrl Pts',(-1.4605636570072,50.9602639430021,0.107505650961708));
#47717=CARTESIAN_POINT('Ctrl Pts',(-1.45454150093415,50.963223437401,0.161682627577081));
#47718=CARTESIAN_POINT('Ctrl Pts',(-1.44852471886776,50.9661802908283,0.215811258146704));
#47719=CARTESIAN_POINT('Ctrl Pts',(-1.4394753011775,50.9691371442556,0.269665114545852));
#47720=CARTESIAN_POINT('Ctrl Pts',(-1.42743962380975,50.972093997683,0.322875162218907));
#47721=CARTESIAN_POINT('Ctrl Pts',(-1.41540959591354,50.9750494631818,0.376060233429001));
#47722=CARTESIAN_POINT('Ctrl Pts',(-1.40039620510289,50.9780049286807,0.428601563323481));
#47723=CARTESIAN_POINT('Ctrl Pts',(-1.38249699180053,50.9809603941795,0.480139893846038));
#47724=CARTESIAN_POINT('Ctrl Pts',(-1.36405759284825,50.9840050535454,0.53323361488209));
#47725=CARTESIAN_POINT('Ctrl Pts',(-1.3425554930314,50.9870497129113,0.5852622190069));
#47726=CARTESIAN_POINT('Ctrl Pts',(-1.31815189464282,50.9900943722772,0.635852052485128));
#47727=CARTESIAN_POINT('Ctrl Pts',(-1.29443999713118,50.9930527331587,0.685007956768811));
#47728=CARTESIAN_POINT('Ctrl Pts',(-1.26798925696604,50.9960110940403,0.732805119962041));
#47729=CARTESIAN_POINT('Ctrl Pts',(-1.23899417013095,50.9989694549218,0.778925989026888));
#47730=CARTESIAN_POINT('Ctrl Pts',(-1.20873035773429,51.0020572635299,0.827064949150997));
#47731=CARTESIAN_POINT('Ctrl Pts',(-1.17569472915931,51.0051450721379,0.873376958923684));
#47732=CARTESIAN_POINT('Ctrl Pts',(-1.14015637285819,51.008232880746,0.917537844140967));
#47733=CARTESIAN_POINT('Ctrl Pts',(-1.10461801655707,51.011320689354,0.961698729358252));
#47734=CARTESIAN_POINT('Ctrl Pts',(-1.0665774408942,51.0144084979621,1.00370805193639));
#47735=CARTESIAN_POINT('Ctrl Pts',(-1.02634574315155,51.0174963065702,1.04328647336899));
#47736=CARTESIAN_POINT('Ctrl Pts',(-0.987149488474935,51.0205046442587,
1.08184626510569));
#47737=CARTESIAN_POINT('Ctrl Pts',(-0.945693589253863,51.0235129819473,
1.11827630448752));
#47738=CARTESIAN_POINT('Ctrl Pts',(-0.902238692061223,51.0265213196358,
1.15230099910902));
#47739=CARTESIAN_POINT('Ctrl Pts',(-0.858861867268464,51.0295242524527,
1.18626456392156));
#47740=CARTESIAN_POINT('Ctrl Pts',(-0.813493584401582,51.0325271852696,
1.21783103629103));
#47741=CARTESIAN_POINT('Ctrl Pts',(-0.766430224103125,51.0355301180865,
1.24676259230907));
#47742=CARTESIAN_POINT('Ctrl Pts',(-0.719413987022348,51.0385300441513,
1.27566517997459));
#47743=CARTESIAN_POINT('Ctrl Pts',(-0.670706482677944,51.0415299702161,
1.30193780161427));
#47744=CARTESIAN_POINT('Ctrl Pts',(-0.620634447017156,51.0445298962809,
1.32538490001045));
#47745=CARTESIAN_POINT('Ctrl Pts',(-0.570592699902108,51.0475280076922,
1.34881781527022));
#47746=CARTESIAN_POINT('Ctrl Pts',(-0.5191885353183,51.0505261191034,1.36942837083828));
#47747=CARTESIAN_POINT('Ctrl Pts',(-0.466772708834034,51.0535242305147,
1.38706722558344));
#47748=CARTESIAN_POINT('Ctrl Pts',(-0.414367813600106,51.0565217166738,
1.40470240176909));
#47749=CARTESIAN_POINT('Ctrl Pts',(-0.360952176354885,51.0595192028329,
1.41936693908409));
#47750=CARTESIAN_POINT('Ctrl Pts',(-0.306893723269394,51.062516688992,1.43096068870457));
#47751=CARTESIAN_POINT('Ctrl Pts',(-0.252785270710211,51.0655169475711,
1.44256516155788));
#47752=CARTESIAN_POINT('Ctrl Pts',(-0.19803333262019,51.0685172061501,1.45109306056883));
#47753=CARTESIAN_POINT('Ctrl Pts',(-0.143016632303413,51.0715174647291,
1.45649527733));
#47754=CARTESIAN_POINT('Ctrl Pts',(-0.0879752325467467,51.0745190702574,
1.46189991938616));
#47755=CARTESIAN_POINT('Ctrl Pts',(-0.0326693630243806,51.0775206757857,
1.46417605998132));
#47756=CARTESIAN_POINT('Ctrl Pts',(0.0225198617747103,51.0805222813141,
1.4633267255899));
#47757=CARTESIAN_POINT('Ctrl Pts',(0.0778152475168805,51.0835296606737,
1.46247575743499));
#47758=CARTESIAN_POINT('Ctrl Pts',(0.132993011308516,51.0865370400333,1.45848734130476));
#47759=CARTESIAN_POINT('Ctrl Pts',(0.187675912787505,51.0895444193929,1.45141655005011));
#47760=CARTESIAN_POINT('Ctrl Pts',(0.23208208519796,51.0919866125234,1.44567459475806));
#47761=CARTESIAN_POINT('Ctrl Pts',(0.276161922100405,51.0944288056539,1.4379009804281));
#47762=CARTESIAN_POINT('Ctrl Pts',(0.319719910248125,51.0968709987844,1.42814965216917));
#47763=CARTESIAN_POINT('Ctrl Pts',(0.373375188595168,51.0998793230382,1.41613784321666));
#47764=CARTESIAN_POINT('Ctrl Pts',(0.426467031557936,51.1028876472921,1.40107248196408));
#47765=CARTESIAN_POINT('Ctrl Pts',(0.478622532392679,51.1058959715459,1.38302303722173));
#47766=CARTESIAN_POINT('Ctrl Pts',(0.530684320895155,51.1088988904815,1.36500602348926));
#47767=CARTESIAN_POINT('Ctrl Pts',(0.581812610201623,51.1119018094171,1.34401573773514));
#47768=CARTESIAN_POINT('Ctrl Pts',(0.631646838239741,51.1149047283526,1.32017215610001));
#47769=CARTESIAN_POINT('Ctrl Pts',(0.681431164075527,51.1179046402732,1.29635245056935));
#47770=CARTESIAN_POINT('Ctrl Pts',(0.729923520747108,51.1209045521939,1.26968533580423));
#47771=CARTESIAN_POINT('Ctrl Pts',(0.776782387469093,51.1239044641145,1.24033921671364));
#47772=CARTESIAN_POINT('Ctrl Pts',(0.823612905445474,51.126902561144,1.21101085148103));
#47773=CARTESIAN_POINT('Ctrl Pts',(0.868811444729117,51.1299006581735,1.17900697421605));
#47774=CARTESIAN_POINT('Ctrl Pts',(0.912062280534688,51.1328987552031,1.14454123841208));
#47775=CARTESIAN_POINT('Ctrl Pts',(0.955304093326832,51.1358962267679,1.11008269286909));
#47776=CARTESIAN_POINT('Ctrl Pts',(0.996598596050201,51.1388936983328,1.0731636379759));
#47777=CARTESIAN_POINT('Ctrl Pts',(1.03566207553139,51.1418911698976,1.03403883645926));
#47778=CARTESIAN_POINT('Ctrl Pts',(1.07476168278522,51.1448914136674,0.994877850456428));
#47779=CARTESIAN_POINT('Ctrl Pts',(1.11162576951702,51.1478916574373,0.953507416879683));
#47780=CARTESIAN_POINT('Ctrl Pts',(1.14600764409953,51.1508919012071,0.910219055868122));
#47781=CARTESIAN_POINT('Ctrl Pts',(1.1804049526737,51.1538934917835,0.866911262751374));
#47782=CARTESIAN_POINT('Ctrl Pts',(1.21231752230337,51.15689508236,0.821684258810234));
#47783=CARTESIAN_POINT('Ctrl Pts',(1.2415411621936,51.1598966729364,0.774859853508333));
#47784=CARTESIAN_POINT('Ctrl Pts',(1.27082101594373,51.1629040372972,0.727945377956145));
#47785=CARTESIAN_POINT('Ctrl Pts',(1.2974013515941,51.1659114016579,0.679427827356803));
#47786=CARTESIAN_POINT('Ctrl Pts',(1.3211238034719,51.1689187660186,0.629653989028841));
#47787=CARTESIAN_POINT('Ctrl Pts',(1.34038902537399,51.1713610743452,0.589232195984588));
#47788=CARTESIAN_POINT('Ctrl Pts',(1.35777027111542,51.1738033826719,0.54798240600597));
#47789=CARTESIAN_POINT('Ctrl Pts',(1.37320679552036,51.1762456909985,0.506098159191196));
#47790=CARTESIAN_POINT('Ctrl Pts',(1.39222087281822,51.179254026171,0.454506862756334));
#47791=CARTESIAN_POINT('Ctrl Pts',(1.40836402779826,51.1822623613435,0.401732519203797));
#47792=CARTESIAN_POINT('Ctrl Pts',(1.4214923408129,51.185270696516,0.348126090677296));
#47793=CARTESIAN_POINT('Ctrl Pts',(1.43459706619233,51.1882736266137,0.294615976801396));
#47794=CARTESIAN_POINT('Ctrl Pts',(1.44469757393154,51.1912765567115,0.240277254096569));
#47795=CARTESIAN_POINT('Ctrl Pts',(1.4516990716003,51.1942794868093,0.185477911123728));
#47796=CARTESIAN_POINT('Ctrl Pts',(1.45869355857537,51.1972794100328,0.130733439469351));
#47797=CARTESIAN_POINT('Ctrl Pts',(1.46259511539236,51.2002793332563,0.0755297831083064));
#47798=CARTESIAN_POINT('Ctrl Pts',(1.46335996314126,51.2032792564798,0.0202452037584424));
#47799=CARTESIAN_POINT('Ctrl Pts',(1.46412434820389,51.2062773649326,-0.0350059317910204));
#47800=CARTESIAN_POINT('Ctrl Pts',(1.4617557775826,51.2092754733855,-0.0903373655677598));
#47801=CARTESIAN_POINT('Ctrl Pts',(1.45626247824288,51.2122735818383,-0.145367962295394));
#47802=CARTESIAN_POINT('Ctrl Pts',(1.45077032473011,51.2152710649268,-0.200387080394777));
#47803=CARTESIAN_POINT('Ctrl Pts',(1.44215478914101,51.2182685480153,-0.255104960072816));
#47804=CARTESIAN_POINT('Ctrl Pts',(1.43047599846893,51.2212660311038,-0.309145059485551));
#47805=CARTESIAN_POINT('Ctrl Pts',(1.41878640648588,51.2242662864611,-0.363235138723685));
#47806=CARTESIAN_POINT('Ctrl Pts',(1.4040280106138,51.2272665418184,-0.416645667089213));
#47807=CARTESIAN_POINT('Ctrl Pts',(1.38631189953782,51.2302667971757,-0.469011265536161));
#47808=CARTESIAN_POINT('Ctrl Pts',(1.36858783542824,51.2332683993936,-0.521400371702286));
#47809=CARTESIAN_POINT('Ctrl Pts',(1.34790360719099,51.2362700016115,-0.572743121336616));
#47810=CARTESIAN_POINT('Ctrl Pts',(1.32441880362076,51.2392716038293,-0.622693409805949));
#47811=CARTESIAN_POINT('Ctrl Pts',(1.30088882590766,51.2422789797726,-0.672739780044094));
#47812=CARTESIAN_POINT('Ctrl Pts',(1.27454776293348,51.2452863557159,-0.72138787160505));
#47813=CARTESIAN_POINT('Ctrl Pts',(1.24560104472301,51.2482937316593,-0.768316528121675));
#47814=CARTESIAN_POINT('Ctrl Pts',(1.22209411576546,51.2507359488437,-0.806426153772103));
#47815=CARTESIAN_POINT('Ctrl Pts',(1.1968697725791,51.2531781660282,-0.8434022913186));
#47816=CARTESIAN_POINT('Ctrl Pts',(1.17005764014261,51.2556203832127,-0.879088942453439));
#47817=CARTESIAN_POINT('Ctrl Pts',(1.13703035115398,51.2586287158366,-0.923047898081409));
#47818=CARTESIAN_POINT('Ctrl Pts',(1.10145188110206,51.2616370484605,-0.96523675864193));
#47819=CARTESIAN_POINT('Ctrl Pts',(1.06353900112097,51.2646453810844,-1.00534424109089));
#47820=CARTESIAN_POINT('Ctrl Pts',(1.025694239492,51.2676483086148,-1.04537966212922));
#47821=CARTESIAN_POINT('Ctrl Pts',(0.985523751349286,51.2706512361452,-1.08334074485816));
#47822=CARTESIAN_POINT('Ctrl Pts',(0.943285260418776,51.2736541636756,-1.11894824164332));
#47823=CARTESIAN_POINT('Ctrl Pts',(0.901089063627699,51.2766540843221,-1.15452008401942));
#47824=CARTESIAN_POINT('Ctrl Pts',(0.856829368080939,51.2796540049687,-1.18774266942952));
#47825=CARTESIAN_POINT('Ctrl Pts',(0.810800199953619,51.2826539256153,-1.21837403360182));
#47826=CARTESIAN_POINT('Ctrl Pts',(0.764798876766984,51.2856520314862,-1.2489868675996));
#47827=CARTESIAN_POINT('Ctrl Pts',(0.717030641866566,51.2886501373571,-1.2770112946511));
#47828=CARTESIAN_POINT('Ctrl Pts',(0.667820145829448,51.2916482432281,-1.30224748140449));
#47829=CARTESIAN_POINT('Ctrl Pts',(0.618619914441686,51.2946457237343,-1.32747840422784));
#47830=CARTESIAN_POINT('Ctrl Pts',(0.567978489586788,51.2976432042406,-1.34992200033207));
#47831=CARTESIAN_POINT('Ctrl Pts',(0.516244815862946,51.3006406847469,-1.36942452880567));
#47832=CARTESIAN_POINT('Ctrl Pts',(0.464463295053354,51.3036409375424,-1.3889450946442));
#47833=CARTESIAN_POINT('Ctrl Pts',(0.411588002911127,51.3066411903379,-1.40551897085507));
#47834=CARTESIAN_POINT('Ctrl Pts',(0.357986150186023,51.3096414431334,-1.41904128420388));
#47835=CARTESIAN_POINT('Ctrl Pts',(0.304360234619387,51.3126430427967,-1.43256966796381));
#47836=CARTESIAN_POINT('Ctrl Pts',(0.250007628546447,51.3156446424599,-1.44304365767043));
#47837=CARTESIAN_POINT('Ctrl Pts',(0.195305659078757,51.3186462421232,-1.45040957992279));
#47838=CARTESIAN_POINT('Ctrl Pts',(0.140498466852667,51.3216536155566,-1.45778967100061));
#47839=CARTESIAN_POINT('Ctrl Pts',(0.085341097405475,51.32466098899,-1.46204970956164));
#47840=CARTESIAN_POINT('Ctrl Pts',(0.0302147853571012,51.3276683624233,
-1.46318806608919));
#47841=CARTESIAN_POINT('Ctrl Pts',(-0.0145523706873162,51.3301106000912,
-1.46411250638656));
#47842=CARTESIAN_POINT('Ctrl Pts',(-0.0592988958543302,51.3325528377591,
-1.46297927242488));
#47843=CARTESIAN_POINT('Ctrl Pts',(-0.103823417662204,51.334995075427,-1.45981264138414));
#47844=CARTESIAN_POINT('Ctrl Pts',(-0.158668410827807,51.3380034066288,
-1.45591200751464));
#47845=CARTESIAN_POINT('Ctrl Pts',(-0.21341023872285,51.3410117378307,-1.44890797275119));
#47846=CARTESIAN_POINT('Ctrl Pts',(-0.267669809080525,51.3440200690326,
-1.4388137903519));
#47847=CARTESIAN_POINT('Ctrl Pts',(-0.321831889869015,51.3470229950882,
-1.42873774443041));
#47848=CARTESIAN_POINT('Ctrl Pts',(-0.375512916934494,51.3500259211439,
-1.4155826645423));
#47849=CARTESIAN_POINT('Ctrl Pts',(-0.428338496100367,51.3530288471995,
-1.39941358531296));
#47850=CARTESIAN_POINT('Ctrl Pts',(-0.481111179516009,51.3560287663401,
-1.38326069664111));
#47851=CARTESIAN_POINT('Ctrl Pts',(-0.533029608593966,51.3590286854808,
-1.36409994071798));
#47852=CARTESIAN_POINT('Ctrl Pts',(-0.583731018456037,51.3620286046214,
-1.34204707372442));
#47853=CARTESIAN_POINT('Ctrl Pts',(-0.634401756449242,51.3650267089579,
-1.32000754763492));
#47854=CARTESIAN_POINT('Ctrl Pts',(-0.683856450380088,51.3680248132945,
-1.29507958848854));
#47855=CARTESIAN_POINT('Ctrl Pts',(-0.731751117097538,51.371022917631,-1.26742753348131));
#47856=CARTESIAN_POINT('Ctrl Pts',(-0.77963579321242,51.374020396577,-1.23978124656289));
#47857=CARTESIAN_POINT('Ctrl Pts',(-0.825960630477322,51.3770178755231,
-1.20941225633633));
#47858=CARTESIAN_POINT('Ctrl Pts',(-0.870407189400394,51.3800153544691,
-1.17653031182376));
#47859=CARTESIAN_POINT('Ctrl Pts',(-0.914894855361113,51.3830156056766,
-1.14361795597308));
#47860=CARTESIAN_POINT('Ctrl Pts',(-0.957500345878216,51.386015856884,-1.10818831725159));
#47861=CARTESIAN_POINT('Ctrl Pts',(-0.997936366369565,51.3890161080915,
-1.070492997958));
#47862=CARTESIAN_POINT('Ctrl Pts',(-1.03839053908992,51.3920177061488,-1.03278075677002));
#47863=CARTESIAN_POINT('Ctrl Pts',(-1.07667293382798,51.395019304206,-0.99280119012461));
#47864=CARTESIAN_POINT('Ctrl Pts',(-1.11253378095445,51.3980209022633,-0.950842172095447));
#47865=CARTESIAN_POINT('Ctrl Pts',(-1.1484636086523,51.4010282740812,-0.908802443283636));
#47866=CARTESIAN_POINT('Ctrl Pts',(-1.18196226166673,51.4040356458992,-0.864776078176582));
#47867=CARTESIAN_POINT('Ctrl Pts',(-1.21282157236841,51.4070430177172,-0.819082464467298));
#47868=CARTESIAN_POINT('Ctrl Pts',(-1.23788204222071,51.4094852676918,-0.78197523806571));
#47869=CARTESIAN_POINT('Ctrl Pts',(-1.26120266896233,51.4119275176664,-0.743769156872513));
#47870=CARTESIAN_POINT('Ctrl Pts',(-1.28269461278464,51.4143697676411,-0.704646564125072));
#47871=CARTESIAN_POINT('Ctrl Pts',(-1.31048195579659,51.4175273990925,-0.654064219727654));
#47872=CARTESIAN_POINT('Ctrl Pts',(-1.33532006112789,51.420685030544,-0.601751349239927));
#47873=CARTESIAN_POINT('Ctrl Pts',(-1.3570020772859,51.4238426619954,-0.548067160338722));
#47874=CARTESIAN_POINT('Ctrl Pts',(-1.3786187933309,51.4269907835522,-0.494544653062373));
#47875=CARTESIAN_POINT('Ctrl Pts',(-1.39709816577733,51.4301389051089,-0.439659463057376));
#47876=CARTESIAN_POINT('Ctrl Pts',(-1.41227996488216,51.4332870266657,-0.383793630474047));
#47877=CARTESIAN_POINT('Ctrl Pts',(-1.42743363924789,51.4364293162326,-0.32803129102451));
#47878=CARTESIAN_POINT('Ctrl Pts',(-1.43930175669946,51.4395716057996,-0.271292351947302));
#47879=CARTESIAN_POINT('Ctrl Pts',(-1.44777284090111,51.4427138953665,-0.213976753758748));
#47880=CARTESIAN_POINT('Ctrl Pts',(-1.45622563919931,51.4458494019052,-0.156784878516293));
#47881=CARTESIAN_POINT('Ctrl Pts',(-1.46129592542497,51.4489849084439,-0.0990192666897063));
#47882=CARTESIAN_POINT('Ctrl Pts',(-1.46292302961044,51.4521204149826,-0.0410908680292959));
#47883=CARTESIAN_POINT('Ctrl Pts',(-1.46330782198311,51.4528619280408,-0.0273914342964181));
#47884=CARTESIAN_POINT('Ctrl Pts',(-1.46350027245807,51.4536034410989,-0.013682939758203));
#47885=CARTESIAN_POINT('Ctrl Pts',(-1.46349999971048,51.4543449541571,2.91106062376064E-5));
#47886=CARTESIAN_POINT('Ctrl Pts',(-1.46349999166114,51.5256550458102,-0.000156230081695943));
#47887=CARTESIAN_POINT('Ctrl Pts',(-1.46349371788756,51.5224767923979,-0.0589263944364653));
#47888=CARTESIAN_POINT('Ctrl Pts',(-1.45994303350198,51.5192985389856,-0.117616406012124));
#47889=CARTESIAN_POINT('Ctrl Pts',(-1.45290268375024,51.5161202855733,-0.175801142064967));
#47890=CARTESIAN_POINT('Ctrl Pts',(-1.44586580081156,51.5129435971984,-0.233957226756734));
#47891=CARTESIAN_POINT('Ctrl Pts',(-1.43534283904945,51.5097669088235,-0.291608116930657));
#47892=CARTESIAN_POINT('Ctrl Pts',(-1.42143930082676,51.5065902204486,-0.34834259582361));
#47893=CARTESIAN_POINT('Ctrl Pts',(-1.40748602039149,51.5034021669444,-0.405280051718877));
#47894=CARTESIAN_POINT('Ctrl Pts',(-1.39012810097255,51.5002141134403,-0.461294120731727));
#47895=CARTESIAN_POINT('Ctrl Pts',(-1.36952103538481,51.4970260599362,-0.515988743712996));
#47896=CARTESIAN_POINT('Ctrl Pts',(-1.34903054608504,51.4938560415784,-0.570373953590711));
#47897=CARTESIAN_POINT('Ctrl Pts',(-1.32532785188886,51.4906860232206,-0.623454270906817));
#47898=CARTESIAN_POINT('Ctrl Pts',(-1.29861052459124,51.4875160048627,-0.674865138691329));
#47899=CARTESIAN_POINT('Ctrl Pts',(-1.2732559103757,51.4845076727933,-0.723653803240071));
#47900=CARTESIAN_POINT('Ctrl Pts',(-1.24509392124162,51.4814993407239,-0.771115667504255));
#47901=CARTESIAN_POINT('Ctrl Pts',(-1.21428722872449,51.4784910086545,-0.81690805857));
#47902=CARTESIAN_POINT('Ctrl Pts',(-1.18353588709454,51.4754880817044,-0.862618173699423));
#47903=CARTESIAN_POINT('Ctrl Pts',(-1.15014956433339,51.4724851547543,-0.906664332828394));
#47904=CARTESIAN_POINT('Ctrl Pts',(-1.1143365921763,51.4694822278042,-0.94872873327254));
#47905=CARTESIAN_POINT('Ctrl Pts',(-1.07855948036464,51.4664823077533,-0.990751013673588));
#47906=CARTESIAN_POINT('Ctrl Pts',(-1.04036087335701,51.4634823877025,-1.03079506539789));
#47907=CARTESIAN_POINT('Ctrl Pts',(-0.999991038550154,51.4604824676516,
-1.06857389675183));
#47908=CARTESIAN_POINT('Ctrl Pts',(-0.959645625317653,51.4574843623906,
-1.10632987394886));
#47909=CARTESIAN_POINT('Ctrl Pts',(-0.917131972827282,51.4544862571297,
-1.14182298600698));
#47910=CARTESIAN_POINT('Ctrl Pts',(-0.872737479869535,51.4514881518688,
-1.17480276694898));
#47911=CARTESIAN_POINT('Ctrl Pts',(-0.828352247206295,51.4484906719858,
-1.20777566860339));
#47912=CARTESIAN_POINT('Ctrl Pts',(-0.782087377374449,51.4454931921028,
-1.23823596487485));
#47913=CARTESIAN_POINT('Ctrl Pts',(-0.734261807223034,51.4424957122199,
-1.26597466343271));
#47914=CARTESIAN_POINT('Ctrl Pts',(-0.686392004729485,51.4394954600635,
-1.29373901662681));
#47915=CARTESIAN_POINT('Ctrl Pts',(-0.636959076313892,51.4364952079071,
-1.31877647675021));
#47916=CARTESIAN_POINT('Ctrl Pts',(-0.586308007005538,51.4334949557508,
-1.34092325318088));
#47917=CARTESIAN_POINT('Ctrl Pts',(-0.535634199676096,51.4304933567364,
-1.36307997163008));
#47918=CARTESIAN_POINT('Ctrl Pts',(-0.483741658060411,51.4274917577221,
-1.38234323505235));
#47919=CARTESIAN_POINT('Ctrl Pts',(-0.430993759607402,51.4244901587077,
-1.39859809422846));
#47920=CARTESIAN_POINT('Ctrl Pts',(-0.378144397297677,51.4214827859314,
-1.41488422063512));
#47921=CARTESIAN_POINT('Ctrl Pts',(-0.324436905909344,51.418475413155,-1.42815025441349));
#47922=CARTESIAN_POINT('Ctrl Pts',(-0.270247069561249,51.4154680403787,
-1.43833194061509));
#47923=CARTESIAN_POINT('Ctrl Pts',(-0.226240311703689,51.4130257978019,
-1.44660033611968));
#47924=CARTESIAN_POINT('Ctrl Pts',(-0.181915769092783,51.4105835552252,
-1.4528356313487));
#47925=CARTESIAN_POINT('Ctrl Pts',(-0.13747606741555,51.4081413126484,-1.45702868224615));
#47926=CARTESIAN_POINT('Ctrl Pts',(-0.0827356464006351,51.4051329804179,
-1.46219364426886));
#47927=CARTESIAN_POINT('Ctrl Pts',(-0.0275870130885459,51.4021246481873,
-1.46428043842858));
#47928=CARTESIAN_POINT('Ctrl Pts',(0.0275937155764213,51.3991163159568,
-1.46323984256194));
#47929=CARTESIAN_POINT('Ctrl Pts',(0.0826753000794172,51.3961133888484,
-1.46220111635174));
#47930=CARTESIAN_POINT('Ctrl Pts',(0.137788341101494,51.39311046174,-1.45804616047742));
#47931=CARTESIAN_POINT('Ctrl Pts',(0.192552846829943,51.3901075346315,-1.45077760224567));
#47932=CARTESIAN_POINT('Ctrl Pts',(0.247262515580034,51.3871076144242,-1.44351632219099));
#47933=CARTESIAN_POINT('Ctrl Pts',(0.301623818697801,51.3841076942168,-1.43314768461669));
#47934=CARTESIAN_POINT('Ctrl Pts',(0.355259900639993,51.3811077740094,-1.41972625988155));
#47935=CARTESIAN_POINT('Ctrl Pts',(0.408863535607975,51.3781096685941,-1.40631295439388));
#47936=CARTESIAN_POINT('Ctrl Pts',(0.461742306892657,51.3751115631787,-1.38985064998074));
#47937=CARTESIAN_POINT('Ctrl Pts',(0.513529902161674,51.3721134577634,-1.37044492395201));
#47938=CARTESIAN_POINT('Ctrl Pts',(0.56530669496165,51.3691159777283,-1.35104324579909));
#47939=CARTESIAN_POINT('Ctrl Pts',(0.615992268706816,51.3661184976932,-1.3286995505863));
#47940=CARTESIAN_POINT('Ctrl Pts',(0.665238045064347,51.3631210176582,-1.30356840764072));
#47941=CARTESIAN_POINT('Ctrl Pts',(0.714529367186659,51.3601207653545,-1.27841402174499));
#47942=CARTESIAN_POINT('Ctrl Pts',(0.762377759096981,51.3571205130508,-1.25046727795835));
#47943=CARTESIAN_POINT('Ctrl Pts',(0.808458486331006,51.3541202607471,-1.21992914789318));
#47944=CARTESIAN_POINT('Ctrl Pts',(0.854559899853462,51.3511186615878,-1.18937730883068));
#47945=CARTESIAN_POINT('Ctrl Pts',(0.898891642411422,51.3481170624285,-1.15623208169307));
#47946=CARTESIAN_POINT('Ctrl Pts',(0.941160033911184,51.3451154632693,-1.12073638317327));
#47947=CARTESIAN_POINT('Ctrl Pts',(0.983509731200422,51.3421080903538,-1.08517240654568));
#47948=CARTESIAN_POINT('Ctrl Pts',(1.02378776191686,51.3391007174382,-1.04724928930633));
#47949=CARTESIAN_POINT('Ctrl Pts',(1.06173630385517,51.3360933445227,-1.00724786973017));
#47950=CARTESIAN_POINT('Ctrl Pts',(1.09255373201681,51.3336511031599,-0.974763331163288));
#47951=CARTESIAN_POINT('Ctrl Pts',(1.12183555220237,51.3312088617972,-0.940908981056737));
#47952=CARTESIAN_POINT('Ctrl Pts',(1.14946416948652,51.3287666204344,-0.905850083107941));
#47953=CARTESIAN_POINT('Ctrl Pts',(1.18349687119876,51.3257582877714,-0.862664823274632));
#47954=CARTESIAN_POINT('Ctrl Pts',(1.21516506212638,51.3227499551084,-0.817466891271791));
#47955=CARTESIAN_POINT('Ctrl Pts',(1.24422336847353,51.3197416224454,-0.770545559551409));
#47956=CARTESIAN_POINT('Ctrl Pts',(1.27322946531484,51.3167386949,-0.723708532109218));
#47957=CARTESIAN_POINT('Ctrl Pts',(1.29963470676274,51.3137357673545,-0.675154695503419));
#47958=CARTESIAN_POINT('Ctrl Pts',(1.32323517542342,51.3107328398091,-0.625204702895095));
#47959=CARTESIAN_POINT('Ctrl Pts',(1.34681201240667,51.3077329191622,-0.575304726332241));
#47960=CARTESIAN_POINT('Ctrl Pts',(1.36758941486602,51.3047329985153,-0.524011838713086));
#47961=CARTESIAN_POINT('Ctrl Pts',(1.38540880358005,51.3017330778685,-0.471672234674566));
#47962=CARTESIAN_POINT('Ctrl Pts',(1.40321741252416,51.2987349720119,-0.419364293276008));
#47963=CARTESIAN_POINT('Ctrl Pts',(1.41807138410431,51.2957368661553,-0.366011390038988));
#47964=CARTESIAN_POINT('Ctrl Pts',(1.42986070871547,51.2927387602988,-0.311978530786503));
#47965=CARTESIAN_POINT('Ctrl Pts',(1.4416475741738,51.2897412798216,-0.2579569423288));
#47966=CARTESIAN_POINT('Ctrl Pts',(1.45037094927048,51.2867437993444,-0.203256195905757));
#47967=CARTESIAN_POINT('Ctrl Pts',(1.45597160189233,51.2837463188673,-0.148252974617942));
#47968=CARTESIAN_POINT('Ctrl Pts',(1.46157743436492,51.2807460661236,-0.0931988827450114));
#47969=CARTESIAN_POINT('Ctrl Pts',(1.46405472000038,51.27774581338,-0.0378422843772192));
#47970=CARTESIAN_POINT('Ctrl Pts',(1.46339614283138,51.2747455606364,0.0174349977411516));
#47971=CARTESIAN_POINT('Ctrl Pts',(1.46273727001795,51.2717439610376,0.0727370945985477));
#47972=CARTESIAN_POINT('Ctrl Pts',(1.45893976440794,51.2687423614389,0.127959275605072));
#47973=CARTESIAN_POINT('Ctrl Pts',(1.45204839301903,51.2657407618402,0.182723053638169));
#47974=CARTESIAN_POINT('Ctrl Pts',(1.44514376568009,51.2627333884916,0.237592172954387));
#47975=CARTESIAN_POINT('Ctrl Pts',(1.43513347892081,51.2597260151431,0.292000606083937));
#47976=CARTESIAN_POINT('Ctrl Pts',(1.42211360828021,51.2567186417945,0.345579419445437));
#47977=CARTESIAN_POINT('Ctrl Pts',(1.41154038796423,51.2542764039364,0.389089882304661));
#47978=CARTESIAN_POINT('Ctrl Pts',(1.39898342387764,51.2518341660783,0.432053342607236));
#47979=CARTESIAN_POINT('Ctrl Pts',(1.38451776352351,51.2493919282201,0.474281364263733));
#47980=CARTESIAN_POINT('Ctrl Pts',(1.36669906659865,51.2463835971003,0.526297539205796));
#47981=CARTESIAN_POINT('Ctrl Pts',(1.34590692717192,51.2433752659804,0.577419073981439));
#47982=CARTESIAN_POINT('Ctrl Pts',(1.32225125853123,51.2403669348606,0.627282918078111));
#47983=CARTESIAN_POINT('Ctrl Pts',(1.2986380924074,51.2373640088572,0.677057171011373));
#47984=CARTESIAN_POINT('Ctrl Pts',(1.2721718315674,51.2343610828538,0.725577743591005));
#47985=CARTESIAN_POINT('Ctrl Pts',(1.24301123978448,51.2313581568505,0.772499390141801));
#47986=CARTESIAN_POINT('Ctrl Pts',(1.21387984715273,51.2283582377439,0.819374053001011));
#47987=CARTESIAN_POINT('Ctrl Pts',(1.18205974533812,51.2253583186373,0.86465251425162));
#47988=CARTESIAN_POINT('Ctrl Pts',(1.14775574875542,51.2223583995308,0.908013761569116));
#47989=CARTESIAN_POINT('Ctrl Pts',(1.11347250420261,51.2193602952101,0.951348777718505));
#47990=CARTESIAN_POINT('Ctrl Pts',(1.07670867038285,51.2163621908895,0.99276846463294));
#47991=CARTESIAN_POINT('Ctrl Pts',(1.03771121117154,51.2133640865689,1.03198240886601));
#47992=CARTESIAN_POINT('Ctrl Pts',(0.998721886411359,51.2103666076207,1.0711881734915));
#47993=CARTESIAN_POINT('Ctrl Pts',(0.957500234080089,51.2073691286724,1.10818873418212));
#47994=CARTESIAN_POINT('Ctrl Pts',(0.914330572024747,51.2043716497241,1.1427300009455));
#47995=CARTESIAN_POINT('Ctrl Pts',(0.871120983484007,51.2013713984864,1.17730321401833));
#47996=CARTESIAN_POINT('Ctrl Pts',(0.825960199223298,51.1983711472487,1.20941225728892));
#47997=CARTESIAN_POINT('Ctrl Pts',(0.779165016506029,51.195370896011,1.23884386710076));
#47998=CARTESIAN_POINT('Ctrl Pts',(0.732348826610749,51.1923692979078,1.26828868927829));
#47999=CARTESIAN_POINT('Ctrl Pts',(0.683897239400804,51.1893676998047,1.29505342568246));
#48000=CARTESIAN_POINT('Ctrl Pts',(0.634152502047362,51.1863661017016,1.3189703765237));
#48001=CARTESIAN_POINT('Ctrl Pts',(0.584312077181155,51.1833587298127,1.3429333333077));
#48002=CARTESIAN_POINT('Ctrl Pts',(0.533174022850266,51.1803513579239,1.36403735821174));
#48003=CARTESIAN_POINT('Ctrl Pts',(0.481100392408416,51.177343986035,1.38216303756991));
#48004=CARTESIAN_POINT('Ctrl Pts',(0.438812032622073,51.1749017360253,1.39688268057475));
#48005=CARTESIAN_POINT('Ctrl Pts',(0.395907127134563,51.1724594860157,1.40963905926866));
#48006=CARTESIAN_POINT('Ctrl Pts',(0.352584691729241,51.170017236006,1.4203930037698));
#48007=CARTESIAN_POINT('Ctrl Pts',(0.299220662541903,51.1670089032662,1.4336395768876));
#48008=CARTESIAN_POINT('Ctrl Pts',(0.244995284244615,51.1640005705265,1.44390289048352));
#48009=CARTESIAN_POINT('Ctrl Pts',(0.190273174697797,51.1609922377867,1.45107834695113));
#48010=CARTESIAN_POINT('Ctrl Pts',(0.135649385547883,51.1579893101833,1.45824091112102));
#48011=CARTESIAN_POINT('Ctrl Pts',(0.0805311562522271,51.15498638258,1.46232655952096));
#48012=CARTESIAN_POINT('Ctrl Pts',(0.0252946456500175,51.1519834549766,
1.46328139156535));
#48013=CARTESIAN_POINT('Ctrl Pts',(-0.0298865551868294,51.1489835342834,
1.4642352675114));
#48014=CARTESIAN_POINT('Ctrl Pts',(-0.0851852765983605,51.1459836135901,
1.4620645277722));
#48015=CARTESIAN_POINT('Ctrl Pts',(-0.140220738055422,51.1429836928969,
1.45676710376751));
#48016=CARTESIAN_POINT('Ctrl Pts',(-0.195222905814022,51.1399855870054,
1.4514728844391));
#48017=CARTESIAN_POINT('Ctrl Pts',(-0.249961603889136,51.136987481114,1.44305578014748));
#48018=CARTESIAN_POINT('Ctrl Pts',(-0.304058893854024,51.1339893752225,
1.43156572991542));
#48019=CARTESIAN_POINT('Ctrl Pts',(-0.358144899378313,51.1309918947219,
1.42007807645387));
#48020=CARTESIAN_POINT('Ctrl Pts',(-0.411589245401469,51.1279944142213,
1.40551885961797));
#48021=CARTESIAN_POINT('Ctrl Pts',(-0.464024246046617,51.1249969337206,
1.38798910265206));
#48022=CARTESIAN_POINT('Ctrl Pts',(-0.516507741708372,51.1219966809712,
1.37044313312117));
#48023=CARTESIAN_POINT('Ctrl Pts',(-0.567979524064569,51.1189964282218,
1.34992130211764));
#48024=CARTESIAN_POINT('Ctrl Pts',(-0.618088586797045,51.1159961754724,
1.3265740646007));
#48025=CARTESIAN_POINT('Ctrl Pts',(-0.668220144020035,51.1129945758776,
1.30321634626085));
#48026=CARTESIAN_POINT('Ctrl Pts',(-0.716987295275605,51.1099929762829,
1.27703094357738));
#48027=CARTESIAN_POINT('Ctrl Pts',(-0.764063506869514,51.1069913766881,
1.24821440765209));
#48028=CARTESIAN_POINT('Ctrl Pts',(-0.811230272020899,51.1039840033594,
1.21934244161138));
#48029=CARTESIAN_POINT('Ctrl Pts',(-0.85669916342403,51.1009766300307,1.18782953311385));
#48030=CARTESIAN_POINT('Ctrl Pts',(-0.900173468365905,51.097969256702,1.15391506483367));
#48031=CARTESIAN_POINT('Ctrl Pts',(-0.935478225094219,51.0955270190653,
1.12637369174438));
#48032=CARTESIAN_POINT('Ctrl Pts',(-0.969468115397339,51.0930847814285,
1.09724941745909));
#48033=CARTESIAN_POINT('Ctrl Pts',(-1.00200228000408,51.0906425437917,1.06668818352255));
#48034=CARTESIAN_POINT('Ctrl Pts',(-1.04146882826977,51.0876799138692,1.02961495822861));
#48035=CARTESIAN_POINT('Ctrl Pts',(-1.07897116203487,51.0847172839467,0.990257845560917));
#48036=CARTESIAN_POINT('Ctrl Pts',(-1.11422790346054,51.0817546540242,0.948856379622301));
#48037=CARTESIAN_POINT('Ctrl Pts',(-1.1494344329215,51.0787962434216,0.907513876845407));
#48038=CARTESIAN_POINT('Ctrl Pts',(-1.18240134639486,51.075837832819,0.864133192028604));
#48039=CARTESIAN_POINT('Ctrl Pts',(-1.21288281519522,51.0728794222163,0.818991774442275));
#48040=CARTESIAN_POINT('Ctrl Pts',(-1.24333380476329,51.0699239698072,0.773895494961382));
#48041=CARTESIAN_POINT('Ctrl Pts',(-1.27130396502406,51.0669685173981,0.727042417870797));
#48042=CARTESIAN_POINT('Ctrl Pts',(-1.29658827545769,51.064013064989,0.67874228831395));
#48043=CARTESIAN_POINT('Ctrl Pts',(-1.3218580231019,51.0610593148067,0.630469977772274));
#48044=CARTESIAN_POINT('Ctrl Pts',(-1.34444473358649,51.0581055646244,0.580752749081789));
#48045=CARTESIAN_POINT('Ctrl Pts',(-1.36418854276114,51.0551518144421,0.529926287137395));
#48046=CARTESIAN_POINT('Ctrl Pts',(-1.38393833124246,51.0521971697324,0.479084432671739));
#48047=CARTESIAN_POINT('Ctrl Pts',(-1.4008432919116,51.0492425250227,0.427133179797992));
#48048=CARTESIAN_POINT('Ctrl Pts',(-1.41479191016864,51.0462878803131,0.37442769785551));
#48049=CARTESIAN_POINT('Ctrl Pts',(-1.42874312731249,51.0433326850982,0.321712395902229));
#48050=CARTESIAN_POINT('Ctrl Pts',(-1.43973678590469,51.0403774898832,0.268243118242051));
#48051=CARTESIAN_POINT('Ctrl Pts',(-1.44771220919992,51.0374222946683,0.214386588511222));
#48052=CARTESIAN_POINT('Ctrl Pts',(-1.45569720330142,51.0344635531086,0.160465428930283));
#48053=CARTESIAN_POINT('Ctrl Pts',(-1.46065668292314,51.0315048115489,0.106156633517691));
#48054=CARTESIAN_POINT('Ctrl Pts',(-1.46258187645247,51.0285460699892,0.0518315027059542));
#48055=CARTESIAN_POINT('Ctrl Pts',(-1.46320892016773,51.0275823952875,0.0341375766995819));
#48056=CARTESIAN_POINT('Ctrl Pts',(-1.46351448948394,51.0266187205858,0.0164419086505343));
#48057=CARTESIAN_POINT('Ctrl Pts',(-1.46349947235337,51.0256550458841,-0.0012427475236237));
#48058=CARTESIAN_POINT('Origin',(0.,55.715,0.));
#48059=CARTESIAN_POINT('',(-1.46391036891612,50.4543447982886,0.00080102880736226));
#48060=CARTESIAN_POINT('',(-1.46349969347884,50.5256550458075,0.00094719973096371));
#48061=CARTESIAN_POINT('',(-1.4635,55.715,-1.79227059055215E-16));
#48062=CARTESIAN_POINT('Ctrl Pts',(-1.46349977934093,50.4543449541571,0.000803659790552031));
#48063=CARTESIAN_POINT('Ctrl Pts',(-1.46347455770472,50.4568544564617,0.0467333671772216));
#48064=CARTESIAN_POINT('Ctrl Pts',(-1.46128737451521,50.4593639587663,0.0926024254620283));
#48065=CARTESIAN_POINT('Ctrl Pts',(-1.45695412945267,50.4618734610709,0.138263931199737));
#48066=CARTESIAN_POINT('Ctrl Pts',(-1.45175846780538,50.4648824127202,0.193013138940129));
#48067=CARTESIAN_POINT('Ctrl Pts',(-1.44346142373346,50.4678913643695,0.247585534401134));
#48068=CARTESIAN_POINT('Ctrl Pts',(-1.43208529592634,50.4709003160188,0.301602312974477));
#48069=CARTESIAN_POINT('Ctrl Pts',(-1.42072960126165,50.4739038631633,0.355522069736163));
#48070=CARTESIAN_POINT('Ctrl Pts',(-1.4063059058018,50.4769074103078,0.408887677011401));
#48071=CARTESIAN_POINT('Ctrl Pts',(-1.38888816280316,50.4799109574523,0.461326263316182));
#48072=CARTESIAN_POINT('Ctrl Pts',(-1.37148785750537,50.4829114976081,0.513712350948678));
#48073=CARTESIAN_POINT('Ctrl Pts',(-1.35109960799791,50.4859120377639,0.565172756848002));
#48074=CARTESIAN_POINT('Ctrl Pts',(-1.32784779785606,50.4889125779197,0.615347443099267));
#48075=CARTESIAN_POINT('Ctrl Pts',(-1.30461006026922,50.4919113020764,0.665491762423053));
#48076=CARTESIAN_POINT('Ctrl Pts',(-1.27851241873977,50.494910026233,0.714351425691465));
#48077=CARTESIAN_POINT('Ctrl Pts',(-1.24972737818508,50.4979087503897,0.761586324860581));
#48078=CARTESIAN_POINT('Ctrl Pts',(-1.22094836304363,50.5009068468401,0.808811336609645));
#48079=CARTESIAN_POINT('Ctrl Pts',(-1.18948334077739,50.5039049432904,0.854411808402353));
#48080=CARTESIAN_POINT('Ctrl Pts',(-1.15554961053038,50.5069030397407,0.898074243925904));
#48081=CARTESIAN_POINT('Ctrl Pts',(-1.12158460055204,50.5099038998027,0.941776926992022));
#48082=CARTESIAN_POINT('Ctrl Pts',(-1.08514666077922,50.5129047598647,0.983537585944588));
#48083=CARTESIAN_POINT('Ctrl Pts',(-1.04649419523657,50.5159056199267,1.02307485030967));
#48084=CARTESIAN_POINT('Ctrl Pts',(-1.00782443070391,50.5189078230297,1.06262980965829));
#48085=CARTESIAN_POINT('Ctrl Pts',(-0.966938555633143,50.5219100261327,
1.09995903351445));
#48086=CARTESIAN_POINT('Ctrl Pts',(-0.92413035215595,50.5249122292358,1.13481951967003));
#48087=CARTESIAN_POINT('Ctrl Pts',(-0.881240022136062,50.5279201919956,
1.16974688485748));
#48088=CARTESIAN_POINT('Ctrl Pts',(-0.836420425108368,50.5309281547555,
1.20219573920285));
#48089=CARTESIAN_POINT('Ctrl Pts',(-0.789995868594206,50.5339361175154,
1.23196541250316));
#48090=CARTESIAN_POINT('Ctrl Pts',(-0.752378157990058,50.5363734627719,
1.25608770981902));
#48091=CARTESIAN_POINT('Ctrl Pts',(-0.713707314398565,50.5388108080285,
1.27845169181399));
#48092=CARTESIAN_POINT('Ctrl Pts',(-0.674166557648519,50.5412481532851,
1.29897332634213));
#48093=CARTESIAN_POINT('Ctrl Pts',(-0.625353734488048,50.5442570411458,
1.3243071590636));
#48094=CARTESIAN_POINT('Ctrl Pts',(-0.575007291188768,50.5472659290066,
1.34693952004985));
#48095=CARTESIAN_POINT('Ctrl Pts',(-0.523457587380063,50.5502748168673,
1.36668372501257));
#48096=CARTESIAN_POINT('Ctrl Pts',(-0.472000164466407,50.5532783184146,
1.38639258519596));
#48097=CARTESIAN_POINT('Ctrl Pts',(-0.419344245117153,50.5562818199619,
1.40322336171202));
#48098=CARTESIAN_POINT('Ctrl Pts',(-0.365843215951807,50.5592853215091,
1.41703598801937));
#48099=CARTESIAN_POINT('Ctrl Pts',(-0.312395551090045,50.5622858272305,
1.43083483699954));
#48100=CARTESIAN_POINT('Ctrl Pts',(-0.258104955463595,50.5652863329519,
1.44162136748116));
#48101=CARTESIAN_POINT('Ctrl Pts',(-0.203341378283216,50.5682868386733,
1.4493048450474));
#48102=CARTESIAN_POINT('Ctrl Pts',(-0.148610740738315,50.5712855396264,
1.45698370109396));
#48103=CARTESIAN_POINT('Ctrl Pts',(-0.0934082079420693,50.5742842405795,
1.46156313010151));
#48104=CARTESIAN_POINT('Ctrl Pts',(-0.0381130768592489,50.5772829415327,
1.46300363751165));
#48105=CARTESIAN_POINT('Ctrl Pts',(0.0171706881136775,50.5802810260922,
1.4644438488204));
#48106=CARTESIAN_POINT('Ctrl Pts',(0.0725464854021787,50.5832791106517,
1.46274640593892));
#48107=CARTESIAN_POINT('Ctrl Pts',(0.127633088951927,50.5862771952113,1.45792388162228));
#48108=CARTESIAN_POINT('Ctrl Pts',(0.182770798663487,50.5892780612201,1.45309688324677));
#48109=CARTESIAN_POINT('Ctrl Pts',(0.237618250753981,50.592278927229,1.44513905673968));
#48110=CARTESIAN_POINT('Ctrl Pts',(0.291798921557676,50.5952797932378,1.43411493241573));
#48111=CARTESIAN_POINT('Ctrl Pts',(0.34600401928565,50.5982820121632,1.42308583795305));
#48112=CARTESIAN_POINT('Ctrl Pts',(0.399541224279997,50.6012842310886,1.40898782469742));
#48113=CARTESIAN_POINT('Ctrl Pts',(0.452047068900792,50.604286450014,1.39193595308771));
#48114=CARTESIAN_POINT('Ctrl Pts',(0.50465392915194,50.6072944448876,1.37485127550046));
#48115=CARTESIAN_POINT('Ctrl Pts',(0.556224970783227,50.6103024397611,1.35480157811856));
#48116=CARTESIAN_POINT('Ctrl Pts',(0.60641574197187,50.6133104346347,1.33195052381412));
#48117=CARTESIAN_POINT('Ctrl Pts',(0.647086859661879,50.6157479049229,1.31343361528798));
#48118=CARTESIAN_POINT('Ctrl Pts',(0.686851949166193,50.6181853752111,1.29307821329013));
#48119=CARTESIAN_POINT('Ctrl Pts',(0.725541042079325,50.6206228454993,1.27099270110353));
#48120=CARTESIAN_POINT('Ctrl Pts',(0.773283808923846,50.6236307106855,1.24373893577659));
#48121=CARTESIAN_POINT('Ctrl Pts',(0.819590948990178,50.6266385758717,1.21373305763258));
#48122=CARTESIAN_POINT('Ctrl Pts',(0.864126513841084,50.6296464410579,1.18115097175461));
#48123=CARTESIAN_POINT('Ctrl Pts',(0.90858189309974,50.6326488906296,1.1486275494158));
#48124=CARTESIAN_POINT('Ctrl Pts',(0.951271603300684,50.6356513402013,1.11353743357303));
#48125=CARTESIAN_POINT('Ctrl Pts',(0.991886332749048,50.638653789773,1.07610118153715));
#48126=CARTESIAN_POINT('Ctrl Pts',(1.03246030521508,50.6416532263791,1.03870249687359));
#48127=CARTESIAN_POINT('Ctrl Pts',(1.07096303435184,50.6446526629852,0.998962696223431));
#48128=CARTESIAN_POINT('Ctrl Pts',(1.10711763680155,50.6476520995912,0.957143034390863));
#48129=CARTESIAN_POINT('Ctrl Pts',(1.14325030143847,50.6506497162055,0.915348747803772));
#48130=CARTESIAN_POINT('Ctrl Pts',(1.17703731783404,50.6536473328198,0.871477500586006));
#48131=CARTESIAN_POINT('Ctrl Pts',(1.20823975515763,50.6566449494341,0.825826219041649));
#48132=CARTESIAN_POINT('Ctrl Pts',(1.23943563764072,50.6596419363252,0.780184527673417));
#48133=CARTESIAN_POINT('Ctrl Pts',(1.26804772071684,50.6626389232163,0.732763980984989));
#48134=CARTESIAN_POINT('Ctrl Pts',(1.29387975260718,50.6656359101074,0.683891391810999));
#48135=CARTESIAN_POINT('Ctrl Pts',(1.31973565535281,50.6686356664531,0.63497364047133));
#48136=CARTESIAN_POINT('Ctrl Pts',(1.34280612603492,50.6716354227989,0.584601634386629));
#48137=CARTESIAN_POINT('Ctrl Pts',(1.36294110295681,50.6746351791446,0.533126438915635));
#48138=CARTESIAN_POINT('Ctrl Pts',(1.38308510443959,50.6776362799907,0.481628172097829));
#48139=CARTESIAN_POINT('Ctrl Pts',(1.40029082451669,50.6806373808368,0.429026233991788));
#48140=CARTESIAN_POINT('Ctrl Pts',(1.41445772863024,50.6836384816829,0.375688147162209));
#48141=CARTESIAN_POINT('Ctrl Pts',(1.4286518996745,50.6866453587246,0.322247400929708));
#48142=CARTESIAN_POINT('Ctrl Pts',(1.43979546294892,50.6896522357662,0.268068194976788));
#48143=CARTESIAN_POINT('Ctrl Pts',(1.44783902743882,50.6926591128079,0.213528453900192));
#48144=CARTESIAN_POINT('Ctrl Pts',(1.45438259331181,50.6951052544431,0.169159519097881));
#48145=CARTESIAN_POINT('Ctrl Pts',(1.45887553632095,50.6975513960783,0.124552255462931));
#48146=CARTESIAN_POINT('Ctrl Pts',(1.46131672144697,50.6999975377135,0.0799105100689137));
#48147=CARTESIAN_POINT('Ctrl Pts',(1.4643190718301,50.7030059839789,0.0250067832033121));
#48148=CARTESIAN_POINT('Ctrl Pts',(1.46422929886921,50.7060144302444,-0.0301834016102755));
#48149=CARTESIAN_POINT('Ctrl Pts',(1.46101306892529,50.7090228765098,-0.0852822515503883));
#48150=CARTESIAN_POINT('Ctrl Pts',(1.45780261640381,50.7120259186016,-0.140282125566023));
#48151=CARTESIAN_POINT('Ctrl Pts',(1.45147688225879,50.7150289606935,-0.195190466727399));
#48152=CARTESIAN_POINT('Ctrl Pts',(1.44205349495465,50.7180320027853,-0.249627658101197));
#48153=CARTESIAN_POINT('Ctrl Pts',(1.43263954159519,50.7210320384706,-0.304010351295545));
#48154=CARTESIAN_POINT('Ctrl Pts',(1.42013416757001,50.724032074156,-0.357922310554726));
#48155=CARTESIAN_POINT('Ctrl Pts',(1.4046067800889,50.7270321098413,-0.410989103661276));
#48156=CARTESIAN_POINT('Ctrl Pts',(1.38908878400445,50.7300303310214,-0.464023800492489));
#48157=CARTESIAN_POINT('Ctrl Pts',(1.37055254518906,50.7330285522015,-0.516213837771159));
#48158=CARTESIAN_POINT('Ctrl Pts',(1.34911802190673,50.7360267733817,-0.567197331593228));
#48159=CARTESIAN_POINT('Ctrl Pts',(1.32768796894709,50.7390243692614,-0.618170192444067));
#48160=CARTESIAN_POINT('Ctrl Pts',(1.30336103655147,50.7420219651411,-0.667936522245004));
#48161=CARTESIAN_POINT('Ctrl Pts',(1.27630543707061,50.7450195610209,-0.716154090474954));
#48162=CARTESIAN_POINT('Ctrl Pts',(1.24922482309904,50.748019928354,-0.764416238678561));
#48163=CARTESIAN_POINT('Ctrl Pts',(1.21941076060294,50.7510202956872,-0.811126301991854));
#48164=CARTESIAN_POINT('Ctrl Pts',(1.1870768873791,50.7540206630203,-0.855967705845461));
#48165=CARTESIAN_POINT('Ctrl Pts',(1.1547285024467,50.7570223769431,-0.900829234890378));
#48166=CARTESIAN_POINT('Ctrl Pts',(1.11985838603432,50.7600240908658,-0.943820021077674));
#48167=CARTESIAN_POINT('Ctrl Pts',(1.08272086373127,50.7630258047885,-0.98465617412425));
#48168=CARTESIAN_POINT('Ctrl Pts',(1.04551193157149,50.7660332905546,-1.02557084893689));
#48169=CARTESIAN_POINT('Ctrl Pts',(1.00602726164272,50.7690407763207,-1.06432224203247));
#48170=CARTESIAN_POINT('Ctrl Pts',(0.964557657605331,50.7720482620868,-1.1006637884272));
#48171=CARTESIAN_POINT('Ctrl Pts',(0.930894761090083,50.7744895847004,-1.13016399089807));
#48172=CARTESIAN_POINT('Ctrl Pts',(0.895924684517973,50.776930907314,-1.15807693695955));
#48173=CARTESIAN_POINT('Ctrl Pts',(0.859816996954149,50.7793722299277,-1.18429176377646));
#48174=CARTESIAN_POINT('Ctrl Pts',(0.815322256397643,50.7823806202079,-1.21659574103587));
#48175=CARTESIAN_POINT('Ctrl Pts',(0.768909613199299,50.7853890104881,-1.24645753244705));
#48176=CARTESIAN_POINT('Ctrl Pts',(0.720877813142877,50.7883974007683,-1.27364336786965));
#48177=CARTESIAN_POINT('Ctrl Pts',(0.672932275764584,50.7914003881321,-1.3007803789099));
#48178=CARTESIAN_POINT('Ctrl Pts',(0.623373808483145,50.7944033754959,-1.32525071247325));
#48179=CARTESIAN_POINT('Ctrl Pts',(0.572530876490621,50.7974063628596,-1.34686326160634));
#48180=CARTESIAN_POINT('Ctrl Pts',(0.521738831608448,50.8004063446267,-1.36845417941077));
#48181=CARTESIAN_POINT('Ctrl Pts',(0.469665352757049,50.8034063263938,-1.38719277258399));
#48182=CARTESIAN_POINT('Ctrl Pts',(0.416662636605764,50.8064063081608,-1.40293424552141));
#48183=CARTESIAN_POINT('Ctrl Pts',(0.363691962520342,50.80940447633,-1.41866620216704));
#48184=CARTESIAN_POINT('Ctrl Pts',(0.309793670411534,50.8124026444992,-1.43140447926226));
#48185=CARTESIAN_POINT('Ctrl Pts',(0.255336836086297,50.8154008126684,-1.44105355561042));
#48186=CARTESIAN_POINT('Ctrl Pts',(0.20089134105466,50.8183983565429,-1.45070062277625));
#48187=CARTESIAN_POINT('Ctrl Pts',(0.14588805518517,50.8213959004175,-1.45725967419364));
#48188=CARTESIAN_POINT('Ctrl Pts',(0.0907057182243708,50.824393444292,-1.46068638751835));
#48189=CARTESIAN_POINT('Ctrl Pts',(0.0354723242544452,50.8273937616197,
-1.46411627138173));
#48190=CARTESIAN_POINT('Ctrl Pts',(-0.0199399228048711,50.8303940789474,
-1.46440799352035));
#48191=CARTESIAN_POINT('Ctrl Pts',(-0.0751491963403478,50.8333943962751,
-1.46156931012162));
#48192=CARTESIAN_POINT('Ctrl Pts',(-0.130383267536119,50.8363960612178,
-1.45872935170691));
#48193=CARTESIAN_POINT('Ctrl Pts',(-0.185413656714807,50.8393977261606,
-1.45275624195342));
#48194=CARTESIAN_POINT('Ctrl Pts',(-0.239863925455392,50.8423993911034,
-1.4437096478396));
#48195=CARTESIAN_POINT('Ctrl Pts',(-0.294418938010553,50.8454068302295,
-1.43464565115278));
#48196=CARTESIAN_POINT('Ctrl Pts',(-0.348391083256365,50.8484142693556,
-1.4224964746592));
#48197=CARTESIAN_POINT('Ctrl Pts',(-0.401415493228798,50.8514217084818,
-1.40737267693951));
#48198=CARTESIAN_POINT('Ctrl Pts',(-0.444465977484462,50.8538634463685,
-1.3950936753258));
#48199=CARTESIAN_POINT('Ctrl Pts',(-0.486891887937306,50.8563051842551,
-1.38085487095812));
#48200=CARTESIAN_POINT('Ctrl Pts',(-0.528508014289907,50.8587469221418,
-1.36473863022607));
#48201=CARTESIAN_POINT('Ctrl Pts',(-0.579779925614663,50.8617551927181,
-1.34488309492947));
#48202=CARTESIAN_POINT('Ctrl Pts',(-0.630040734325549,50.8647634632944,
-1.32209182286124));
#48203=CARTESIAN_POINT('Ctrl Pts',(-0.678932014993594,50.8677717338707,
-1.29648893902599));
#48204=CARTESIAN_POINT('Ctrl Pts',(-0.727735426344551,50.8707745978657,
-1.27093206969245));
#48205=CARTESIAN_POINT('Ctrl Pts',(-0.775173729354133,50.8737774618607,
-1.24257385940806));
#48206=CARTESIAN_POINT('Ctrl Pts',(-0.820908213835026,50.8767803258557,
-1.21158654435339));
#48207=CARTESIAN_POINT('Ctrl Pts',(-0.866596889467469,50.8797801821041,
-1.18063026699894));
#48208=CARTESIAN_POINT('Ctrl Pts',(-0.910584691336295,50.8827800383525,
-1.14705039625305));
#48209=CARTESIAN_POINT('Ctrl Pts',(-0.952558937867875,50.8857798946009,
-1.11106422851608));
#48210=CARTESIAN_POINT('Ctrl Pts',(-0.994507781445313,50.8887779353263,
-1.07509983972797));
#48211=CARTESIAN_POINT('Ctrl Pts',(-1.03444508413165,50.8917759760517,-1.03673238372182));
#48212=CARTESIAN_POINT('Ctrl Pts',(-1.07209040014527,50.8947740167771,-0.996220068015273));
#48213=CARTESIAN_POINT('Ctrl Pts',(-1.10972785573044,50.8977714315047,-0.955716211373298));
#48214=CARTESIAN_POINT('Ctrl Pts',(-1.14507391504389,50.9007688462322,-0.91306877149604));
#48215=CARTESIAN_POINT('Ctrl Pts',(-1.17788589952651,50.9037662609598,-0.868571849472821));
#48216=CARTESIAN_POINT('Ctrl Pts',(-1.21072822657144,50.9067664475174,-0.824033779355371));
#48217=CARTESIAN_POINT('Ctrl Pts',(-1.24103148194678,50.909766634075,-0.77764323641579));
#48218=CARTESIAN_POINT('Ctrl Pts',(-1.26859506181715,50.9127668206326,-0.729725166849231));
#48219=CARTESIAN_POINT('Ctrl Pts',(-1.29617101243885,50.9157683536975,-0.68178559127635));
#48220=CARTESIAN_POINT('Ctrl Pts',(-1.3210045986092,50.9187698867624,-0.632317595956556));
#48221=CARTESIAN_POINT('Ctrl Pts',(-1.34294174817087,50.9217714198273,-0.581669761135786));
#48222=CARTESIAN_POINT('Ctrl Pts',(-1.36492109801395,50.9247787269122,-0.530924495567432));
#48223=CARTESIAN_POINT('Ctrl Pts',(-1.38399269674653,50.9277860339971,-0.478995353963776));
#48224=CARTESIAN_POINT('Ctrl Pts',(-1.40005150163908,50.930793341082,-0.426248803820208));
#48225=CARTESIAN_POINT('Ctrl Pts',(-1.4130956534759,50.93323609884,-0.383404145482011));
#48226=CARTESIAN_POINT('Ctrl Pts',(-1.42415292766332,50.935678856598,-0.340020587674471));
#48227=CARTESIAN_POINT('Ctrl Pts',(-1.43319201428126,50.938121614356,-0.296298667226898));
#48228=CARTESIAN_POINT('Ctrl Pts',(-1.44896036148208,50.9423829135429,-0.220027418698728));
#48229=CARTESIAN_POINT('Ctrl Pts',(-1.45864431504176,50.9466442127298,-0.142458225153691));
#48230=CARTESIAN_POINT('Ctrl Pts',(-1.46208250160868,50.9509055119168,-0.0643972708248851));
#48231=CARTESIAN_POINT('Ctrl Pts',(-1.46300752811584,50.9520519926635,-0.0433953703978048));
#48232=CARTESIAN_POINT('Ctrl Pts',(-1.46348069847868,50.9531984734103,-0.0223580200854855));
#48233=CARTESIAN_POINT('Ctrl Pts',(-1.46349942146304,50.9543449541571,-0.00130129832626773));
#48234=CARTESIAN_POINT('Ctrl Pts',(-1.46349947235273,51.0256550458429,-0.00124274828025101));
#48235=CARTESIAN_POINT('Ctrl Pts',(-1.46342876260759,51.0211174845061,-0.0845127687219559));
#48236=CARTESIAN_POINT('Ctrl Pts',(-1.45624797044794,51.0165799231693,-0.16748978317585));
#48237=CARTESIAN_POINT('Ctrl Pts',(-1.44212460500004,51.0120423618326,-0.249216519623962));
#48238=CARTESIAN_POINT('Ctrl Pts',(-1.44132103890206,51.0117841917476,-0.25386646194476));
#48239=CARTESIAN_POINT('Ctrl Pts',(-1.4404950095162,51.0115260216626,-0.258512364733264));
#48240=CARTESIAN_POINT('Ctrl Pts',(-1.439646551692,51.0112678515777,-0.263154054122935));
#48241=CARTESIAN_POINT('Ctrl Pts',(-1.42975990758924,51.0082595279165,-0.317241281233215));
#48242=CARTESIAN_POINT('Ctrl Pts',(-1.4167998670086,51.0052512042553,-0.37088592099037));
#48243=CARTESIAN_POINT('Ctrl Pts',(-1.4008211405863,51.0022428805941,-0.42371261733219));
#48244=CARTESIAN_POINT('Ctrl Pts',(-1.38487112339493,50.9992399620357,-0.476444399111713));
#48245=CARTESIAN_POINT('Ctrl Pts',(-1.36591333510058,50.9962370434773,-0.528360651755262));
#48246=CARTESIAN_POINT('Ctrl Pts',(-1.34405344116184,50.9932341249189,-0.579096362707456));
#48247=CARTESIAN_POINT('Ctrl Pts',(-1.32221543597803,50.9902342132437,-0.629781270963807));
#48248=CARTESIAN_POINT('Ctrl Pts',(-1.29748128946475,50.9872343015685,-0.67928749577689));
#48249=CARTESIAN_POINT('Ctrl Pts',(-1.27000580900265,50.9842343898933,-0.727267141495828));
#48250=CARTESIAN_POINT('Ctrl Pts',(-1.24254694949504,50.9812362929779,-0.775217762517333));
#48251=CARTESIAN_POINT('Ctrl Pts',(-1.21235030497094,50.9782381960624,-0.821643176682928));
#48252=CARTESIAN_POINT('Ctrl Pts',(-1.17961691336254,50.9752400991469,-0.866219480102497));
#48253=CARTESIAN_POINT('Ctrl Pts',(-1.14689034918043,50.9722426275649,-0.910786485939042));
#48254=CARTESIAN_POINT('Ctrl Pts',(-1.11162840134636,50.9692451559829,-0.953504720769974));
#48255=CARTESIAN_POINT('Ctrl Pts',(-1.07407444729542,50.9662476844009,-0.994080646460353));
#48256=CARTESIAN_POINT('Ctrl Pts',(-1.03648575900856,50.9632474404109,-1.03469410145521));
#48257=CARTESIAN_POINT('Ctrl Pts',(-0.996601188783579,50.9602471964208,
-1.07316089917715));
#48258=CARTESIAN_POINT('Ctrl Pts',(-0.954702302684935,50.9572469524307,
-1.10922304485982));
#48259=CARTESIAN_POINT('Ctrl Pts',(-0.912784606643465,50.9542453615214,
-1.145301380159));
#48260=CARTESIAN_POINT('Ctrl Pts',(-0.868851212548808,50.951243770612,-1.17897258901797));
#48261=CARTESIAN_POINT('Ctrl Pts',(-0.823215628063835,50.9482421797026,
-1.21001995012953));
#48262=CARTESIAN_POINT('Ctrl Pts',(-0.777492257362881,50.9452348148274,
-1.2411270350373));
#48263=CARTESIAN_POINT('Ctrl Pts',(-0.73006060926692,50.9422274499522,-1.26959991548894));
#48264=CARTESIAN_POINT('Ctrl Pts',(-0.681260956796725,50.9392200850769,
-1.29526667476023));
#48265=CARTESIAN_POINT('Ctrl Pts',(-0.64163031188215,50.9367777765057,-1.31611088514491));
#48266=CARTESIAN_POINT('Ctrl Pts',(-0.601098024097525,50.9343354679346,
-1.33510523574745));
#48267=CARTESIAN_POINT('Ctrl Pts',(-0.559855087663332,50.9318931593634,
-1.35218139715701));
#48268=CARTESIAN_POINT('Ctrl Pts',(-0.509053676778809,50.9288848206766,
-1.37321513449726));
#48269=CARTESIAN_POINT('Ctrl Pts',(-0.456956925343664,50.9258764819898,
-1.39142683058595));
#48270=CARTESIAN_POINT('Ctrl Pts',(-0.403909847570677,50.922868143303,-1.40665883747106));
#48271=CARTESIAN_POINT('Ctrl Pts',(-0.350958082281005,50.9198652098571,
-1.42186347620578));
#48272=CARTESIAN_POINT('Ctrl Pts',(-0.297059883158429,50.9168622764111,
-1.43409890505244));
#48273=CARTESIAN_POINT('Ctrl Pts',(-0.242579214891096,50.9138593429652,
-1.44325589363176));
#48274=CARTESIAN_POINT('Ctrl Pts',(-0.188153100665166,50.9108594164969,
-1.45240371289012));
#48275=CARTESIAN_POINT('Ctrl Pts',(-0.133146191533447,50.9078594900287,
-1.45847911066817));
#48276=CARTESIAN_POINT('Ctrl Pts',(-0.0779347290763724,50.9048595635605,
-1.46142342529597));
#48277=CARTESIAN_POINT('Ctrl Pts',(-0.0227566681379459,50.9018614519708,
-1.46436595868893));
#48278=CARTESIAN_POINT('Ctrl Pts',(0.032625173825781,50.8988633403812,-1.46418113498521));
#48279=CARTESIAN_POINT('Ctrl Pts',(0.087829633035611,50.8958652287915,-1.46086214461216));
#48280=CARTESIAN_POINT('Ctrl Pts',(0.143022575293431,50.8928677426787,-1.45754384665876));
#48281=CARTESIAN_POINT('Ctrl Pts',(0.198037680648211,50.8898702565658,-1.45109271203716));
#48282=CARTESIAN_POINT('Ctrl Pts',(0.252496328463599,50.8868727704529,-1.44155397197344));
#48283=CARTESIAN_POINT('Ctrl Pts',(0.307005339582375,50.8838725122679,-1.43200641049239));
#48284=CARTESIAN_POINT('Ctrl Pts',(0.360956342816656,50.8808722540828,-1.41936562965639));
#48285=CARTESIAN_POINT('Ctrl Pts',(0.413979861946499,50.8778719958978,-1.40372822294871));
#48286=CARTESIAN_POINT('Ctrl Pts',(0.467027182283583,50.8748703909563,-1.38808379691898));
#48287=CARTESIAN_POINT('Ctrl Pts',(0.519145689647756,50.8718687860147,-1.36944024194494));
#48288=CARTESIAN_POINT('Ctrl Pts',(0.569983254564791,50.8688671810732,-1.34794337400194));
#48289=CARTESIAN_POINT('Ctrl Pts',(0.62091860441094,50.8658598026112,-1.32640515731001));
#48290=CARTESIAN_POINT('Ctrl Pts',(0.670567613442345,50.8628524241491,-1.30200289686416));
#48291=CARTESIAN_POINT('Ctrl Pts',(0.718601273244825,50.859845045687,-1.2749291980698));
#48292=CARTESIAN_POINT('Ctrl Pts',(0.757607823904044,50.8574028528411,-1.25294354034776));
#48293=CARTESIAN_POINT('Ctrl Pts',(0.795549513672652,50.8549606599952,-1.22919714062126));
#48294=CARTESIAN_POINT('Ctrl Pts',(0.832265358514905,50.8525184671493,-1.20381336718615));
#48295=CARTESIAN_POINT('Ctrl Pts',(0.877492811124125,50.8495101158046,-1.17254503017764));
#48296=CARTESIAN_POINT('Ctrl Pts',(0.921052116665841,50.84650176446,-1.13865766713958));
#48297=CARTESIAN_POINT('Ctrl Pts',(0.962623684385345,50.8434934131153,-1.10235561061773));
#48298=CARTESIAN_POINT('Ctrl Pts',(1.00412056290765,50.8404904666991,-1.06611877587141));
#48299=CARTESIAN_POINT('Ctrl Pts',(1.04363639538093,50.8374875202828,-1.02747620167254));
#48300=CARTESIAN_POINT('Ctrl Pts',(1.08088198703955,50.8344845738666,-0.986674404296291));
#48301=CARTESIAN_POINT('Ctrl Pts',(1.11809028534983,50.8314846342471,-0.945913461033893));
#48302=CARTESIAN_POINT('Ctrl Pts',(1.15303249076323,50.8284846946277,-0.90299796571356));
#48303=CARTESIAN_POINT('Ctrl Pts',(1.18545523163875,50.8254847550083,-0.858212178764858));
#48304=CARTESIAN_POINT('Ctrl Pts',(1.21785835936004,50.8224866301114,-0.813453483620316));
#48305=CARTESIAN_POINT('Ctrl Pts',(1.2477447336037,50.8194885052145,-0.766827166632986));
#48306=CARTESIAN_POINT('Ctrl Pts',(1.27490187343789,50.8164903803176,-0.718649749950941));
#48307=CARTESIAN_POINT('Ctrl Pts',(1.30205334886781,50.813492880766,-0.670482382057797));
#48308=CARTESIAN_POINT('Ctrl Pts',(1.32647646063315,50.8104953812145,-0.62076501730944));
#48309=CARTESIAN_POINT('Ctrl Pts',(1.34800382649144,50.807497881663,-0.569840270395509));
#48310=CARTESIAN_POINT('Ctrl Pts',(1.36955110141698,50.804497609946,-0.518868426952557));
#48311=CARTESIAN_POINT('Ctrl Pts',(1.38819707305615,50.801497338229,-0.466687458465234));
#48312=CARTESIAN_POINT('Ctrl Pts',(1.40382246858234,50.798497066512,-0.413660158467528));
#48313=CARTESIAN_POINT('Ctrl Pts',(1.41945487838904,50.7954954479652,-0.360609054377571));
#48314=CARTESIAN_POINT('Ctrl Pts',(1.43206388827817,50.7924938294185,-0.306711377327725));
#48315=CARTESIAN_POINT('Ctrl Pts',(1.44158098649968,50.7894922108717,-0.252342048344332));
#48316=CARTESIAN_POINT('Ctrl Pts',(1.45111639039091,50.7864848188595,-0.197868142634271));
#48317=CARTESIAN_POINT('Ctrl Pts',(1.45754793952193,50.7834774268474,-0.142921299290412));
#48318=CARTESIAN_POINT('Ctrl Pts',(1.46085897144578,50.7804700348352,-0.0878823961120183));
#48319=CARTESIAN_POINT('Ctrl Pts',(1.46354762220071,50.7780279482018,-0.0431892635827417));
#48320=CARTESIAN_POINT('Ctrl Pts',(1.46417964027166,50.7755858615684,0.00156438341266757));
#48321=CARTESIAN_POINT('Ctrl Pts',(1.46277133862608,50.773143774935,0.0461764105801477));
#48322=CARTESIAN_POINT('Ctrl Pts',(1.46103653263137,50.7701355085281,0.101131407195287));
#48323=CARTESIAN_POINT('Ctrl Pts',(1.45619680074368,50.7671272421212,0.156105727972618));
#48324=CARTESIAN_POINT('Ctrl Pts',(1.44825042847767,50.7641189757143,0.210720066472687));
#48325=CARTESIAN_POINT('Ctrl Pts',(1.44031833374732,50.7611161143689,0.265236277407166));
#48326=CARTESIAN_POINT('Ctrl Pts',(1.42929075075258,50.7581132530235,0.319393270513705));
#48327=CARTESIAN_POINT('Ctrl Pts',(1.41521789141983,50.7551103916782,0.372814390555439));
#48328=CARTESIAN_POINT('Ctrl Pts',(1.40115912348797,50.7521105371505,0.426182019092628));
#48329=CARTESIAN_POINT('Ctrl Pts',(1.38406125330985,50.7491106826229,0.478814725233145));
#48330=CARTESIAN_POINT('Ctrl Pts',(1.36402563367689,50.7461108280952,0.530345472944148));
#48331=CARTESIAN_POINT('Ctrl Pts',(1.34400213348727,50.7431127881642,0.58184504997071));
#48332=CARTESIAN_POINT('Ctrl Pts',(1.32104459699756,50.7401147482331,0.632243497694544));
#48333=CARTESIAN_POINT('Ctrl Pts',(1.29530366105929,50.7371167083021,0.681190630915026));
#48334=CARTESIAN_POINT('Ctrl Pts',(1.26956809194593,50.7341192934437,0.730127558962903));
#48335=CARTESIAN_POINT('Ctrl Pts',(1.24105052168738,50.7311218785853,0.77761330546091));
#48336=CARTESIAN_POINT('Ctrl Pts',(1.20994797104225,50.7281244637269,0.823321418020167));
#48337=CARTESIAN_POINT('Ctrl Pts',(1.17881664375618,50.7251242756062,0.869071820549729));
#48338=CARTESIAN_POINT('Ctrl Pts',(1.145095855535,50.7221240874855,0.913040864647186));
#48339=CARTESIAN_POINT('Ctrl Pts',(1.10902567610588,50.7191238993648,0.954931568091603));
#48340=CARTESIAN_POINT('Ctrl Pts',(1.07293929855558,50.7161223639425,0.996841083493761));
#48341=CARTESIAN_POINT('Ctrl Pts',(1.03450179452092,50.7131208285202,1.0366700163551));
#48342=CARTESIAN_POINT('Ctrl Pts',(0.993990956745005,50.7101192930979,1.07415745024142));
#48343=CARTESIAN_POINT('Ctrl Pts',(0.953402171440967,50.707111982375,1.11171701427778));
#48344=CARTESIAN_POINT('Ctrl Pts',(0.91073249143381,50.704104671652,1.1469257408952));
#48345=CARTESIAN_POINT('Ctrl Pts',(0.866292838772237,50.7010973609291,1.1795630409147));
#48346=CARTESIAN_POINT('Ctrl Pts',(0.830195677755104,50.6986546015264,1.206073461303));
#48347=CARTESIAN_POINT('Ctrl Pts',(0.792931412066315,50.6962118421236,1.23088802403368));
#48348=CARTESIAN_POINT('Ctrl Pts',(0.754678858566674,50.6937690827209,1.2539107107097));
#48349=CARTESIAN_POINT('Ctrl Pts',(0.707568640778594,50.6907606841451,1.28226447233202));
#48350=CARTESIAN_POINT('Ctrl Pts',(0.658757845635839,50.6877522855694,1.30802005425201));
#48351=CARTESIAN_POINT('Ctrl Pts',(0.608564225018396,50.6847438869936,1.33097026038442));
#48352=CARTESIAN_POINT('Ctrl Pts',(0.558460800518663,50.6817408944011,1.3538792258279));
#48353=CARTESIAN_POINT('Ctrl Pts',(0.5069799585649,50.6787379018086,1.37399260114022));
#48354=CARTESIAN_POINT('Ctrl Pts',(0.454465389109663,50.6757349092161,1.39114825238053));
#48355=CARTESIAN_POINT('Ctrl Pts',(0.40200341254252,50.6727349240947,1.40828672238418));
#48356=CARTESIAN_POINT('Ctrl Pts',(0.348510259315172,50.6697349389734,1.42247317234456));
#48357=CARTESIAN_POINT('Ctrl Pts',(0.294349278233204,50.666734953852,1.43359364968027));
#48358=CARTESIAN_POINT('Ctrl Pts',(0.240221073141164,50.6637367841978,1.44470739736215));
#48359=CARTESIAN_POINT('Ctrl Pts',(0.185426358146335,50.6607386145436,1.45275874348916));
#48360=CARTESIAN_POINT('Ctrl Pts',(0.130341059055819,50.6577404448894,1.45768427937061));
#48361=CARTESIAN_POINT('Ctrl Pts',(0.0752672644074769,50.6547429013963,
1.46260878656485));
#48362=CARTESIAN_POINT('Ctrl Pts',(0.0199035326198596,50.6517453579032,
1.46440873264817));
#48363=CARTESIAN_POINT('Ctrl Pts',(-0.0353689875074307,50.64874781441,1.46307254937091));
#48364=CARTESIAN_POINT('Ctrl Pts',(-0.0906925948275551,50.6457475003524,
1.4617351310884));
#48365=CARTESIAN_POINT('Ctrl Pts',(-0.14592429216002,50.6427471862947,1.45725580448248));
#48366=CARTESIAN_POINT('Ctrl Pts',(-0.200684336464834,50.6397468722371,
1.44967515226608));
#48367=CARTESIAN_POINT('Ctrl Pts',(-0.255468947440346,50.6367452121665,
1.44209109918707));
#48368=CARTESIAN_POINT('Ctrl Pts',(-0.309780963692739,50.633743552096,1.43140304914164));
#48369=CARTESIAN_POINT('Ctrl Pts',(-0.363250476642326,50.6307418920254,
1.41770283953271));
#48370=CARTESIAN_POINT('Ctrl Pts',(-0.416822800948029,50.6277344603529,
1.4039762871155));
#48371=CARTESIAN_POINT('Ctrl Pts',(-0.469548880081667,50.6247270286804,
1.38722616461457));
#48372=CARTESIAN_POINT('Ctrl Pts',(-0.521074711920323,50.621719597008,1.36759401673053));
#48373=CARTESIAN_POINT('Ctrl Pts',(-0.562908564353531,50.6192778615076,
1.35165466459936));
#48374=CARTESIAN_POINT('Ctrl Pts',(-0.603951475876654,50.6168361260072,
1.33381652431876));
#48375=CARTESIAN_POINT('Ctrl Pts',(-0.644026008875002,50.6143943905067,
1.31417759450256));
#48376=CARTESIAN_POINT('Ctrl Pts',(-0.69340155100613,50.6113859458649,1.28998061118176));
#48377=CARTESIAN_POINT('Ctrl Pts',(-0.741516750164403,50.608377501223,1.26294552122677));
#48378=CARTESIAN_POINT('Ctrl Pts',(-0.788025175090753,50.6053690565812,
1.2332268945426));
#48379=CARTESIAN_POINT('Ctrl Pts',(-0.83445006565773,50.6023660154441,1.20356164585276));
#48380=CARTESIAN_POINT('Ctrl Pts',(-0.879273466979466,50.599362974307,1.17122270757813));
#48381=CARTESIAN_POINT('Ctrl Pts',(-0.922172736471481,50.5963599331699,
1.13641088260748));
#48382=CARTESIAN_POINT('Ctrl Pts',(-0.965029064456583,50.5933598980306,
1.10163390373654));
#48383=CARTESIAN_POINT('Ctrl Pts',(-1.00596466714275,50.5903598628914,1.06438927286245));
#48384=CARTESIAN_POINT('Ctrl Pts',(-1.04468671702488,50.5873598277522,1.02492044241091));
#48385=CARTESIAN_POINT('Ctrl Pts',(-1.08338535198395,50.5843616067109,0.985475478454843));
#48386=CARTESIAN_POINT('Ctrl Pts',(-1.11987271736089,50.5813633856696,0.943809357216002));
#48387=CARTESIAN_POINT('Ctrl Pts',(-1.15389162651969,50.5783651646283,0.900203512683514));
#48388=CARTESIAN_POINT('Ctrl Pts',(-1.18790344540187,50.5753675684812,0.856606756552381));
#48389=CARTESIAN_POINT('Ctrl Pts',(-1.21944750449566,50.572369972334,0.811071496575774));
#48390=CARTESIAN_POINT('Ctrl Pts',(-1.2483073359531,50.5693723761869,0.763911673562907));
#48391=CARTESIAN_POINT('Ctrl Pts',(-1.27719385605675,50.566372007959,0.71670823865876));
#48392=CARTESIAN_POINT('Ctrl Pts',(-1.30339091205091,50.5633716397311,0.667877690987514));
#48393=CARTESIAN_POINT('Ctrl Pts',(-1.3267266110265,50.5603712715032,0.617761078082899));
#48394=CARTESIAN_POINT('Ctrl Pts',(-1.35007278596125,50.5573695563375,0.567621966619721));
#48395=CARTESIAN_POINT('Ctrl Pts',(-1.3705548470833,50.5543678411718,0.516196131186225));
#48396=CARTESIAN_POINT('Ctrl Pts',(-1.38804929530734,50.5513661260061,0.46384415895512));
#48397=CARTESIAN_POINT('Ctrl Pts',(-1.4055773859604,50.5483586384383,0.411391512070742));
#48398=CARTESIAN_POINT('Ctrl Pts',(-1.42010624628452,50.5453511508705,0.358009681929733));
#48399=CARTESIAN_POINT('Ctrl Pts',(-1.4315627645176,50.5423436633027,0.304072855162587));
#48400=CARTESIAN_POINT('Ctrl Pts',(-1.4408625689543,50.5399023416327,0.26028975015062));
#48401=CARTESIAN_POINT('Ctrl Pts',(-1.44813886589741,50.5374610199626,0.216141274358366));
#48402=CARTESIAN_POINT('Ctrl Pts',(-1.45337774111322,50.5350196982925,0.171829542386152));
#48403=CARTESIAN_POINT('Ctrl Pts',(-1.4600763320478,50.5318981474759,0.115171165567171));
#48404=CARTESIAN_POINT('Ctrl Pts',(-1.46346269457913,50.5287765966594,0.0581134335821789));
#48405=CARTESIAN_POINT('Ctrl Pts',(-1.46349969347842,50.5256550458429,0.000947200379455493));
#48406=CARTESIAN_POINT('Origin',(0.,55.715,0.));
#48407=CARTESIAN_POINT('',(-1.28852825769066,50.065,0.693921594369763));
#48408=CARTESIAN_POINT('Ctrl Pts',(-1.46349969347884,50.5256550458075,0.000947199730964576));
#48409=CARTESIAN_POINT('Ctrl Pts',(-1.46353482282959,50.5226912244331,-0.0533304698703549));
#48410=CARTESIAN_POINT('Ctrl Pts',(-1.4605461735546,50.5197274030587,-0.107727267896845));
#48411=CARTESIAN_POINT('Ctrl Pts',(-1.45452035935177,50.5167635816843,-0.161872709964321));
#48412=CARTESIAN_POINT('Ctrl Pts',(-1.44850182572144,50.5138033412893,-0.215952731857356));
#48413=CARTESIAN_POINT('Ctrl Pts',(-1.43945344630703,50.5108431008942,-0.26978146135027));
#48414=CARTESIAN_POINT('Ctrl Pts',(-1.42741383466044,50.5078828604992,-0.322989155576445));
#48415=CARTESIAN_POINT('Ctrl Pts',(-1.41538368556614,50.5049249467099,-0.376155031129087));
#48416=CARTESIAN_POINT('Ctrl Pts',(-1.40036707739651,50.5019670329206,-0.428700307980801));
#48417=CARTESIAN_POINT('Ctrl Pts',(-1.38245400783414,50.4990091191313,-0.480263642412506));
#48418=CARTESIAN_POINT('Ctrl Pts',(-1.36454745537885,50.4960522814859,-0.531808217146408));
#48419=CARTESIAN_POINT('Ctrl Pts',(-1.34374670863753,50.4930954438406,-0.582371043352419));
#48420=CARTESIAN_POINT('Ctrl Pts',(-1.32019138050361,50.4901386061952,-0.631606656744505));
#48421=CARTESIAN_POINT('Ctrl Pts',(-1.29661750760403,50.4871794406747,-0.680881032615597));
#48422=CARTESIAN_POINT('Ctrl Pts',(-1.27028495177837,50.4842202751543,-0.728825613385225));
#48423=CARTESIAN_POINT('Ctrl Pts',(-1.24138048400446,50.4812611096338,-0.775117245281548));
#48424=CARTESIAN_POINT('Ctrl Pts',(-1.21246571703341,50.4783008897079,-0.821425371743577));
#48425=CARTESIAN_POINT('Ctrl Pts',(-1.18097752545467,50.475340669782,-0.866078928781415));
#48426=CARTESIAN_POINT('Ctrl Pts',(-1.14714552231686,50.4723804498561,-0.90878457327816));
#48427=CARTESIAN_POINT('Ctrl Pts',(-1.11324870640735,50.4694145589666,-0.951572029992054));
#48428=CARTESIAN_POINT('Ctrl Pts',(-1.07699947243047,50.466448668077,-0.992403711374319));
#48429=CARTESIAN_POINT('Ctrl Pts',(-1.03866628085557,50.4634827771875,-1.03102114770438));
#48430=CARTESIAN_POINT('Ctrl Pts',(-1.00489938555175,50.4608701868178,-1.0650384281834));
#48431=CARTESIAN_POINT('Ctrl Pts',(-0.969516194411335,50.4582575964481,
-1.0973379734395));
#48432=CARTESIAN_POINT('Ctrl Pts',(-0.9327204188105,50.4556450060784,-1.12776986585649));
#48433=CARTESIAN_POINT('Ctrl Pts',(-0.890342237235046,50.4526360511844,
-1.16281867897358));
#48434=CARTESIAN_POINT('Ctrl Pts',(-0.845895538558477,50.4496270962905,
-1.19555012316991));
#48435=CARTESIAN_POINT('Ctrl Pts',(-0.799663853035677,50.4466181413966,
-1.22571202659847));
#48436=CARTESIAN_POINT('Ctrl Pts',(-0.753515307750692,50.4436145976232,
-1.25581968870325));
#48437=CARTESIAN_POINT('Ctrl Pts',(-0.705588584788405,50.4406110538499,
-1.28336669349437));
#48438=CARTESIAN_POINT('Ctrl Pts',(-0.656199557617031,50.4376075100765,
-1.30814157895207));
#48439=CARTESIAN_POINT('Ctrl Pts',(-0.606860041905433,50.4346069772926,
-1.33289162810877));
#48440=CARTESIAN_POINT('Ctrl Pts',(-0.556061595897285,50.4316064445086,
-1.35487482683292));
#48441=CARTESIAN_POINT('Ctrl Pts',(-0.504146693165044,50.4286059117247,
-1.37392443815908));
#48442=CARTESIAN_POINT('Ctrl Pts',(-0.452263277975644,50.4256071988306,
-1.3929624954724));
#48443=CARTESIAN_POINT('Ctrl Pts',(-0.399265243405242,50.4226084859365,
-1.40907031007267));
#48444=CARTESIAN_POINT('Ctrl Pts',(-0.34551501355974,50.4196097730424,-1.42212925762914));
#48445=CARTESIAN_POINT('Ctrl Pts',(-0.291776102853237,50.4166116916404,
-1.43518545513147));
#48446=CARTESIAN_POINT('Ctrl Pts',(-0.237285824802378,50.4136136102384,
-1.44519393568715));
#48447=CARTESIAN_POINT('Ctrl Pts',(-0.182419477212928,50.4106155288365,
-1.45208656227284));
#48448=CARTESIAN_POINT('Ctrl Pts',(-0.127502655314952,50.4076146893489,
-1.45898552973188));
#48449=CARTESIAN_POINT('Ctrl Pts',(-0.0722095982901611,50.4046138498613,
-1.46276284973304));
#48450=CARTESIAN_POINT('Ctrl Pts',(-0.0169219692928829,50.4016130103737,
-1.46340216514643));
#48451=CARTESIAN_POINT('Ctrl Pts',(0.0383903471274892,50.39861083093,-1.46404176603146));
#48452=CARTESIAN_POINT('Ctrl Pts',(0.0936967015878671,50.3956086514863,
-1.46154059277131));
#48453=CARTESIAN_POINT('Ctrl Pts',(0.14861752829933,50.3926064720427,-1.45593443543389));
#48454=CARTESIAN_POINT('Ctrl Pts',(0.203643636320153,50.3895985375257,-1.45031753128837));
#48455=CARTESIAN_POINT('Ctrl Pts',(0.258282216616718,50.3865906030087,-1.44158383518267));
#48456=CARTESIAN_POINT('Ctrl Pts',(0.312162035999495,50.3835826684918,-1.42982065773322));
#48457=CARTESIAN_POINT('Ctrl Pts',(0.355823042622614,50.3811452169492,-1.42028847714291));
#48458=CARTESIAN_POINT('Ctrl Pts',(0.398985900736044,50.3787077654067,-1.4087680018665));
#48459=CARTESIAN_POINT('Ctrl Pts',(0.441461587347743,50.3762703138641,-1.39532932202273));
#48460=CARTESIAN_POINT('Ctrl Pts',(0.493895812924911,50.3732613952518,-1.37873990754595));
#48461=CARTESIAN_POINT('Ctrl Pts',(0.54550501015341,50.3702524766396,-1.35915555163723));
#48462=CARTESIAN_POINT('Ctrl Pts',(0.595923536242905,50.3672435580273,-1.33667774311977));
#48463=CARTESIAN_POINT('Ctrl Pts',(0.646251713829184,50.3642400313079,-1.31424021416842));
#48464=CARTESIAN_POINT('Ctrl Pts',(0.695392975524007,50.3612365045885,-1.28891973535305));
#48465=CARTESIAN_POINT('Ctrl Pts',(0.742998345345203,50.3582329778691,-1.26086704644633));
#48466=CARTESIAN_POINT('Ctrl Pts',(0.79055617710117,50.3552324504301,-1.23284237056755));
#48467=CARTESIAN_POINT('Ctrl Pts',(0.836580701893695,50.352231922991,-1.20209115605839));
#48468=CARTESIAN_POINT('Ctrl Pts',(0.880746100695365,50.349231395552,-1.16881074435082));
#48469=CARTESIAN_POINT('Ctrl Pts',(0.924884882543173,50.3462326764267,-1.13555038959296));
#48470=CARTESIAN_POINT('Ctrl Pts',(0.967166337697631,50.3432339573015,-1.09976417610463));
#48471=CARTESIAN_POINT('Ctrl Pts',(1.00729425568835,50.3402352381762,-1.06169229650462));
#48472=CARTESIAN_POINT('Ctrl Pts',(1.04741387657129,50.3372371390855,-1.0236282888926));
#48473=CARTESIAN_POINT('Ctrl Pts',(1.08538046116735,50.3342390399948,-0.98327991721212));
#48474=CARTESIAN_POINT('Ctrl Pts',(1.12093323976277,50.3312409409041,-0.94092556666026));
#48475=CARTESIAN_POINT('Ctrl Pts',(1.15651893115896,50.3282400663387,-0.898532006787599));
#48476=CARTESIAN_POINT('Ctrl Pts',(1.1896860111028,50.3252391917733,-0.854129163371487));
#48477=CARTESIAN_POINT('Ctrl Pts',(1.22021376407475,50.3222383172079,-0.808028848471721));
#48478=CARTESIAN_POINT('Ctrl Pts',(1.25075524670215,50.319236093019,-0.761907800259525));
#48479=CARTESIAN_POINT('Ctrl Pts',(1.2786547690964,50.31623386883,-0.714088216096344));
#48480=CARTESIAN_POINT('Ctrl Pts',(1.30373656897248,50.3132316446411,-0.664908421306164));
#48481=CARTESIAN_POINT('Ctrl Pts',(1.32886657582411,50.3102236502064,-0.615634103428473));
#48482=CARTESIAN_POINT('Ctrl Pts',(1.3511678269104,50.3072156557718,-0.564994837064679));
#48483=CARTESIAN_POINT('Ctrl Pts',(1.37051236645305,50.3042076613371,-0.513349883996552));
#48484=CARTESIAN_POINT('Ctrl Pts',(1.38618704537271,50.3017703147747,-0.471502516403251));
#48485=CARTESIAN_POINT('Ctrl Pts',(1.39992134641109,50.2993329682124,-0.428995320515241));
#48486=CARTESIAN_POINT('Ctrl Pts',(1.41167166311979,50.29689562165,-0.386025084087313));
#48487=CARTESIAN_POINT('Ctrl Pts',(1.42615711337943,50.2938909313705,-0.333052620633494));
#48488=CARTESIAN_POINT('Ctrl Pts',(1.43768809010586,50.2908862410911,-0.279149052216486));
#48489=CARTESIAN_POINT('Ctrl Pts',(1.44615115225048,50.2878815508116,-0.224675532367466));
#48490=CARTESIAN_POINT('Ctrl Pts',(1.45459897720145,50.2848822702819,-0.170300088552479));
#48491=CARTESIAN_POINT('Ctrl Pts',(1.45998976692289,50.2818829897521,-0.115357249028846));
#48492=CARTESIAN_POINT('Ctrl Pts',(1.46226047055535,50.2788837092223,-0.0602209784978448));
#48493=CARTESIAN_POINT('Ctrl Pts',(1.46452889744066,50.2758874359557,-0.00513999098368401));
#48494=CARTESIAN_POINT('Ctrl Pts',(1.46368341260466,50.2728911626891,0.0501335162761768));
#48495=CARTESIAN_POINT('Ctrl Pts',(1.45971266687425,50.2698948894225,0.105219675759159));
#48496=CARTESIAN_POINT('Ctrl Pts',(1.4557443184603,50.2669004251399,0.160272577268573));
#48497=CARTESIAN_POINT('Ctrl Pts',(1.44865448637538,50.2639059608572,0.215137827320708));
#48498=CARTESIAN_POINT('Ctrl Pts',(1.43848388312004,50.2609114965745,0.269437131820935));
#48499=CARTESIAN_POINT('Ctrl Pts',(1.42831536328326,50.2579176456992,0.323725313266256));
#48500=CARTESIAN_POINT('Ctrl Pts',(1.41506742283674,50.2549237948238,0.377447258392881));
#48501=CARTESIAN_POINT('Ctrl Pts',(1.39883209022656,50.2519299439485,0.430233696207518));
#48502=CARTESIAN_POINT('Ctrl Pts',(1.38258146762911,50.2489332735471,0.483069846829524));
#48503=CARTESIAN_POINT('Ctrl Pts',(1.36333798780192,50.2459366031458,0.534968221800448));
#48504=CARTESIAN_POINT('Ctrl Pts',(1.34124349563131,50.2429399327445,0.585575046793066));
#48505=CARTESIAN_POINT('Ctrl Pts',(1.31913892395465,50.2399418952623,0.636204958616343));
#48506=CARTESIAN_POINT('Ctrl Pts',(1.29418098750364,50.2369438577801,0.685541672072548));
#48507=CARTESIAN_POINT('Ctrl Pts',(1.26655818513784,50.233945820298,0.733254808139941));
#48508=CARTESIAN_POINT('Ctrl Pts',(1.23888146057457,50.2309419303767,0.781061084545183));
#48509=CARTESIAN_POINT('Ctrl Pts',(1.20852976973247,50.2279380404554,0.827237007586373));
#48510=CARTESIAN_POINT('Ctrl Pts',(1.17573512600955,50.2249341505341,0.871481017273076));
#48511=CARTESIAN_POINT('Ctrl Pts',(1.14875744583217,50.2224630768347,0.907877227373038));
#48512=CARTESIAN_POINT('Ctrl Pts',(1.12012747192073,50.2199920031353,0.94296656694366));
#48513=CARTESIAN_POINT('Ctrl Pts',(1.08999331599448,50.2175209294358,0.976599621691185));
#48514=CARTESIAN_POINT('Ctrl Pts',(1.05323995169542,50.2145070646339,1.01762044592303));
#48515=CARTESIAN_POINT('Ctrl Pts',(1.01409059008519,50.2114931998319,1.05664969724153));
#48516=CARTESIAN_POINT('Ctrl Pts',(0.972789141077472,50.2084793350299,1.09339541658165));
#48517=CARTESIAN_POINT('Ctrl Pts',(0.931562323867634,50.2054709162874,1.13007473633616));
#48518=CARTESIAN_POINT('Ctrl Pts',(0.888191527718388,50.2024624975449,1.16447836631213));
#48519=CARTESIAN_POINT('Ctrl Pts',(0.842958644095413,50.1994540788024,1.19634985449275));
#48520=CARTESIAN_POINT('Ctrl Pts',(0.797771407815691,50.1964486960442,1.22818917915328));
#48521=CARTESIAN_POINT('Ctrl Pts',(0.750726235319475,50.1934433132859,1.2575011225332));
#48522=CARTESIAN_POINT('Ctrl Pts',(0.702137934126864,50.1904379305277,1.28406953529007));
#48523=CARTESIAN_POINT('Ctrl Pts',(0.653579593944909,50.1874344009791,1.31062156516304));
#48524=CARTESIAN_POINT('Ctrl Pts',(0.603480472428103,50.1844308714304,1.33443316555242));
#48525=CARTESIAN_POINT('Ctrl Pts',(0.55218223856742,50.1814273418817,1.35533280983332));
#48526=CARTESIAN_POINT('Ctrl Pts',(0.500895501923475,50.1784244854991,1.37622776998141));
#48527=CARTESIAN_POINT('Ctrl Pts',(0.448410674124299,50.1754216291166,1.39421187125809));
#48528=CARTESIAN_POINT('Ctrl Pts',(0.395089662303164,50.172418772734,1.40916159780955));
#48529=CARTESIAN_POINT('Ctrl Pts',(0.341721495107952,50.1694132607225,1.42412454541448));
#48530=CARTESIAN_POINT('Ctrl Pts',(0.28751617447663,50.1664077487111,1.43604761333399));
#48531=CARTESIAN_POINT('Ctrl Pts',(0.232849607511033,50.1634022366997,1.44485753978791));
#48532=CARTESIAN_POINT('Ctrl Pts',(0.178159567937786,50.1603954341883,1.45367124902824));
#48533=CARTESIAN_POINT('Ctrl Pts',(0.1230084120419,50.1573886316769,1.45936909650855));
#48534=CARTESIAN_POINT('Ctrl Pts',(0.0677777807641783,50.1543818291655,
1.46192969134452));
#48535=CARTESIAN_POINT('Ctrl Pts',(0.0124440031447415,50.1513694112795,
1.46449506823682));
#48536=CARTESIAN_POINT('Ctrl Pts',(-0.0429690181593199,50.1483569933936,
1.46391149169015));
#48537=CARTESIAN_POINT('Ctrl Pts',(-0.0980801710523986,50.1453445755077,
1.46020975549622));
#48538=CARTESIAN_POINT('Ctrl Pts',(-0.141977215097185,50.1429451294123,
1.45726125472611));
#48539=CARTESIAN_POINT('Ctrl Pts',(-0.185682698960755,50.140545683317,1.45233551036316));
#48540=CARTESIAN_POINT('Ctrl Pts',(-0.229008582239096,50.1381462372216,
1.44547131388376));
#48541=CARTESIAN_POINT('Ctrl Pts',(-0.284040820412925,50.1350984773374,
1.43675245884971));
#48542=CARTESIAN_POINT('Ctrl Pts',(-0.338705226109161,50.1320507174532,
1.4248654024174));
#48543=CARTESIAN_POINT('Ctrl Pts',(-0.392604340574882,50.1290029575689,
1.40985605001424));
#48544=CARTESIAN_POINT('Ctrl Pts',(-0.445154391254212,50.1260314813589,
1.39522237305557));
#48545=CARTESIAN_POINT('Ctrl Pts',(-0.496976453258863,50.1230600051489,
1.37762101676102));
#48546=CARTESIAN_POINT('Ctrl Pts',(-0.547709178015198,50.1200885289389,
1.35714660457812));
#48547=CARTESIAN_POINT('Ctrl Pts',(-0.598393489551697,50.117119888349,1.33669173071536));
#48548=CARTESIAN_POINT('Ctrl Pts',(-0.647990022335606,50.114151247759,1.31336942968564));
#48549=CARTESIAN_POINT('Ctrl Pts',(-0.696153357328885,50.1111826071691,
1.28732387264422));
#48550=CARTESIAN_POINT('Ctrl Pts',(-0.744290795247793,50.1082155627955,
1.2612923201091));
#48551=CARTESIAN_POINT('Ctrl Pts',(-0.790996087047045,50.105248518422,1.23254066940583));
#48552=CARTESIAN_POINT('Ctrl Pts',(-0.8359468332237,50.1022814740484,1.20125981453775));
#48553=CARTESIAN_POINT('Ctrl Pts',(-0.883014719253845,50.0991746845444,
1.16850565944385));
#48554=CARTESIAN_POINT('Ctrl Pts',(-0.928158107811135,50.0960678950404,
1.13297842579747));
#48555=CARTESIAN_POINT('Ctrl Pts',(-0.971041640784116,50.0929611055363,
1.09494766170045));
#48556=CARTESIAN_POINT('Ctrl Pts',(-1.01202925853428,50.0899916696761,1.05859826804073));
#48557=CARTESIAN_POINT('Ctrl Pts',(-1.05095229273905,50.087022233816,1.01996252088922));
#48558=CARTESIAN_POINT('Ctrl Pts',(-1.08755484312706,50.0840527979558,0.979314409773936));
#48559=CARTESIAN_POINT('Ctrl Pts',(-1.12417879476268,50.0810816258878,0.938642532000828));
#48560=CARTESIAN_POINT('Ctrl Pts',(-1.15847922710366,50.0781104538199,0.895956372875629));
#48561=CARTESIAN_POINT('Ctrl Pts',(-1.19024132733919,50.0751392817519,0.851561995801738));
#48562=CARTESIAN_POINT('Ctrl Pts',(-1.2220545016143,50.0721633319848,0.807096231755478));
#48563=CARTESIAN_POINT('Ctrl Pts',(-1.251320922671,50.0691873822177,0.760917232211028));
#48564=CARTESIAN_POINT('Ctrl Pts',(-1.27787071671936,50.0662114324505,0.713357330761477));
#48565=CARTESIAN_POINT('Ctrl Pts',(-1.28147329568094,50.0658076216337,0.706903860724575));
#48566=CARTESIAN_POINT('Ctrl Pts',(-1.28502592793118,50.0654038108168,0.700424996050097));
#48567=CARTESIAN_POINT('Ctrl Pts',(-1.28852825769066,50.065,0.693921594369763));
#48568=CARTESIAN_POINT('',(-0.262389908308853,50.065,1.43978602091341));
#48569=CARTESIAN_POINT('Origin',(0.,50.065,0.));
#48570=CARTESIAN_POINT('Ctrl Pts',(-0.262389908308852,50.065,1.43978602091341));
#48571=CARTESIAN_POINT('Ctrl Pts',(0.216315810969557,50.0914582307381,1.52702644967428));
#48572=CARTESIAN_POINT('Ctrl Pts',(1.25937612909543,50.1443746922141,1.1847701442246));
#48573=CARTESIAN_POINT('Ctrl Pts',(1.67952585005074,50.2237493844286,-0.41815389563593));
#48574=CARTESIAN_POINT('Ctrl Pts',(0.5592028946949,50.3031240766425,-1.6364077241352));
#48575=CARTESIAN_POINT('Ctrl Pts',(-1.01956042907598,50.3799890265663,-1.36693371954133));
#48576=CARTESIAN_POINT('Ctrl Pts',(-1.4624799194635,50.4303957457519,-0.438091132407085));
#48577=CARTESIAN_POINT('Ctrl Pts',(-1.46539629526008,50.4543442341995,0.000791507262081051));
#48578=CARTESIAN_POINT('Origin',(0.,56.5393671147362,0.));
#48579=CARTESIAN_POINT('',(-1.17776886881611,50.2893670693371,0.000646086109262299));
#48580=CARTESIAN_POINT('Ctrl Pts',(0.18873835403253,50.4271343927849,1.16119835837062));
#48581=CARTESIAN_POINT('Ctrl Pts',(-0.0598496141700551,50.4101796998113,
1.19981666554508));
#48582=CARTESIAN_POINT('Ctrl Pts',(-0.73034770528701,50.3667667760997,1.1033036474199));
#48583=CARTESIAN_POINT('Ctrl Pts',(-1.16118938021621,50.3208443500834,0.464624652439107));
#48584=CARTESIAN_POINT('Ctrl Pts',(-1.17952169233894,50.2918766170408,0.0376575097721022));
#48585=CARTESIAN_POINT('Ctrl Pts',(-1.17927611201048,50.2893671147362,0.000647582463977861));
#48586=CARTESIAN_POINT('',(1.11732377115968,50.0650022861545,-0.372401198845414));
#48587=CARTESIAN_POINT('Ctrl Pts',(-1.17774982279649,50.2893670687634,0.000646067200833073));
#48588=CARTESIAN_POINT('Ctrl Pts',(-1.17777512123915,50.2862359274727,-0.0454717922400353));
#48589=CARTESIAN_POINT('Ctrl Pts',(-1.17508737128827,50.2831047861821,-0.0917002762411251));
#48590=CARTESIAN_POINT('Ctrl Pts',(-1.16967387860585,50.2799736448915,-0.137688344485505));
#48591=CARTESIAN_POINT('Ctrl Pts',(-1.16426758621388,50.2768466682185,-0.183615245666733));
#48592=CARTESIAN_POINT('Ctrl Pts',(-1.15614278161509,50.2737196915454,-0.229301796990624));
#48593=CARTESIAN_POINT('Ctrl Pts',(-1.1453387574601,50.2705927148724,-0.274397873825134));
#48594=CARTESIAN_POINT('Ctrl Pts',(-1.13454402590275,50.2674684277283,-0.319455163288285));
#48595=CARTESIAN_POINT('Ctrl Pts',(-1.12107476478285,50.2643441405842,-0.363922425653406));
#48596=CARTESIAN_POINT('Ctrl Pts',(-1.10502154489056,50.2612198534402,-0.407458522831076));
#48597=CARTESIAN_POINT('Ctrl Pts',(-1.08897459093607,50.2580967857766,-0.450977626877231));
#48598=CARTESIAN_POINT('Ctrl Pts',(-1.07034587439882,50.2549737181131,-0.493565746964381));
#48599=CARTESIAN_POINT('Ctrl Pts',(-1.04927525504211,50.2518506504495,-0.534898590067613));
#48600=CARTESIAN_POINT('Ctrl Pts',(-1.02818743552271,50.2487250333938,-0.5762651735946));
#48601=CARTESIAN_POINT('Ctrl Pts',(-1.00465399029067,50.2455994163381,-0.616373918841575));
#48602=CARTESIAN_POINT('Ctrl Pts',(-0.978861277365035,50.2424737992824,
-0.654924165209448));
#48603=CARTESIAN_POINT('Ctrl Pts',(-0.953057907966577,50.2393468908521,
-0.693490338930674));
#48604=CARTESIAN_POINT('Ctrl Pts',(-0.924993758960615,50.2362199824218,
-0.730496272194395));
#48605=CARTESIAN_POINT('Ctrl Pts',(-0.894896920286096,50.2330930739916,
-0.765672622314825));
#48606=CARTESIAN_POINT('Ctrl Pts',(-0.864741962809198,50.2299601273134,
-0.800916900079192));
#48607=CARTESIAN_POINT('Ctrl Pts',(-0.832546880296198,50.2268271806352,
-0.834324128454841));
#48608=CARTESIAN_POINT('Ctrl Pts',(-0.798576897345711,50.223694233957,-0.865661597580543));
#48609=CARTESIAN_POINT('Ctrl Pts',(-0.776264883462669,50.2216364657833,
-0.886244535382166));
#48610=CARTESIAN_POINT('Ctrl Pts',(-0.753187891129945,50.2195786976095,
-0.905935366721064));
#48611=CARTESIAN_POINT('Ctrl Pts',(-0.729428030643133,50.2175209294358,
-0.924678220037695));
#48612=CARTESIAN_POINT('Ctrl Pts',(-0.691240792213901,50.2142136505935,
-0.954802042054396));
#48613=CARTESIAN_POINT('Ctrl Pts',(-0.651096382328785,50.2109063717513,
-0.982625730784162));
#48614=CARTESIAN_POINT('Ctrl Pts',(-0.609305396523816,50.207599092909,-1.00788987308483));
#48615=CARTESIAN_POINT('Ctrl Pts',(-0.5691739691615,50.2044231491482,-1.03215075308278));
#48616=CARTESIAN_POINT('Ctrl Pts',(-0.527524815107055,50.2012472053874,
-1.05405123231057));
#48617=CARTESIAN_POINT('Ctrl Pts',(-0.484665993251312,50.1980712616266,
-1.07340297068981));
#48618=CARTESIAN_POINT('Ctrl Pts',(-0.441850609314778,50.1948985367221,
-1.09273509585498));
#48619=CARTESIAN_POINT('Ctrl Pts',(-0.397828488955413,50.1917258118176,
-1.1095233654687));
#48620=CARTESIAN_POINT('Ctrl Pts',(-0.352932200540133,50.1885530869131,
-1.12362534873591));
#48621=CARTESIAN_POINT('Ctrl Pts',(-0.308061769503081,50.1853821892944,
-1.1377192101666));
#48622=CARTESIAN_POINT('Ctrl Pts',(-0.262318697469956,50.1822112916756,
-1.14912968372275));
#48623=CARTESIAN_POINT('Ctrl Pts',(-0.216052893589172,50.1790403940568,
-1.15776345151838));
#48624=CARTESIAN_POINT('Ctrl Pts',(-0.169793492708456,50.1758699352775,
-1.16639602443547));
#48625=CARTESIAN_POINT('Ctrl Pts',(-0.12301205036318,50.1726994764981,-1.17225255427138));
#48626=CARTESIAN_POINT('Ctrl Pts',(-0.0760682379740762,50.1695290177188,
-1.17529089406475));
#48627=CARTESIAN_POINT('Ctrl Pts',(-0.0290785465389814,50.1663554603921,
-1.17833220328314));
#48628=CARTESIAN_POINT('Ctrl Pts',(0.0180732756024785,50.1631819030654,
-1.17854979153053));
#48629=CARTESIAN_POINT('Ctrl Pts',(0.0650248635361245,50.1600083457387,
-1.17595358310696));
#48630=CARTESIAN_POINT('Ctrl Pts',(0.112003821854029,50.1568329383898,-1.17335586122612));
#48631=CARTESIAN_POINT('Ctrl Pts',(0.158781760840182,50.1536575310408,-1.16794114135168));
#48632=CARTESIAN_POINT('Ctrl Pts',(0.205002381111276,50.1504821236918,-1.15977113528433));
#48633=CARTESIAN_POINT('Ctrl Pts',(0.251305107393855,50.1473010755698,-1.15158661607094));
#48634=CARTESIAN_POINT('Ctrl Pts',(0.29704799991131,50.1441200274477,-1.14063717773628));
#48635=CARTESIAN_POINT('Ctrl Pts',(0.341887748020115,50.1409389793256,-1.12703497295059));
#48636=CARTESIAN_POINT('Ctrl Pts',(0.355009822639454,50.140008065291,-1.12305437195006));
#48637=CARTESIAN_POINT('Ctrl Pts',(0.3680546771462,50.1390771512563,-1.11884690372938));
#48638=CARTESIAN_POINT('Ctrl Pts',(0.381014047717165,50.1381462372216,-1.11441615114919));
#48639=CARTESIAN_POINT('Ctrl Pts',(0.424750478343914,50.1350045061573,-1.09946285524747));
#48640=CARTESIAN_POINT('Ctrl Pts',(0.467712432024237,50.131862775093,-1.08189410993567));
#48641=CARTESIAN_POINT('Ctrl Pts',(0.509561861228147,50.1287210440287,-1.06181061026989));
#48642=CARTESIAN_POINT('Ctrl Pts',(0.551350779696744,50.1255838556418,-1.04175614964611));
#48643=CARTESIAN_POINT('Ctrl Pts',(0.592029843000789,50.1224466672549,-1.01919436609024));
#48644=CARTESIAN_POINT('Ctrl Pts',(0.63127840950339,50.119309478868,-0.994274927872));
#48645=CARTESIAN_POINT('Ctrl Pts',(0.670488458522769,50.116175369233,-0.969379944917456));
#48646=CARTESIAN_POINT('Ctrl Pts',(0.708270307016205,50.1130412595981,-0.942132187805565));
#48647=CARTESIAN_POINT('Ctrl Pts',(0.744328103564076,50.1099071499631,-0.91272708776759));
#48648=CARTESIAN_POINT('Ctrl Pts',(0.780367258885852,50.106774660606,-0.88333718963241));
#48649=CARTESIAN_POINT('Ctrl Pts',(0.814683685085752,50.1036421712488,-0.851792517324745));
#48650=CARTESIAN_POINT('Ctrl Pts',(0.84701310639821,50.1005096818916,-0.818329921296817));
#48651=CARTESIAN_POINT('Ctrl Pts',(0.879363404201221,50.0973751697521,-0.784845717038939));
#48652=CARTESIAN_POINT('Ctrl Pts',(0.909723729823394,50.0942406576125,-0.749441520262926));
#48653=CARTESIAN_POINT('Ctrl Pts',(0.937866933143905,50.0911061454729,-0.712390818452376));
#48654=CARTESIAN_POINT('Ctrl Pts',(0.966018410066383,50.0879707118425,-0.675329224393495));
#48655=CARTESIAN_POINT('Ctrl Pts',(0.991951141948852,50.084835278212,-0.636620632544208));
#48656=CARTESIAN_POINT('Ctrl Pts',(1.01548083214313,50.0816998445815,-0.596568304597124));
#48657=CARTESIAN_POINT('Ctrl Pts',(1.03905380048362,50.0785586439497,-0.55644230842533));
#48658=CARTESIAN_POINT('Ctrl Pts',(1.06021463686071,50.0754174433179,-0.514968148918674));
#48659=CARTESIAN_POINT('Ctrl Pts',(1.07882547523649,50.072276242686,-0.472472916134642));
#48660=CARTESIAN_POINT('Ctrl Pts',(1.09319094088995,50.0698515905089,-0.439671395071001));
#48661=CARTESIAN_POINT('Ctrl Pts',(1.10603804082557,50.0674269383317,-0.406262031775874));
#48662=CARTESIAN_POINT('Ctrl Pts',(1.11732377115968,50.0650022861545,-0.372401198845414));
#48663=CARTESIAN_POINT('',(0.00936663037036535,50.065,-1.17771275306651));
#48664=CARTESIAN_POINT('Origin',(0.,50.065,0.));
#48665=CARTESIAN_POINT('',(-1.17774995261315,50.1906328853284,0.000334095391369985));
#48666=CARTESIAN_POINT('Ctrl Pts',(-1.17774995261342,50.1906328852638,0.00033409442925833));
#48667=CARTESIAN_POINT('Ctrl Pts',(-1.17776337198618,50.1874545667427,-0.0469718892821487));
#48668=CARTESIAN_POINT('Ctrl Pts',(-1.17492228750547,50.1842762482216,-0.0942679073399217));
#48669=CARTESIAN_POINT('Ctrl Pts',(-1.16925640012487,50.1810979297006,-0.141189706661034));
#48670=CARTESIAN_POINT('Ctrl Pts',(-1.1635813242645,50.1779144568385,-0.188187599976752));
#48671=CARTESIAN_POINT('Ctrl Pts',(-1.15507236871164,50.1747309839765,-0.234809516368601));
#48672=CARTESIAN_POINT('Ctrl Pts',(-1.1438109064012,50.1715475111144,-0.280698544523596));
#48673=CARTESIAN_POINT('Ctrl Pts',(-1.13254022492645,50.1683614321113,-0.326625139601852));
#48674=CARTESIAN_POINT('Ctrl Pts',(-1.11851271896753,50.1651753531082,-0.371817128265236));
#48675=CARTESIAN_POINT('Ctrl Pts',(-1.1018593880314,50.1619892741051,-0.415933830683532));
#48676=CARTESIAN_POINT('Ctrl Pts',(-1.0851621986251,50.158794804195,-0.460166719532286));
#48677=CARTESIAN_POINT('Ctrl Pts',(-1.06582559866182,50.1556003342849,-0.503318164050547));
#48678=CARTESIAN_POINT('Ctrl Pts',(-1.04402789396152,50.1524058643748,-0.545069554396752));
#48679=CARTESIAN_POINT('Ctrl Pts',(-1.02576079236807,50.1497288069879,-0.580058416738353));
#48680=CARTESIAN_POINT('Ctrl Pts',(-1.00576619787879,50.147051749601,-0.614064346226491));
#48681=CARTESIAN_POINT('Ctrl Pts',(-0.98417163956616,50.1443746922142,-0.646916722904622));
#48682=CARTESIAN_POINT('Ctrl Pts',(-0.957493382250771,50.1410674133719,
-0.687503066267285));
#48683=CARTESIAN_POINT('Ctrl Pts',(-0.928250578353563,50.1377601345296,
-0.726512868370853));
#48684=CARTESIAN_POINT('Ctrl Pts',(-0.89665288202166,50.1344528556874,-0.763615526074641));
#48685=CARTESIAN_POINT('Ctrl Pts',(-0.865550916610211,50.1311974641842,
-0.800136086448879));
#48686=CARTESIAN_POINT('Ctrl Pts',(-0.832167754761042,50.1279420726811,
-0.834808491110521));
#48687=CARTESIAN_POINT('Ctrl Pts',(-0.796747002603892,50.124686681178,-0.867346111043172));
#48688=CARTESIAN_POINT('Ctrl Pts',(-0.761373237829212,50.1214356081129,
-0.899840568211077));
#48689=CARTESIAN_POINT('Ctrl Pts',(-0.723967625987618,50.1181845350479,
-0.930205506818803));
#48690=CARTESIAN_POINT('Ctrl Pts',(-0.684811448333999,50.1149334619828,
-0.958190139132464));
#48691=CARTESIAN_POINT('Ctrl Pts',(-0.645693425711961,50.1116855568673,
-0.98614750232555));
#48692=CARTESIAN_POINT('Ctrl Pts',(-0.604828645240271,50.1084376517518,
-1.01172885962529));
#48693=CARTESIAN_POINT('Ctrl Pts',(-0.562530619339646,50.1051897466363,
-1.03472429410223));
#48694=CARTESIAN_POINT('Ctrl Pts',(-0.518914121840659,50.1018406010833,
-1.05843651917646));
#48695=CARTESIAN_POINT('Ctrl Pts',(-0.473773979815151,50.0984914555303,
-1.07939853978092));
#48696=CARTESIAN_POINT('Ctrl Pts',(-0.427483669944292,50.0951423099773,
-1.09743007723999));
#48697=CARTESIAN_POINT('Ctrl Pts',(-0.38261975794465,50.0918963655931,-1.11490598768514));
#48698=CARTESIAN_POINT('Ctrl Pts',(-0.336676080022107,50.088650421209,-1.12962928489099));
#48699=CARTESIAN_POINT('Ctrl Pts',(-0.290012540618924,50.0854044768249,
-1.14148490519312));
#48700=CARTESIAN_POINT('Ctrl Pts',(-0.241123578700135,50.0820037306874,
-1.15390592976365));
#48701=CARTESIAN_POINT('Ctrl Pts',(-0.191444948498638,50.0786029845499,
-1.16317864132221));
#48702=CARTESIAN_POINT('Ctrl Pts',(-0.141404631578315,50.0752022384124,
-1.16923042753266));
#48703=CARTESIAN_POINT('Ctrl Pts',(-0.0913643146579857,50.071801492275,
-1.17528221374311));
#48704=CARTESIAN_POINT('Ctrl Pts',(-0.0409629669169127,50.0684007461375,
-1.17811303635567));
#48705=CARTESIAN_POINT('Ctrl Pts',(0.00936663037036528,50.065,-1.17771275306651));
#48706=CARTESIAN_POINT('Ctrl Pts',(0.188938462403167,50.3284861847587,1.16249615910106));
#48707=CARTESIAN_POINT('Ctrl Pts',(0.14248009936766,50.3253116014759,1.17004695538454));
#48708=CARTESIAN_POINT('Ctrl Pts',(0.0956040622939412,50.3221370181931,
1.17480267720841));
#48709=CARTESIAN_POINT('Ctrl Pts',(0.0486718089546751,50.3189624349103,
1.17674386232225));
#48710=CARTESIAN_POINT('Ctrl Pts',(0.0016509726456754,50.3157818597138,
1.17868871135439));
#48711=CARTESIAN_POINT('Ctrl Pts',(-0.0454257344863767,50.3126012845172,
1.17780842344634));
#48712=CARTESIAN_POINT('Ctrl Pts',(-0.0921978227533305,50.3094207093207,
1.17413569231991));
#48713=CARTESIAN_POINT('Ctrl Pts',(-0.12306295890079,50.3073218317613,1.17171203858857));
#48714=CARTESIAN_POINT('Ctrl Pts',(-0.153795520395974,50.3052229542019,
1.16807342677931));
#48715=CARTESIAN_POINT('Ctrl Pts',(-0.184294402276791,50.3031240766425,
1.16324143486614));
#48716=CARTESIAN_POINT('Ctrl Pts',(-0.232352616204662,50.2998167978003,
1.15562748685427));
#48717=CARTESIAN_POINT('Ctrl Pts',(-0.280048180995003,50.296509518958,1.14501289851391));
#48718=CARTESIAN_POINT('Ctrl Pts',(-0.32697913045126,50.2932022401158,1.13145026879193));
#48719=CARTESIAN_POINT('Ctrl Pts',(-0.372007028384608,50.2900290715378,
1.11843760414516));
#48720=CARTESIAN_POINT('Ctrl Pts',(-0.416330533826876,50.2868559029599,
1.10271157111116));
#48721=CARTESIAN_POINT('Ctrl Pts',(-0.459602722373217,50.283682734382,1.08437096977332));
#48722=CARTESIAN_POINT('Ctrl Pts',(-0.502832382507399,50.2805126844312,
1.06604839379262));
#48723=CARTESIAN_POINT('Ctrl Pts',(-0.545012260170822,50.2773426344804,
1.04511655198512));
#48724=CARTESIAN_POINT('Ctrl Pts',(-0.58581260118302,50.2741725845297,1.02172337684678));
#48725=CARTESIAN_POINT('Ctrl Pts',(-0.626590765441402,50.2710042576384,
0.998342916913098));
#48726=CARTESIAN_POINT('Ctrl Pts',(-0.665990395956384,50.2678359307472,
0.972504050473419));
#48727=CARTESIAN_POINT('Ctrl Pts',(-0.703706131398171,50.264667603856,0.944400732280858));
#48728=CARTESIAN_POINT('Ctrl Pts',(-0.741417932828378,50.2614996074431,
0.916300345458397));
#48729=CARTESIAN_POINT('Ctrl Pts',(-0.777445742742863,50.2583316110302,
0.885936310231308));
#48730=CARTESIAN_POINT('Ctrl Pts',(-0.811515247945782,50.2551636146174,
0.853544412934381));
#48731=CARTESIAN_POINT('Ctrl Pts',(-0.845619973557182,50.2519923431899,
0.821119029508215));
#48732=CARTESIAN_POINT('Ctrl Pts',(-0.877761951698038,50.2488210717624,
0.78666198668075));
#48733=CARTESIAN_POINT('Ctrl Pts',(-0.907703359196014,50.2456498003349,
0.750446316670467));
#48734=CARTESIAN_POINT('Ctrl Pts',(-0.937663178849942,50.2424765787672,
0.714208376212005));
#48735=CARTESIAN_POINT('Ctrl Pts',(-0.965419406449462,50.2393033571994,
0.676210106592592));
#48736=CARTESIAN_POINT('Ctrl Pts',(-0.990776454845308,50.2361301356317,
0.636755116998806));
#48737=CARTESIAN_POINT('Ctrl Pts',(-1.01617991710229,50.2329511057592,0.597227908494544));
#48738=CARTESIAN_POINT('Ctrl Pts',(-1.03917516977404,50.2297720758867,0.556239147564299));
#48739=CARTESIAN_POINT('Ctrl Pts',(-1.05961254906646,50.2265930460142,0.514117018159183));
#48740=CARTESIAN_POINT('Ctrl Pts',(-1.06570633582303,50.2256451588189,0.501557517713692));
#48741=CARTESIAN_POINT('Ctrl Pts',(-1.0715730451748,50.2246972716236,0.48889738151205));
#48742=CARTESIAN_POINT('Ctrl Pts',(-1.07720955856848,50.2237493844284,0.476145596880503));
#48743=CARTESIAN_POINT('Ctrl Pts',(-1.09783991697972,50.2202799963145,0.429472437613947));
#48744=CARTESIAN_POINT('Ctrl Pts',(-1.11546555051765,50.2168106082007,0.381383059316153));
#48745=CARTESIAN_POINT('Ctrl Pts',(-1.12990975478779,50.2133412200869,0.332263462534478));
#48746=CARTESIAN_POINT('Ctrl Pts',(-1.14430397109725,50.2098838387013,0.283313857012021));
#48747=CARTESIAN_POINT('Ctrl Pts',(-1.15553853907606,50.2064264573158,0.233341485789629));
#48748=CARTESIAN_POINT('Ctrl Pts',(-1.16348484842626,50.2029690759303,0.182751388455792));
#48749=CARTESIAN_POINT('Ctrl Pts',(-1.17139080064078,50.1995292536409,0.132418224414226));
#48750=CARTESIAN_POINT('Ctrl Pts',(-1.17604165465704,50.1960894313515,0.0814739523451495));
#48751=CARTESIAN_POINT('Ctrl Pts',(-1.17735926665214,50.1926496090621,0.0303351236742758));
#48752=CARTESIAN_POINT('Ctrl Pts',(-1.17761676632884,50.1919773678176,0.0203411103391975));
#48753=CARTESIAN_POINT('Ctrl Pts',(-1.17774711429415,50.191305126573,0.0103397109874767));
#48754=CARTESIAN_POINT('Ctrl Pts',(-1.17774995261315,50.1906328853284,0.000334095391379412));
#48755=CARTESIAN_POINT('Origin',(3.28582941601228E-17,50.065,0.));
#48756=CARTESIAN_POINT('',(-1.30071912068084,50.065,0.670792083357623));
#48757=CARTESIAN_POINT('',(-1.4635,50.065,1.79227059055215E-16));
#48758=CARTESIAN_POINT('Origin',(0.,50.065,0.));
#48759=CARTESIAN_POINT('Ctrl Pts',(-1.30071912068084,50.065,0.670792083357622));
#48760=CARTESIAN_POINT('Ctrl Pts',(-1.31175604994526,50.065,0.643640642407746));
#48761=CARTESIAN_POINT('Ctrl Pts',(-1.32190228759372,50.065,0.616162032086531));
#48762=CARTESIAN_POINT('Ctrl Pts',(-1.33112168336828,50.065,0.588379227984466));
#48763=CARTESIAN_POINT('Ctrl Pts',(-1.34927016508087,50.065,0.533688473351472));
#48764=CARTESIAN_POINT('Ctrl Pts',(-1.36383020120747,50.065,0.477818733970761));
#48765=CARTESIAN_POINT('Ctrl Pts',(-1.37486275654977,50.065,0.421110295908625));
#48766=CARTESIAN_POINT('Ctrl Pts',(-1.38091979747305,50.065,0.389976499668264));
#48767=CARTESIAN_POINT('Ctrl Pts',(-1.38591268206054,50.065,0.358589878940197));
#48768=CARTESIAN_POINT('Ctrl Pts',(-1.38984515858309,50.065,0.327007742108425));
#48769=CARTESIAN_POINT('Ctrl Pts',(-1.39224930977373,50.065,0.307699748422531));
#48770=CARTESIAN_POINT('Ctrl Pts',(-1.3942544329935,50.065,0.288338607708039));
#48771=CARTESIAN_POINT('Ctrl Pts',(-1.3958626601646,50.065,0.268947491632431));
#48772=CARTESIAN_POINT('Ctrl Pts',(-1.40061569214788,50.065,0.211638053914574));
#48773=CARTESIAN_POINT('Ctrl Pts',(-1.40190929233838,50.065,0.154037716185528));
#48774=CARTESIAN_POINT('Ctrl Pts',(-1.39979622763592,50.065,0.0964884123102473));
#48775=CARTESIAN_POINT('Ctrl Pts',(-1.39799633646646,50.065,0.0474683876358261));
#48776=CARTESIAN_POINT('Ctrl Pts',(-1.39372374270588,50.065,-0.00151496550527628));
#48777=CARTESIAN_POINT('Ctrl Pts',(-1.38698332842043,50.065,-0.0502392570618477));
#48778=CARTESIAN_POINT('Ctrl Pts',(-1.38548901145288,50.065,-0.061041194824286));
#48779=CARTESIAN_POINT('Ctrl Pts',(-1.38387401566659,50.065,-0.0718248289893012));
#48780=CARTESIAN_POINT('Ctrl Pts',(-1.38213998134003,50.065,-0.0825802196834237));
#48781=CARTESIAN_POINT('Ctrl Pts',(-1.37319554758143,50.065,-0.138058290756452));
#48782=CARTESIAN_POINT('Ctrl Pts',(-1.36107927502691,50.065,-0.192849000747329));
#48783=CARTESIAN_POINT('Ctrl Pts',(-1.34584240689984,50.065,-0.246634504257576));
#48784=CARTESIAN_POINT('Ctrl Pts',(-1.3309686912773,50.065,-0.299138094703773));
#48785=CARTESIAN_POINT('Ctrl Pts',(-1.31312085741118,50.065,-0.350684738983978));
#48786=CARTESIAN_POINT('Ctrl Pts',(-1.29230435568534,50.065,-0.400954342832866));
#48787=CARTESIAN_POINT('Ctrl Pts',(-1.28027653029496,50.065,-0.430000242355331));
#48788=CARTESIAN_POINT('Ctrl Pts',(-1.26725685158702,50.065,-0.458619267214444));
#48789=CARTESIAN_POINT('Ctrl Pts',(-1.25324064993564,50.065,-0.486744051974305));
#48790=CARTESIAN_POINT('Ctrl Pts',(-1.24638872355449,50.065,-0.500493066111903));
#48791=CARTESIAN_POINT('Ctrl Pts',(-1.23929858571003,50.065,-0.514123894689191));
#48792=CARTESIAN_POINT('Ctrl Pts',(-1.23196935359747,50.065,-0.527628224413549));
#48793=CARTESIAN_POINT('Ctrl Pts',(-1.22699450677309,50.065,-0.536794528715686));
#48794=CARTESIAN_POINT('Ctrl Pts',(-1.2219086199582,50.065,-0.545904071351034));
#48795=CARTESIAN_POINT('Ctrl Pts',(-1.21671412257452,50.065,-0.554949372359807));
#48796=CARTESIAN_POINT('Ctrl Pts',(-1.19038939303419,50.065,-0.600789245802538));
#48797=CARTESIAN_POINT('Ctrl Pts',(-1.16138549452255,50.065,-0.644797644261427));
#48798=CARTESIAN_POINT('Ctrl Pts',(-1.12972143997519,50.065,-0.686686087702281));
#48799=CARTESIAN_POINT('Ctrl Pts',(-1.1202930926426,50.065,-0.699158867945605));
#48800=CARTESIAN_POINT('Ctrl Pts',(-1.11062862879451,50.065,-0.711443459549966));
#48801=CARTESIAN_POINT('Ctrl Pts',(-1.10072790598129,50.065,-0.723531608836915));
#48802=CARTESIAN_POINT('Ctrl Pts',(-1.06670404828826,50.065,-0.765072562853135));
#48803=CARTESIAN_POINT('Ctrl Pts',(-1.02989193273851,50.065,-0.804297171032527));
#48804=CARTESIAN_POINT('Ctrl Pts',(-0.990590001990912,50.065,-0.841070267115875));
#48805=CARTESIAN_POINT('Ctrl Pts',(-0.971180658196642,50.065,-0.85923074042303));
#48806=CARTESIAN_POINT('Ctrl Pts',(-0.951163683276724,50.065,-0.876792598798188));
#48807=CARTESIAN_POINT('Ctrl Pts',(-0.930573455824569,50.065,-0.89373515421317));
#48808=CARTESIAN_POINT('Ctrl Pts',(-0.916787514647906,50.065,-0.905078840089203));
#48809=CARTESIAN_POINT('Ctrl Pts',(-0.902744577782523,50.065,-0.916144842788307));
#48810=CARTESIAN_POINT('Ctrl Pts',(-0.888454863816197,50.065,-0.926926174066913));
#48811=CARTESIAN_POINT('Ctrl Pts',(-0.880246416042113,50.065,-0.933119299761667));
#48812=CARTESIAN_POINT('Ctrl Pts',(-0.871963127969767,50.065,-0.939213453383781));
#48813=CARTESIAN_POINT('Ctrl Pts',(-0.863611899391003,50.065,-0.945204552503321));
#48814=CARTESIAN_POINT('Ctrl Pts',(-0.82097856900588,50.065,-0.975789334817011));
#48815=CARTESIAN_POINT('Ctrl Pts',(-0.776538365170856,50.065,-1.00372098297481));
#48816=CARTESIAN_POINT('Ctrl Pts',(-0.730581585765392,50.065,-1.02889132098778));
#48817=CARTESIAN_POINT('Ctrl Pts',(-0.6849361843158,50.065,-1.05389111858212));
#48818=CARTESIAN_POINT('Ctrl Pts',(-0.637793529996918,50.065,-1.07616713862166));
#48819=CARTESIAN_POINT('Ctrl Pts',(-0.5894257667048,50.065,-1.09556439483884));
#48820=CARTESIAN_POINT('Ctrl Pts',(-0.564948289877972,50.065,-1.10538076543867));
#48821=CARTESIAN_POINT('Ctrl Pts',(-0.540156966365709,50.065,-1.11445906184859));
#48822=CARTESIAN_POINT('Ctrl Pts',(-0.515087268773155,50.065,-1.12277406719407));
#48823=CARTESIAN_POINT('Ctrl Pts',(-0.496757115239239,50.065,-1.12885373066249));
#48824=CARTESIAN_POINT('Ctrl Pts',(-0.478278145159383,50.065,-1.134525262181));
#48825=CARTESIAN_POINT('Ctrl Pts',(-0.459664493506921,50.065,-1.13977758010901));
#48826=CARTESIAN_POINT('Ctrl Pts',(-0.45066760368625,50.065,-1.14231628270127));
#48827=CARTESIAN_POINT('Ctrl Pts',(-0.441640205098046,50.065,-1.14475666360343));
#48828=CARTESIAN_POINT('Ctrl Pts',(-0.432596391441415,50.065,-1.14709452097211));
#48829=CARTESIAN_POINT('Ctrl Pts',(-0.383773881833472,50.065,-1.15971530996425));
#48830=CARTESIAN_POINT('Ctrl Pts',(-0.334376697505691,50.065,-1.16938014447876));
#48831=CARTESIAN_POINT('Ctrl Pts',(-0.284657998630276,50.065,-1.17596097943796));
#48832=CARTESIAN_POINT('Ctrl Pts',(-0.23594412541215,50.065,-1.18240881429936));
#48833=CARTESIAN_POINT('Ctrl Pts',(-0.186920658325916,50.065,-1.18589607879924));
#48834=CARTESIAN_POINT('Ctrl Pts',(-0.137832125061594,50.065,-1.18625310484368));
#48835=CARTESIAN_POINT('Ctrl Pts',(-0.088743591797191,50.065,-1.18661013088813));
#48836=CARTESIAN_POINT('Ctrl Pts',(-0.0395890858340499,50.065,-1.18383710324689));
#48837=CARTESIAN_POINT('Ctrl Pts',(0.009366630370399,50.065,-1.17771275306651));
#48838=CARTESIAN_POINT('Ctrl Pts',(1.11912387040083,50.065,-0.3729656372709));
#48839=CARTESIAN_POINT('Ctrl Pts',(1.13246075041995,50.065,-0.344966336154387));
#48840=CARTESIAN_POINT('Ctrl Pts',(1.14459340453453,50.065,-0.316466733140529));
#48841=CARTESIAN_POINT('Ctrl Pts',(1.15546879160855,50.065,-0.28752483843055));
#48842=CARTESIAN_POINT('Ctrl Pts',(1.17244188610288,50.065,-0.242355548324976));
#48843=CARTESIAN_POINT('Ctrl Pts',(1.18635529783476,50.065,-0.196110283010327));
#48844=CARTESIAN_POINT('Ctrl Pts',(1.19732570794754,50.065,-0.149071507418727));
#48845=CARTESIAN_POINT('Ctrl Pts',(1.20207169098707,50.065,-0.128721745754101));
#48846=CARTESIAN_POINT('Ctrl Pts',(1.20626631636867,50.065,-0.108223099821439));
#48847=CARTESIAN_POINT('Ctrl Pts',(1.20991649016097,50.065,-0.0875970128177899));
#48848=CARTESIAN_POINT('Ctrl Pts',(1.21236509669315,50.065,-0.0737606383752849));
#48849=CARTESIAN_POINT('Ctrl Pts',(1.21456884754754,50.065,-0.059864243936097));
#48850=CARTESIAN_POINT('Ctrl Pts',(1.21652661323577,50.065,-0.0459384094572504));
#48851=CARTESIAN_POINT('Ctrl Pts',(1.2235769855708,50.065,0.0042117789653206));
#48852=CARTESIAN_POINT('Ctrl Pts',(1.22745360466983,50.065,0.0548056738949035));
#48853=CARTESIAN_POINT('Ctrl Pts',(1.22828254246297,50.065,0.105533114130644));
#48854=CARTESIAN_POINT('Ctrl Pts',(1.22886776554746,50.065,0.141346258721905));
#48855=CARTESIAN_POINT('Ctrl Pts',(1.22793295114377,50.065,0.177226698754145));
#48856=CARTESIAN_POINT('Ctrl Pts',(1.22550808937998,50.065,0.213071201673675));
#48857=CARTESIAN_POINT('Ctrl Pts',(1.22464231733817,50.065,0.225869114092314));
#48858=CARTESIAN_POINT('Ctrl Pts',(1.22358648781239,50.065,0.238662474148506));
#48859=CARTESIAN_POINT('Ctrl Pts',(1.22234159897063,50.065,0.251446654317747));
#48860=CARTESIAN_POINT('Ctrl Pts',(1.22143521697024,50.065,0.260754594437777));
#48861=CARTESIAN_POINT('Ctrl Pts',(1.22042868456239,50.065,0.270056192665202));
#48862=CARTESIAN_POINT('Ctrl Pts',(1.21932376301989,50.065,0.27934010984953));
#48863=CARTESIAN_POINT('Ctrl Pts',(1.21304427883545,50.065,0.332102418200232));
#48864=CARTESIAN_POINT('Ctrl Pts',(1.20358324825889,50.065,0.384376692221464));
#48865=CARTESIAN_POINT('Ctrl Pts',(1.19107048812719,50.065,0.435835777877265));
#48866=CARTESIAN_POINT('Ctrl Pts',(1.17861838364559,50.065,0.48704541542878));
#48867=CARTESIAN_POINT('Ctrl Pts',(1.16314397006523,50.065,0.537448933599227));
#48868=CARTESIAN_POINT('Ctrl Pts',(1.14472492208604,50.065,0.586733910875349));
#48869=CARTESIAN_POINT('Ctrl Pts',(1.13394477086779,50.065,0.615579023197392));
#48870=CARTESIAN_POINT('Ctrl Pts',(1.12215501838417,50.065,0.64404108706711));
#48871=CARTESIAN_POINT('Ctrl Pts',(1.10936337857097,50.065,0.672056579431857));
#48872=CARTESIAN_POINT('Ctrl Pts',(1.10160261146699,50.065,0.689053752172891));
#48873=CARTESIAN_POINT('Ctrl Pts',(1.09347294523412,50.065,0.70588652224452));
#48874=CARTESIAN_POINT('Ctrl Pts',(1.08497507156082,50.065,0.722540339201735));
#48875=CARTESIAN_POINT('Ctrl Pts',(1.08052819384105,50.065,0.731255164865588));
#48876=CARTESIAN_POINT('Ctrl Pts',(1.07598037774297,50.065,0.739920924916033));
#48877=CARTESIAN_POINT('Ctrl Pts',(1.07133886425922,50.065,0.748522809552601));
#48878=CARTESIAN_POINT('Ctrl Pts',(1.04531350200145,50.065,0.796754310882876));
#48879=CARTESIAN_POINT('Ctrl Pts',(1.01629564612237,50.065,0.843079360691641));
#48880=CARTESIAN_POINT('Ctrl Pts',(0.984386029779273,50.065,0.887164229561829));
#48881=CARTESIAN_POINT('Ctrl Pts',(0.979086611727012,50.065,0.894485663558722));
#48882=CARTESIAN_POINT('Ctrl Pts',(0.97370731930311,50.065,0.901745301457201));
#48883=CARTESIAN_POINT('Ctrl Pts',(0.968248475848336,50.065,0.908941595055685));
#48884=CARTESIAN_POINT('Ctrl Pts',(0.936337800817732,50.065,0.951008854970467));
#48885=CARTESIAN_POINT('Ctrl Pts',(0.901712641810621,50.065,0.990913516768476));
#48886=CARTESIAN_POINT('Ctrl Pts',(0.864670234321161,50.065,1.02859685862274));
#48887=CARTESIAN_POINT('Ctrl Pts',(0.845706643529314,50.065,1.04788857109572));
#48888=CARTESIAN_POINT('Ctrl Pts',(0.826108741599738,50.065,1.06659771666816));
#48889=CARTESIAN_POINT('Ctrl Pts',(0.805912002498264,50.065,1.08471359677496));
#48890=CARTESIAN_POINT('Ctrl Pts',(0.793586884256897,50.065,1.09576886481803));
#48891=CARTESIAN_POINT('Ctrl Pts',(0.781038699666901,50.065,1.10660315596534));
#48892=CARTESIAN_POINT('Ctrl Pts',(0.768275050659485,50.065,1.11721363233496));
#48893=CARTESIAN_POINT('Ctrl Pts',(0.760318925263968,50.065,1.12382759362878));
#48894=CARTESIAN_POINT('Ctrl Pts',(0.7522775593948,50.065,1.13035566915275));
#48895=CARTESIAN_POINT('Ctrl Pts',(0.744166470702853,50.065,1.13678655984908));
#48896=CARTESIAN_POINT('Ctrl Pts',(0.70143902438249,50.065,1.17066308955491));
#48897=CARTESIAN_POINT('Ctrl Pts',(0.656704573419184,50.065,1.2019097711863));
#48898=CARTESIAN_POINT('Ctrl Pts',(0.610290795174932,50.065,1.23047751400324));
#48899=CARTESIAN_POINT('Ctrl Pts',(0.562526701200975,50.065,1.25987637796452));
#48900=CARTESIAN_POINT('Ctrl Pts',(0.512983462755402,50.065,1.28643883982959));
#48901=CARTESIAN_POINT('Ctrl Pts',(0.46197321398113,50.065,1.31007946992396));
#48902=CARTESIAN_POINT('Ctrl Pts',(0.433134381054957,50.065,1.32344478763841));
#48903=CARTESIAN_POINT('Ctrl Pts',(0.40382590289864,50.065,1.33587558469587));
#48904=CARTESIAN_POINT('Ctrl Pts',(0.374099449030773,50.065,1.34735081798353));
#48905=CARTESIAN_POINT('Ctrl Pts',(0.355628125637758,50.065,1.35448125964363));
#48906=CARTESIAN_POINT('Ctrl Pts',(0.336995357365496,50.065,1.3612426655871));
#48907=CARTESIAN_POINT('Ctrl Pts',(0.318213056572565,50.065,1.36762909032308));
#48908=CARTESIAN_POINT('Ctrl Pts',(0.308740505021669,50.065,1.37084998100119));
#48909=CARTESIAN_POINT('Ctrl Pts',(0.299229914316878,50.065,1.37397548289385));
#48910=CARTESIAN_POINT('Ctrl Pts',(0.289682784609941,50.065,1.37700476219547));
#48911=CARTESIAN_POINT('Ctrl Pts',(0.279575173142051,50.065,1.38021188089485));
#48912=CARTESIAN_POINT('Ctrl Pts',(0.2694357466268,50.065,1.38330822235196));
#48913=CARTESIAN_POINT('Ctrl Pts',(0.259269706426227,50.065,1.38629245527359));
#48914=CARTESIAN_POINT('Ctrl Pts',(0.203372665229807,50.065,1.40270098674391));
#48915=CARTESIAN_POINT('Ctrl Pts',(0.146643819123119,50.065,1.41573293027852));
#48916=CARTESIAN_POINT('Ctrl Pts',(0.089415544266844,50.065,1.42530658648151));
#48917=CARTESIAN_POINT('Ctrl Pts',(0.0313884653490651,50.065,1.43501387375197));
#48918=CARTESIAN_POINT('Ctrl Pts',(-0.0271531028235179,50.065,1.44116635899906));
#48919=CARTESIAN_POINT('Ctrl Pts',(-0.0858909126126426,50.065,1.44363247257722));
#48920=CARTESIAN_POINT('Ctrl Pts',(-0.144628722401879,50.065,1.44609858615538));
#48921=CARTESIAN_POINT('Ctrl Pts',(-0.203563913133846,50.065,1.44487896824704));
#48922=CARTESIAN_POINT('Ctrl Pts',(-0.262389908308771,50.065,1.43978602091342));
#48923=CARTESIAN_POINT('Origin',(0.,50.065,0.));
#48924=CARTESIAN_POINT('Ctrl Pts',(-0.509296898212844,55.7812034156616,
1.05958297275613));
#48925=CARTESIAN_POINT('Ctrl Pts',(-0.861591212604499,55.7547451849235,
0.890249936843907));
#48926=CARTESIAN_POINT('Ctrl Pts',(-1.37785557857217,55.7018287234474,0.175325859793372));
#48927=CARTESIAN_POINT('Ctrl Pts',(-0.89405509938618,55.6224540312332,-1.06476771329504));
#48928=CARTESIAN_POINT('Ctrl Pts',(0.409241656719022,55.543079339019,-1.32750887748838));
#48929=CARTESIAN_POINT('Ctrl Pts',(1.33736108858238,55.4637046468048,-0.376885391722574));
#48930=CARTESIAN_POINT('Ctrl Pts',(1.04199119975101,55.3843299545907,0.919363910817131));
#48931=CARTESIAN_POINT('Ctrl Pts',(-0.20709067843855,55.3049552623765,1.3739204743444));
#48932=CARTESIAN_POINT('Ctrl Pts',(-1.26657263663979,55.2255805701623,0.57137806271837));
#48933=CARTESIAN_POINT('Ctrl Pts',(-1.16704611942123,55.1462058779482,-0.754135090264633));
#48934=CARTESIAN_POINT('Ctrl Pts',(0.00047956154262669,55.0668311857339,
-1.38948211737794));
#48935=CARTESIAN_POINT('Ctrl Pts',(1.16755463529987,54.9874564935198,-0.753324638459543));
#48936=CARTESIAN_POINT('Ctrl Pts',(1.26619427179722,54.9080818013055,0.572220836148192));
#48937=CARTESIAN_POINT('Ctrl Pts',(0.206123279084574,54.8287071090914,1.37411455837363));
#48938=CARTESIAN_POINT('Ctrl Pts',(-1.04257172449213,54.7493324168772,0.91854502704819));
#48939=CARTESIAN_POINT('Ctrl Pts',(-1.33719926070647,54.669957724663,-0.377596321548186));
#48940=CARTESIAN_POINT('Ctrl Pts',(-0.40814140684798,54.5905830324488,-1.32819448115672));
#48941=CARTESIAN_POINT('Ctrl Pts',(0.894410699853024,54.5112083402347,-1.06334845704124));
#48942=CARTESIAN_POINT('Ctrl Pts',(1.37847835230742,54.4318336480205,0.174579051125748));
#48943=CARTESIAN_POINT('Ctrl Pts',(0.601086036540525,54.3524589558063,1.25274733591148));
#48944=CARTESIAN_POINT('Ctrl Pts',(-0.726366352456438,54.2730842635921,
1.18451352739661));
#48945=CARTESIAN_POINT('Ctrl Pts',(-1.38911333142688,54.193709571378,0.032319008359879));
#48946=CARTESIAN_POINT('Ctrl Pts',(-0.780668207941864,54.1143348791637,
-1.14945095732061));
#48947=CARTESIAN_POINT('Ctrl Pts',(0.542174529980675,54.0349601869497,-1.27934637292781));
#48948=CARTESIAN_POINT('Ctrl Pts',(1.36886770346268,53.9555854947353,-0.238498577598694));
#48949=CARTESIAN_POINT('Ctrl Pts',(0.942895765841905,53.8762108025213,1.02060175121614));
#48950=CARTESIAN_POINT('Ctrl Pts',(-0.345929919276582,53.796836110307,1.34573877552148));
#48951=CARTESIAN_POINT('Ctrl Pts',(-1.31819152809999,53.717461418093,0.439376212287943));
#48952=CARTESIAN_POINT('Ctrl Pts',(-1.08416232315526,53.6380867258786,-0.869064104425588));
#48953=CARTESIAN_POINT('Ctrl Pts',(0.141995129440038,53.5587120336646,-1.38221479659209));
#48954=CARTESIAN_POINT('Ctrl Pts',(1.2382113583717,53.4793373414503,-0.630486314404458));
#48955=CARTESIAN_POINT('Ctrl Pts',(1.2013274610036,53.3999626492361,0.698206768858064));
#48956=CARTESIAN_POINT('Ctrl Pts',(0.0650962764719148,53.320587957022,1.38796355696017));
#48957=CARTESIAN_POINT('Ctrl Pts',(-1.13070518949629,53.2412132648078,0.807580420204971));
#48958=CARTESIAN_POINT('Ctrl Pts',(-1.29178654540564,53.1618385725937,-0.511827980634577));
#48959=CARTESIAN_POINT('Ctrl Pts',(-0.270740562688289,53.0824638803794,
-1.36285725898538));
#48960=CARTESIAN_POINT('Ctrl Pts',(0.99806293226542,53.0030891881654,-0.966721647575289));
#48961=CARTESIAN_POINT('Ctrl Pts',(1.3535286299656,52.923714495951,0.314071024636275));
#48962=CARTESIAN_POINT('Ctrl Pts',(0.470366163602632,52.844339803737,1.30745402702759));
#48963=CARTESIAN_POINT('Ctrl Pts',(-0.843233284116505,52.7649651115227,
1.10437221497646));
#48964=CARTESIAN_POINT('Ctrl Pts',(-1.38518116018734,52.6855904193086,-0.109332127545164));
#48965=CARTESIAN_POINT('Ctrl Pts',(-0.659535311713787,52.6062157270943,
-1.22298550001824));
#48966=CARTESIAN_POINT('Ctrl Pts',(0.669658178237574,52.5268410348802,-1.21747208796736));
#48967=CARTESIAN_POINT('Ctrl Pts',(1.38604048598882,52.447466342666,-0.0978372722456281));
#48968=CARTESIAN_POINT('Ctrl Pts',(0.834042691206619,52.3680916504517,1.11132945155648));
#48969=CARTESIAN_POINT('Ctrl Pts',(-0.481196267839791,52.2887169582377,
1.30350700516717));
#48970=CARTESIAN_POINT('Ctrl Pts',(-1.35608750414732,52.2093422660234,0.302831705153106));
#48971=CARTESIAN_POINT('Ctrl Pts',(-0.99000892405737,52.1299675738093,-0.974968046125547));
#48972=CARTESIAN_POINT('Ctrl Pts',(0.282037146610221,52.0505928815951,-1.36056437147411));
#48973=CARTESIAN_POINT('Ctrl Pts',(1.29598808285279,51.971218189381,-0.501094051981872));
#48974=CARTESIAN_POINT('Ctrl Pts',(1.12396681059968,51.8918434971667,0.816932659262804));
#48975=CARTESIAN_POINT('Ctrl Pts',(-0.0766082126106224,51.8124688049526,
1.38737577629275));
#48976=CARTESIAN_POINT('Ctrl Pts',(-1.20707825824582,51.7330941127383,0.688216850016528));
#48977=CARTESIAN_POINT('Ctrl Pts',(-1.23293840873169,51.6537194205242,-0.640736487273394));
#48978=CARTESIAN_POINT('Ctrl Pts',(-0.130523751273304,51.57434472831,-1.38334519369534));
#48979=CARTESIAN_POINT('Ctrl Pts',(1.09133452682926,51.4949700360959,-0.860040267375685));
#48980=CARTESIAN_POINT('Ctrl Pts',(1.3145012484704,51.4155953438816,0.450296436408177));
#48981=CARTESIAN_POINT('Ctrl Pts',(0.334754072362915,51.3362206516676,1.3485622537132));
#48982=CARTESIAN_POINT('Ctrl Pts',(-0.951329854768783,51.2568459594532,
1.01274453599346));
#48983=CARTESIAN_POINT('Ctrl Pts',(-1.36684228725746,51.1774712672391,-0.249845965837834));
#48984=CARTESIAN_POINT('Ctrl Pts',(-0.531542350422215,51.098096575025,-1.28380041172025));
#48985=CARTESIAN_POINT('Ctrl Pts',(0.790176083470376,51.0187218828107,-1.14293454879374));
#48986=CARTESIAN_POINT('Ctrl Pts',(1.38879899296093,50.9393471905966,0.0438403513319658));
#48987=CARTESIAN_POINT('Ctrl Pts',(0.716511864201961,50.8599724983823,1.19050098100684));
#48988=CARTESIAN_POINT('Ctrl Pts',(-0.611451749480356,50.7805978061683,
1.24771292473461));
#48989=CARTESIAN_POINT('Ctrl Pts',(-1.3798910848444,50.701223113954,0.163147090662219));
#48990=CARTESIAN_POINT('Ctrl Pts',(-0.885535284470352,50.6218484217398,
-1.07075038846525));
#48991=CARTESIAN_POINT('Ctrl Pts',(0.419099779724909,50.5424737295257,-1.32472615794866));
#48992=CARTESIAN_POINT('Ctrl Pts',(1.34037590341986,50.4630990373115,-0.366562543644245));
#48993=CARTESIAN_POINT('Ctrl Pts',(1.03473860200598,50.3837243450974,0.92730432182043));
#48994=CARTESIAN_POINT('Ctrl Pts',(-0.217166894820808,50.3043496528831,
1.3720776556735));
#48995=CARTESIAN_POINT('Ctrl Pts',(-1.27158730416588,50.224974960669,0.562254863827906));
#48996=CARTESIAN_POINT('Ctrl Pts',(-1.15984632322935,50.1455937665709,-0.76428168828827));
#48997=CARTESIAN_POINT('Ctrl Pts',(-0.381323777793448,50.092670803211,-1.17880055994548));
#48998=CARTESIAN_POINT('Ctrl Pts',(0.00963790343894936,50.0662060705889,
-1.17558773000307));
#48999=CARTESIAN_POINT('Ctrl Pts',(-0.551142003322691,55.7254357270455,
1.1466409560723));
#49000=CARTESIAN_POINT('Ctrl Pts',(-0.932381698428526,55.6989774963075,
0.9633950950257));
#49001=CARTESIAN_POINT('Ctrl Pts',(-1.49106363405782,55.6460610348314,0.189731070304719));
#49002=CARTESIAN_POINT('Ctrl Pts',(-0.967512899225719,55.5666863426171,
-1.15225168784261));
#49003=CARTESIAN_POINT('Ctrl Pts',(0.442865973302976,55.4873116504031,-1.43658032227372));
#49004=CARTESIAN_POINT('Ctrl Pts',(1.44724201563678,55.4079369581888,-0.407851236765698));
#49005=CARTESIAN_POINT('Ctrl Pts',(1.1276037990622,55.3285622659747,0.994901145811772));
#49006=CARTESIAN_POINT('Ctrl Pts',(-0.22410576578139,55.2491875737605,1.48680521183891));
#49007=CARTESIAN_POINT('Ctrl Pts',(-1.37063740769069,55.1698128815463,0.618323911349722));
#49008=CARTESIAN_POINT('Ctrl Pts',(-1.26293354325317,55.0904381893321,-0.816096712708995));
#49009=CARTESIAN_POINT('Ctrl Pts',(0.000518963516653217,55.0110634971179,
-1.50364543832878));
#49010=CARTESIAN_POINT('Ctrl Pts',(1.2634838400664,54.9316888049038,-0.815219672159533));
#49011=CARTESIAN_POINT('Ctrl Pts',(1.37022795544771,54.8523141126896,0.619235929149326));
#49012=CARTESIAN_POINT('Ctrl Pts',(0.223058882480454,54.7729394204754,1.48701524229669));
#49013=CARTESIAN_POINT('Ctrl Pts',(-1.12823202116588,54.6935647282612,0.994014980507249));
#49014=CARTESIAN_POINT('Ctrl Pts',(-1.44706689157843,54.614190036047,-0.408620578361293));
#49015=CARTESIAN_POINT('Ctrl Pts',(-0.441675324154704,54.5348153438328,
-1.43732225685171));
#49016=CARTESIAN_POINT('Ctrl Pts',(0.967897716715009,54.4554406516187,-1.15071582195045));
#49017=CARTESIAN_POINT('Ctrl Pts',(1.49173757643851,54.3760659594045,0.188922901971819));
#49018=CARTESIAN_POINT('Ctrl Pts',(0.650472766495819,54.2966912671903,1.3556761857263));
#49019=CARTESIAN_POINT('Ctrl Pts',(-0.786046426050945,54.2173165749761,
1.2818361170921));
#49020=CARTESIAN_POINT('Ctrl Pts',(-1.50324635200296,54.1379418827619,0.0349744188024213));
#49021=CARTESIAN_POINT('Ctrl Pts',(-0.844809857600208,54.0585671905478,
-1.24389271869101));
#49022=CARTESIAN_POINT('Ctrl Pts',(0.586720943427397,53.9791924983336,-1.38446066605414));
#49023=CARTESIAN_POINT('Ctrl Pts',(1.48133729268241,53.8998178061194,-0.258094216376765));
#49024=CARTESIAN_POINT('Ctrl Pts',(1.02036643681545,53.8204431139052,1.10445694001623));
#49025=CARTESIAN_POINT('Ctrl Pts',(-0.374352385393229,53.741068421691,1.4563080342578));
#49026=CARTESIAN_POINT('Ctrl Pts',(-1.42649743618979,53.6616937294769,0.47547645921754));
#49027=CARTESIAN_POINT('Ctrl Pts',(-1.17323980728636,53.5823190372627,-0.940468581704944));
#49028=CARTESIAN_POINT('Ctrl Pts',(0.153661803903112,53.5029443450485,-1.49578101631727));
#49029=CARTESIAN_POINT('Ctrl Pts',(1.33994589596871,53.4235696528344,-0.682288644615303));
#49030=CARTESIAN_POINT('Ctrl Pts',(1.3000315254765,53.3441949606201,0.75557318073647));
#49031=CARTESIAN_POINT('Ctrl Pts',(0.0704447491227194,53.264820268406,1.50200210919453));
#49032=CARTESIAN_POINT('Ctrl Pts',(-1.22360675176528,53.1854455761918,0.873933244435241));
#49033=CARTESIAN_POINT('Ctrl Pts',(-1.39792295417167,53.1060708839776,-0.553881045797489));
#49034=CARTESIAN_POINT('Ctrl Pts',(-0.292985283484647,53.0266961917634,
-1.47483301507595));
#49035=CARTESIAN_POINT('Ctrl Pts',(1.08006627541054,52.9473214995492,-1.04614991249642));
#49036=CARTESIAN_POINT('Ctrl Pts',(1.46473792259796,52.8679468073351,0.339875884402707));
#49037=CARTESIAN_POINT('Ctrl Pts',(0.509012622328653,52.7885721151209,1.41487771521272));
#49038=CARTESIAN_POINT('Ctrl Pts',(-0.912515436687621,52.7091974229067,
1.19511019429316));
#49039=CARTESIAN_POINT('Ctrl Pts',(-1.4989911037539,52.6298227306925,-0.118315128197754));
#49040=CARTESIAN_POINT('Ctrl Pts',(-0.713724380092507,52.5504480384784,
-1.32346904306683));
#49041=CARTESIAN_POINT('Ctrl Pts',(0.72467896661141,52.4710733462642,-1.31750263531229));
#49042=CARTESIAN_POINT('Ctrl Pts',(1.49992103390936,52.39169865405,-0.105875826878788));
#49043=CARTESIAN_POINT('Ctrl Pts',(0.902569721711059,52.3123239618358,1.20263905480605));
#49044=CARTESIAN_POINT('Ctrl Pts',(-0.520732554977762,52.2329492696216,
1.41060639617868));
#49045=CARTESIAN_POINT('Ctrl Pts',(-1.46750704027315,52.1535745774075,0.327713114360973));
#49046=CARTESIAN_POINT('Ctrl Pts',(-1.0713505297735,52.0741998851933,-1.05507385574668));
#49047=CARTESIAN_POINT('Ctrl Pts',(0.305210022954444,51.9948251929791,-1.47235173820035));
#49048=CARTESIAN_POINT('Ctrl Pts',(1.40246970042868,51.9154505007649,-0.542265190759049));
#49049=CARTESIAN_POINT('Ctrl Pts',(1.21631473082964,51.8360758085508,0.884053886810973));
#49050=CARTESIAN_POINT('Ctrl Pts',(-0.0829025346852592,51.7567011163365,
1.50136603499951));
#49051=CARTESIAN_POINT('Ctrl Pts',(-1.30625482258257,51.6773264241224,0.744762465213426));
#49052=CARTESIAN_POINT('Ctrl Pts',(-1.33423970761725,51.5979517319082,-0.693380997286618));
#49053=CARTESIAN_POINT('Ctrl Pts',(-0.141247908656813,51.518577039694,-1.49700428966964));
#49054=CARTESIAN_POINT('Ctrl Pts',(1.18100129712657,51.4392023474798,-0.93070332366629));
#49055=CARTESIAN_POINT('Ctrl Pts',(1.42250395396948,51.3598276552657,0.487293916224389));
#49056=CARTESIAN_POINT('Ctrl Pts',(0.36225830298583,51.2804529630515,1.45936349646929));
#49057=CARTESIAN_POINT('Ctrl Pts',(-1.02949349155242,51.2010782708373,1.09595415636771));
#49058=CARTESIAN_POINT('Ctrl Pts',(-1.47914546322335,51.1217035786231,-0.270373934373359));
#49059=CARTESIAN_POINT('Ctrl Pts',(-0.575215197442902,51.042328886409,-1.38928065979757));
#49060=CARTESIAN_POINT('Ctrl Pts',(0.855098923927749,50.9629541941947,-1.23684090576505));
#49061=CARTESIAN_POINT('Ctrl Pts',(1.50290618670359,50.8835795019806,0.0474423840872669));
#49062=CARTESIAN_POINT('Ctrl Pts',(0.775382268430225,50.8042048097663,1.28831551484441));
#49063=CARTESIAN_POINT('Ctrl Pts',(-0.66169015229881,50.7248301175523,1.35022813475386));
#49064=CARTESIAN_POINT('Ctrl Pts',(-1.49326638260898,50.645455425338,0.176551663085664));
#49065=CARTESIAN_POINT('Ctrl Pts',(-0.958293075038441,50.5660807331238,
-1.15872591454633));
#49066=CARTESIAN_POINT('Ctrl Pts',(0.453534064315373,50.4867060409097,-1.43356896754687));
#49067=CARTESIAN_POINT('Ctrl Pts',(1.4505045351907,50.4073313486955,-0.39668023770827));
#49068=CARTESIAN_POINT('Ctrl Pts',(1.1197553097733,50.3279566564813,1.00349396081402));
#49069=CARTESIAN_POINT('Ctrl Pts',(-0.235009869266641,50.2485819642671,
1.48481098258362));
#49070=CARTESIAN_POINT('Ctrl Pts',(-1.3760640928247,50.169207272053,0.60845112765352));
#49071=CARTESIAN_POINT('Ctrl Pts',(-1.2551421938249,50.0898260779548,-0.827076980567057));
#49072=CARTESIAN_POINT('Ctrl Pts',(-0.41265429172088,50.0369031145949,-1.27565375796722));
#49073=CARTESIAN_POINT('Ctrl Pts',(0.0104297776558427,50.0104383819729,
-1.27217695389282));
#49074=CARTESIAN_POINT('Ctrl Pts',(-0.592987108432538,55.6696680384294,
1.23369893938847));
#49075=CARTESIAN_POINT('Ctrl Pts',(-1.00317218425256,55.6432098076914,1.03654025320749));
#49076=CARTESIAN_POINT('Ctrl Pts',(-1.60427168954347,55.5902933462152,0.204136280816067));
#49077=CARTESIAN_POINT('Ctrl Pts',(-1.04097069906526,55.5109186540011,-1.23973566239017));
#49078=CARTESIAN_POINT('Ctrl Pts',(0.476490289886929,55.4315439617868,-1.54565176705905));
#49079=CARTESIAN_POINT('Ctrl Pts',(1.55712294269118,55.3521692695727,-0.43881708180882));
#49080=CARTESIAN_POINT('Ctrl Pts',(1.21321639837339,55.2727945773585,1.07043838080641));
#49081=CARTESIAN_POINT('Ctrl Pts',(-0.241120853124227,55.1934198851444,
1.59968994933341));
#49082=CARTESIAN_POINT('Ctrl Pts',(-1.4747021787416,55.1140451929302,0.665269759981073));
#49083=CARTESIAN_POINT('Ctrl Pts',(-1.35882096708512,55.034670500716,-0.878058335153355));
#49084=CARTESIAN_POINT('Ctrl Pts',(0.000558365490677323,54.9552958085018,
-1.61780875927963));
#49085=CARTESIAN_POINT('Ctrl Pts',(1.35941304483292,54.8759211162877,-0.877114705859523));
#49086=CARTESIAN_POINT('Ctrl Pts',(1.47426163909818,54.7965464240734,0.666251022150459));
#49087=CARTESIAN_POINT('Ctrl Pts',(0.239994485876334,54.7171717318593,1.59991592621975));
#49088=CARTESIAN_POINT('Ctrl Pts',(-1.21389231783962,54.637797039645,1.06948493396631));
#49089=CARTESIAN_POINT('Ctrl Pts',(-1.55693452245038,54.558422347431,-0.4396448351744));
#49090=CARTESIAN_POINT('Ctrl Pts',(-0.475209241461426,54.4790476552166,
-1.5464500325467));
#49091=CARTESIAN_POINT('Ctrl Pts',(1.041384733577,54.3996729630026,-1.23808318685966));
#49092=CARTESIAN_POINT('Ctrl Pts',(1.6049968005696,54.3202982707883,0.203266752817891));
#49093=CARTESIAN_POINT('Ctrl Pts',(0.699859496451111,54.2409235785742,1.45860503554111));
#49094=CARTESIAN_POINT('Ctrl Pts',(-0.845726499645454,54.16154888636,1.3791587067876));
#49095=CARTESIAN_POINT('Ctrl Pts',(-1.61737937257903,54.0821741941458,0.0376298292449642));
#49096=CARTESIAN_POINT('Ctrl Pts',(-0.908951507258555,54.0027995019317,
-1.3383344800614));
#49097=CARTESIAN_POINT('Ctrl Pts',(0.63126735687412,53.9234248097175,-1.48957495918046));
#49098=CARTESIAN_POINT('Ctrl Pts',(1.59380688190213,53.8440501175034,-0.277689855154838));
#49099=CARTESIAN_POINT('Ctrl Pts',(1.09783710778899,53.7646754252891,1.18831212881632));
#49100=CARTESIAN_POINT('Ctrl Pts',(-0.402774851509876,53.6853007330749,
1.56687729299412));
#49101=CARTESIAN_POINT('Ctrl Pts',(-1.53480334427959,53.6059260408607,0.511576706147138));
#49102=CARTESIAN_POINT('Ctrl Pts',(-1.26231729141747,53.5265513486466,-1.0118730589843));
#49103=CARTESIAN_POINT('Ctrl Pts',(0.165328478366184,53.4471766564323,-1.60934723604244));
#49104=CARTESIAN_POINT('Ctrl Pts',(1.44168043356572,53.3678019642183,-0.734090974826148));
#49105=CARTESIAN_POINT('Ctrl Pts',(1.3987355899494,53.288427272004,0.812939592614877));
#49106=CARTESIAN_POINT('Ctrl Pts',(0.075793221773523,53.2090525797899,1.61604066142889));
#49107=CARTESIAN_POINT('Ctrl Pts',(-1.31650831403428,53.1296778875756,0.94028606866551));
#49108=CARTESIAN_POINT('Ctrl Pts',(-1.50405936293771,53.0503031953615,-0.595934110960401));
#49109=CARTESIAN_POINT('Ctrl Pts',(-0.315230004281003,52.9709285031473,
-1.58680877116654));
#49110=CARTESIAN_POINT('Ctrl Pts',(1.16206961855566,52.8915538109331,-1.12557817741755));
#49111=CARTESIAN_POINT('Ctrl Pts',(1.57594721523033,52.8121791187189,0.365680744169135));
#49112=CARTESIAN_POINT('Ctrl Pts',(0.547659081054675,52.7328044265048,1.52230140339784));
#49113=CARTESIAN_POINT('Ctrl Pts',(-0.981797589258738,52.6534297342906,
1.28584817360984));
#49114=CARTESIAN_POINT('Ctrl Pts',(-1.61280104732045,52.5740550420764,-0.127298128850341));
#49115=CARTESIAN_POINT('Ctrl Pts',(-0.767913448471228,52.4946803498622,
-1.42395258611544));
#49116=CARTESIAN_POINT('Ctrl Pts',(0.779699754985248,52.4153056576481,-1.41753318265721));
#49117=CARTESIAN_POINT('Ctrl Pts',(1.61380158182991,52.3359309654339,-0.113914381511949));
#49118=CARTESIAN_POINT('Ctrl Pts',(0.971096752215498,52.2565562732197,1.29394865805562));
#49119=CARTESIAN_POINT('Ctrl Pts',(-0.560268842115734,52.1771815810055,
1.51770578719019));
#49120=CARTESIAN_POINT('Ctrl Pts',(-1.57892657639899,52.0978068887914,0.352594523568839));
#49121=CARTESIAN_POINT('Ctrl Pts',(-1.15269213548962,52.0184321965771,-1.1351796653678));
#49122=CARTESIAN_POINT('Ctrl Pts',(0.328382899298671,51.939057504363,-1.58413910492659));
#49123=CARTESIAN_POINT('Ctrl Pts',(1.50895131800458,51.8596828121488,-0.583436329536225));
#49124=CARTESIAN_POINT('Ctrl Pts',(1.30866265105961,51.7803081199346,0.951175114359142));
#49125=CARTESIAN_POINT('Ctrl Pts',(-0.0891968567598987,51.7009334277205,
1.61535629370628));
#49126=CARTESIAN_POINT('Ctrl Pts',(-1.40543138691931,51.6215587355062,0.801308080410322));
#49127=CARTESIAN_POINT('Ctrl Pts',(-1.43554100650283,51.5421840432921,-0.746025507299841));
#49128=CARTESIAN_POINT('Ctrl Pts',(-0.151972066040321,51.4628093510779,
-1.61066338564395));
#49129=CARTESIAN_POINT('Ctrl Pts',(1.27066806742387,51.3834346588637,-1.00136637995689));
#49130=CARTESIAN_POINT('Ctrl Pts',(1.53050665946856,51.3040599666495,0.5242913960406));
#49131=CARTESIAN_POINT('Ctrl Pts',(0.389762533608743,51.2246852744354,1.57016473922538));
#49132=CARTESIAN_POINT('Ctrl Pts',(-1.10765712833604,51.1453105822212,1.17916377674197));
#49133=CARTESIAN_POINT('Ctrl Pts',(-1.59144863918925,51.065935890007,-0.290901902908883));
#49134=CARTESIAN_POINT('Ctrl Pts',(-0.618888044463587,50.9865611977928,
-1.49476090787491));
#49135=CARTESIAN_POINT('Ctrl Pts',(0.92002176438512,50.9071865055787,-1.33074726273637));
#49136=CARTESIAN_POINT('Ctrl Pts',(1.61701338044625,50.8278118133645,0.0510444168425675));
#49137=CARTESIAN_POINT('Ctrl Pts',(0.834252672658487,50.7484371211503,1.38613004868199));
#49138=CARTESIAN_POINT('Ctrl Pts',(-0.711928555117263,50.6690624289361,
1.45274334477311));
#49139=CARTESIAN_POINT('Ctrl Pts',(-1.60664168037358,50.589687736722,0.189956235509111));
#49140=CARTESIAN_POINT('Ctrl Pts',(-1.03105086560653,50.5103130445077,-1.24670144062743));
#49141=CARTESIAN_POINT('Ctrl Pts',(0.487968348905836,50.4309383522937,-1.54241177714507));
#49142=CARTESIAN_POINT('Ctrl Pts',(1.56063316696155,50.3515636600793,-0.426797931772294));
#49143=CARTESIAN_POINT('Ctrl Pts',(1.20477201754063,50.2721889678652,1.07968359980762));
#49144=CARTESIAN_POINT('Ctrl Pts',(-0.252852843712473,50.192814275651,1.59754430949374));
#49145=CARTESIAN_POINT('Ctrl Pts',(-1.48054088148351,50.1134395834369,0.654647391479134));
#49146=CARTESIAN_POINT('Ctrl Pts',(-1.35043806442046,50.0340583893389,-0.889872272845844));
#49147=CARTESIAN_POINT('Ctrl Pts',(-0.443984805648313,49.9811354259788,
-1.37250695598898));
#49148=CARTESIAN_POINT('Ctrl Pts',(0.011221651872736,49.9546706933568,-1.36876617778256));
#49149=CARTESIAN_POINT('Ctrl Pts',(-0.634832213542385,55.6139003498134,
1.32075692270464));
#49150=CARTESIAN_POINT('Ctrl Pts',(-1.07396267007658,55.5874421190754,1.10968541138929));
#49151=CARTESIAN_POINT('Ctrl Pts',(-1.71747974502912,55.5345256575993,0.218541491327414));
#49152=CARTESIAN_POINT('Ctrl Pts',(-1.11442849890479,55.455150965385,-1.32721963693774));
#49153=CARTESIAN_POINT('Ctrl Pts',(0.510114606470883,55.3757762731709,-1.65472321184439));
#49154=CARTESIAN_POINT('Ctrl Pts',(1.66700386974557,55.2964015809567,-0.469782926851943));
#49155=CARTESIAN_POINT('Ctrl Pts',(1.29882899768456,55.2170268887425,1.14597561580105));
#49156=CARTESIAN_POINT('Ctrl Pts',(-0.258135940467066,55.1376521965284,
1.71257468682791));
#49157=CARTESIAN_POINT('Ctrl Pts',(-1.57876694979249,55.0582775043141,0.712215608612426));
#49158=CARTESIAN_POINT('Ctrl Pts',(-1.45470839091706,54.9789028121001,-0.940019957597718));
#49159=CARTESIAN_POINT('Ctrl Pts',(0.000597767464702774,54.8995281198857,
-1.73197208023047));
#49160=CARTESIAN_POINT('Ctrl Pts',(1.45534224959945,54.8201534276717,-0.939009739559512));
#49161=CARTESIAN_POINT('Ctrl Pts',(1.57829532274867,54.7407787354574,0.713266115151591));
#49162=CARTESIAN_POINT('Ctrl Pts',(0.256930089272216,54.6614040432433,1.71281661014281));
#49163=CARTESIAN_POINT('Ctrl Pts',(-1.29955261451337,54.582029351029,1.14495488742536));
#49164=CARTESIAN_POINT('Ctrl Pts',(-1.66680215332233,54.5026546588149,-0.470669091987506));
#49165=CARTESIAN_POINT('Ctrl Pts',(-0.50874315876815,54.4232799666007,-1.65557780824169));
#49166=CARTESIAN_POINT('Ctrl Pts',(1.11487175043898,54.3439052743866,-1.32545055176888));
#49167=CARTESIAN_POINT('Ctrl Pts',(1.7182560247007,54.2645305821723,0.217610603663962));
#49168=CARTESIAN_POINT('Ctrl Pts',(0.749246226406404,54.1851558899582,1.56153388535592));
#49169=CARTESIAN_POINT('Ctrl Pts',(-0.90540657323996,54.105781197744,1.47648129648309));
#49170=CARTESIAN_POINT('Ctrl Pts',(-1.73151239315509,54.0264065055298,0.0402852396875059));
#49171=CARTESIAN_POINT('Ctrl Pts',(-0.973093156916901,53.9470318133156,
-1.4327762414318));
#49172=CARTESIAN_POINT('Ctrl Pts',(0.675813770320844,53.8676571211015,-1.59468925230679));
#49173=CARTESIAN_POINT('Ctrl Pts',(1.70627647112185,53.7882824288872,-0.297285493932909));
#49174=CARTESIAN_POINT('Ctrl Pts',(1.17530777876252,53.7089077366732,1.27216731761641));
#49175=CARTESIAN_POINT('Ctrl Pts',(-0.431197317626523,53.6295330444589,
1.67744655173045));
#49176=CARTESIAN_POINT('Ctrl Pts',(-1.64310925236939,53.5501583522448,0.547676953076732));
#49177=CARTESIAN_POINT('Ctrl Pts',(-1.35139477554857,53.4707836600306,-1.08327753626366));
#49178=CARTESIAN_POINT('Ctrl Pts',(0.176995152829257,53.3914089678163,-1.72291345576761));
#49179=CARTESIAN_POINT('Ctrl Pts',(1.54341497116274,53.3120342756023,-0.785893305036992));
#49180=CARTESIAN_POINT('Ctrl Pts',(1.4974396544223,53.2326595833879,0.870306004493283));
#49181=CARTESIAN_POINT('Ctrl Pts',(0.0811416944243273,53.1532848911739,
1.73007921366326));
#49182=CARTESIAN_POINT('Ctrl Pts',(-1.40940987630327,53.0739101989596,1.00663889289578));
#49183=CARTESIAN_POINT('Ctrl Pts',(-1.61019577170375,52.9945355067455,-0.637987176123315));
#49184=CARTESIAN_POINT('Ctrl Pts',(-0.337474725077362,52.9151608145313,
-1.69878452725711));
#49185=CARTESIAN_POINT('Ctrl Pts',(1.24407296170078,52.8357861223171,-1.20500644233868));
#49186=CARTESIAN_POINT('Ctrl Pts',(1.68715650786268,52.7564114301029,0.391485603935567));
#49187=CARTESIAN_POINT('Ctrl Pts',(0.586305539780697,52.6770367378888,1.62972509158297));
#49188=CARTESIAN_POINT('Ctrl Pts',(-1.05107974182985,52.5976620456745,1.37658615292654));
#49189=CARTESIAN_POINT('Ctrl Pts',(-1.72661099088702,52.5182873534605,-0.13628112950293));
#49190=CARTESIAN_POINT('Ctrl Pts',(-0.822102516849947,52.4389126612462,
-1.52443612916404));
#49191=CARTESIAN_POINT('Ctrl Pts',(0.834720543359083,52.3595379690321,-1.51756373000215));
#49192=CARTESIAN_POINT('Ctrl Pts',(1.72768212975045,52.2801632768178,-0.121952936145109));
#49193=CARTESIAN_POINT('Ctrl Pts',(1.03962378271994,52.2007885846037,1.3852582613052));
#49194=CARTESIAN_POINT('Ctrl Pts',(-0.599805129253705,52.1214138923895,
1.62480517820171));
#49195=CARTESIAN_POINT('Ctrl Pts',(-1.69034611252483,52.0420392001754,0.377475932776706));
#49196=CARTESIAN_POINT('Ctrl Pts',(-1.23403374120574,51.9626645079611,-1.21528547498893));
#49197=CARTESIAN_POINT('Ctrl Pts',(0.351555775642897,51.883289815747,-1.69592647165283));
#49198=CARTESIAN_POINT('Ctrl Pts',(1.61543293558047,51.8039151235328,-0.624607468313401));
#49199=CARTESIAN_POINT('Ctrl Pts',(1.40101057128958,51.7245404313186,1.01829634190731));
#49200=CARTESIAN_POINT('Ctrl Pts',(-0.0954911788345371,51.6451657391045,
1.72934655241303));
#49201=CARTESIAN_POINT('Ctrl Pts',(-1.50460795125606,51.5657910468902,0.857853695607218));
#49202=CARTESIAN_POINT('Ctrl Pts',(-1.53684230538839,51.4864163546762,-0.798670017313065));
#49203=CARTESIAN_POINT('Ctrl Pts',(-0.162696223423829,51.4070416624618,
-1.72432248161826));
#49204=CARTESIAN_POINT('Ctrl Pts',(1.36033483772117,51.3276669702478,-1.0720294362475));
#49205=CARTESIAN_POINT('Ctrl Pts',(1.63850936496764,51.2482922780335,0.561288875856811));
#49206=CARTESIAN_POINT('Ctrl Pts',(0.417266764231657,51.1689175858195,1.68096598198148));
#49207=CARTESIAN_POINT('Ctrl Pts',(-1.18582076511967,51.0895428936051,1.26237339711622));
#49208=CARTESIAN_POINT('Ctrl Pts',(-1.70375181515514,51.010168201391,-0.311429871444408));
#49209=CARTESIAN_POINT('Ctrl Pts',(-0.662560891484271,50.9307935091768,
-1.60024115595223));
#49210=CARTESIAN_POINT('Ctrl Pts',(0.98494460484249,50.8514188169627,-1.42465361970768));
#49211=CARTESIAN_POINT('Ctrl Pts',(1.73112057418891,50.7720441247485,0.054646449597867));
#49212=CARTESIAN_POINT('Ctrl Pts',(0.893123076886749,50.6926694325343,1.48394458251956));
#49213=CARTESIAN_POINT('Ctrl Pts',(-0.762166957935716,50.6132947403201,
1.55525855479236));
#49214=CARTESIAN_POINT('Ctrl Pts',(-1.72001697813816,50.5339200481059,0.203360807932558));
#49215=CARTESIAN_POINT('Ctrl Pts',(-1.10380865617462,50.4545453558917,-1.33467696670851));
#49216=CARTESIAN_POINT('Ctrl Pts',(0.5224026334963,50.3751706636775,-1.65125458674327));
#49217=CARTESIAN_POINT('Ctrl Pts',(1.67076179873239,50.2957959714634,-0.456915625836322));
#49218=CARTESIAN_POINT('Ctrl Pts',(1.28978872530794,50.2164212792492,1.15587323880121));
#49219=CARTESIAN_POINT('Ctrl Pts',(-0.270695818158305,50.137046587035,1.71027763640386));
#49220=CARTESIAN_POINT('Ctrl Pts',(-1.58501767014233,50.0576718948208,0.700843655304749));
#49221=CARTESIAN_POINT('Ctrl Pts',(-1.44573393501602,49.9782907007227,-0.952667565124631));
#49222=CARTESIAN_POINT('Ctrl Pts',(-0.475315319575745,49.9253677373627,
-1.46936015401072));
#49223=CARTESIAN_POINT('Ctrl Pts',(0.0120135260896293,49.8989030047408,
-1.4653554016723));
#49224=CARTESIAN_POINT('Ctrl Pts',(-1.28852825769066,50.065,0.693921594369763));
#49225=CARTESIAN_POINT('Ctrl Pts',(-1.29259187868739,50.065,0.686211757365716));
#49226=CARTESIAN_POINT('Ctrl Pts',(-1.29665549968411,50.065,0.67850192036167));
#49227=CARTESIAN_POINT('Ctrl Pts',(-1.30071912068084,50.065,0.670792083357623));
#49228=CARTESIAN_POINT('Ctrl Pts',(-0.686166456961371,55.615,-0.959540123316451));
#49229=CARTESIAN_POINT('Ctrl Pts',(-0.713413796911466,55.615,-0.944727431681135));
#49230=CARTESIAN_POINT('Ctrl Pts',(-0.739980968402287,55.615,-0.928802159412089));
#49231=CARTESIAN_POINT('Ctrl Pts',(-0.765790962793899,55.615,-0.911780060719286));
#49232=CARTESIAN_POINT('Ctrl Pts',(-0.806300133279505,55.615,-0.885063623376951));
#49233=CARTESIAN_POINT('Ctrl Pts',(-0.844945527882661,55.615,-0.85564803640011));
#49234=CARTESIAN_POINT('Ctrl Pts',(-0.881654237249992,55.615,-0.823835334333387));
#49235=CARTESIAN_POINT('Ctrl Pts',(-0.897239265429731,55.615,-0.810328952149743));
#49236=CARTESIAN_POINT('Ctrl Pts',(-0.91247497671016,55.615,-0.7963898664341));
#49237=CARTESIAN_POINT('Ctrl Pts',(-0.927354620595185,55.615,-0.782038646482574));
#49238=CARTESIAN_POINT('Ctrl Pts',(-0.937468429879662,55.615,-0.772284011041641));
#49239=CARTESIAN_POINT('Ctrl Pts',(-0.947419424992027,55.615,-0.762336894601238));
#49240=CARTESIAN_POINT('Ctrl Pts',(-0.957188717566935,55.615,-0.752221373165328));
#49241=CARTESIAN_POINT('Ctrl Pts',(-0.992370133259333,55.615,-0.715793109618777));
#49242=CARTESIAN_POINT('Ctrl Pts',(-1.02524473489684,55.615,-0.677140392748355));
#49243=CARTESIAN_POINT('Ctrl Pts',(-1.05573220817217,55.615,-0.636588252605784));
#49244=CARTESIAN_POINT('Ctrl Pts',(-1.07725611353962,55.615,-0.607958775213741));
#49245=CARTESIAN_POINT('Ctrl Pts',(-1.09758983810779,55.615,-0.578381398104754));
#49246=CARTESIAN_POINT('Ctrl Pts',(-1.11669696564595,55.615,-0.547957266410611));
#49247=CARTESIAN_POINT('Ctrl Pts',(-1.12351935004655,55.615,-0.537094036390431));
#49248=CARTESIAN_POINT('Ctrl Pts',(-1.13018528144804,55.615,-0.526122764219766));
#49249=CARTESIAN_POINT('Ctrl Pts',(-1.13669284706255,55.615,-0.515047781095408));
#49250=CARTESIAN_POINT('Ctrl Pts',(-1.14143068161862,55.615,-0.506984637231359));
#49251=CARTESIAN_POINT('Ctrl Pts',(-1.14608376236126,55.615,-0.49886775743124));
#49252=CARTESIAN_POINT('Ctrl Pts',(-1.15064685006719,55.615,-0.490707349154656));
#49253=CARTESIAN_POINT('Ctrl Pts',(-1.1763516666904,55.615,-0.444738081886885));
#49254=CARTESIAN_POINT('Ctrl Pts',(-1.19924569348006,55.615,-0.397319323655606));
#49255=CARTESIAN_POINT('Ctrl Pts',(-1.21924407138793,55.615,-0.348783334871917));
#49256=CARTESIAN_POINT('Ctrl Pts',(-1.23956435361566,55.615,-0.299466085501526));
#49257=CARTESIAN_POINT('Ctrl Pts',(-1.25689577956724,55.615,-0.24899444005167));
#49258=CARTESIAN_POINT('Ctrl Pts',(-1.27111323015662,55.615,-0.197677848868708));
#49259=CARTESIAN_POINT('Ctrl Pts',(-1.27928931799279,55.615,-0.168167005533828));
#49260=CARTESIAN_POINT('Ctrl Pts',(-1.28643485880816,55.615,-0.13837608268905));
#49261=CARTESIAN_POINT('Ctrl Pts',(-1.29251925576579,55.615,-0.108360072500537));
#49262=CARTESIAN_POINT('Ctrl Pts',(-1.29623123190128,55.615,-0.0900478692898342));
#49263=CARTESIAN_POINT('Ctrl Pts',(-1.29954814897365,55.615,-0.0716518423879908));
#49264=CARTESIAN_POINT('Ctrl Pts',(-1.30246201461502,55.615,-0.0531841690282108));
#49265=CARTESIAN_POINT('Ctrl Pts',(-1.30398684891677,55.615,-0.0435199822473792));
#49266=CARTESIAN_POINT('Ctrl Pts',(-1.30540118376147,55.615,-0.033836160950599));
#49267=CARTESIAN_POINT('Ctrl Pts',(-1.30670217233378,55.615,-0.0241489422268533));
#49268=CARTESIAN_POINT('Ctrl Pts',(-1.31399697767701,55.615,0.0301685025311241));
#49269=CARTESIAN_POINT('Ctrl Pts',(-1.31775021860916,55.615,0.084702533890493));
#49270=CARTESIAN_POINT('Ctrl Pts',(-1.31784722812879,55.615,0.139123948194586));
#49271=CARTESIAN_POINT('Ctrl Pts',(-1.31786333897964,55.615,0.148161981701328));
#49272=CARTESIAN_POINT('Ctrl Pts',(-1.3177785083462,55.615,0.157196969940163));
#49273=CARTESIAN_POINT('Ctrl Pts',(-1.31759208781496,55.615,0.166227470352783));
#49274=CARTESIAN_POINT('Ctrl Pts',(-1.31649771872793,55.615,0.219240410644158));
#49275=CARTESIAN_POINT('Ctrl Pts',(-1.31190679820835,55.615,0.272097989836632));
#49276=CARTESIAN_POINT('Ctrl Pts',(-1.30402779002026,55.615,0.324575174779585));
#49277=CARTESIAN_POINT('Ctrl Pts',(-1.29759318812667,55.615,0.36743206558918));
#49278=CARTESIAN_POINT('Ctrl Pts',(-1.28896443766674,55.615,0.41003571745502));
#49279=CARTESIAN_POINT('Ctrl Pts',(-1.27822940812215,55.615,0.452264473592666));
#49280=CARTESIAN_POINT('Ctrl Pts',(-1.27568035532626,55.615,0.46229177053234));
#49281=CARTESIAN_POINT('Ctrl Pts',(-1.27301185909614,55.615,0.472299687376204));
#49282=CARTESIAN_POINT('Ctrl Pts',(-1.27022983206114,55.615,0.482269961965456));
#49283=CARTESIAN_POINT('Ctrl Pts',(-1.2555747222539,55.615,0.534791187343801));
#49284=CARTESIAN_POINT('Ctrl Pts',(-1.23775012514738,55.615,0.586364505451297));
#49285=CARTESIAN_POINT('Ctrl Pts',(-1.21699228297199,55.615,0.63675759876728));
#49286=CARTESIAN_POINT('Ctrl Pts',(-1.19563053272573,55.615,0.688616778756082));
#49287=CARTESIAN_POINT('Ctrl Pts',(-1.17116222891849,55.615,0.739227014421633));
#49288=CARTESIAN_POINT('Ctrl Pts',(-1.14378967960996,55.615,0.78833572555278));
#49289=CARTESIAN_POINT('Ctrl Pts',(-1.12831450200091,55.615,0.816099527102268));
#49290=CARTESIAN_POINT('Ctrl Pts',(-1.11191007542324,55.615,0.843383335748853));
#49291=CARTESIAN_POINT('Ctrl Pts',(-1.09460583269318,55.615,0.87013975692643));
#49292=CARTESIAN_POINT('Ctrl Pts',(-1.08385338689301,55.615,0.886765562112273));
#49293=CARTESIAN_POINT('Ctrl Pts',(-1.07275341592303,55.615,0.903187706241318));
#49294=CARTESIAN_POINT('Ctrl Pts',(-1.06131206243182,55.615,0.919394377481652));
#49295=CARTESIAN_POINT('Ctrl Pts',(-1.05554179996197,55.615,0.927567951254296));
#49296=CARTESIAN_POINT('Ctrl Pts',(-1.04968469512178,55.615,0.935686712806367));
#49297=CARTESIAN_POINT('Ctrl Pts',(-1.04374147146349,55.615,0.943749105818433));
#49298=CARTESIAN_POINT('Ctrl Pts',(-1.03744933002585,55.615,0.952284829875686));
#49299=CARTESIAN_POINT('Ctrl Pts',(-1.03106633620261,55.615,0.960749633607578));
#49300=CARTESIAN_POINT('Ctrl Pts',(-1.02459591553728,55.615,0.969139382618596));
#49301=CARTESIAN_POINT('Ctrl Pts',(-0.989018945593423,55.615,1.01526959019551));
#49302=CARTESIAN_POINT('Ctrl Pts',(-0.950784323740741,55.615,1.05915700560731));
#49303=CARTESIAN_POINT('Ctrl Pts',(-0.910112926818086,55.615,1.10054016857051));
#49304=CARTESIAN_POINT('Ctrl Pts',(-0.868873824614699,55.615,1.14250097188848));
#49305=CARTESIAN_POINT('Ctrl Pts',(-0.825129032595075,55.615,1.18188829248971));
#49306=CARTESIAN_POINT('Ctrl Pts',(-0.779058684490665,55.615,1.21840862870409));
#49307=CARTESIAN_POINT('Ctrl Pts',(-0.732988336386267,55.615,1.25492896491846));
#49308=CARTESIAN_POINT('Ctrl Pts',(-0.684591886750651,55.615,1.28858350433891));
#49309=CARTESIAN_POINT('Ctrl Pts',(-0.634007094575044,55.615,1.31904027763693));
#49310=CARTESIAN_POINT('Origin',(-3.28582941601228E-17,55.615,0.));
#49311=CARTESIAN_POINT('',(0.658022064252088,55.615,1.30722576969605));
#49312=CARTESIAN_POINT('',(-1.79227059055215E-16,55.615,-1.4635));
#49313=CARTESIAN_POINT('Origin',(0.,55.615,0.));
#49314=CARTESIAN_POINT('Ctrl Pts',(0.658022064252089,55.6150000000001,1.30722576969605));
#49315=CARTESIAN_POINT('Ctrl Pts',(0.68291041760411,55.6150000000001,1.29174709945824));
#49316=CARTESIAN_POINT('Ctrl Pts',(0.70727048796654,55.6150000000001,1.27548020477116));
#49317=CARTESIAN_POINT('Ctrl Pts',(0.731059524014722,55.6150000000001,1.25842242479073));
#49318=CARTESIAN_POINT('Ctrl Pts',(0.778314131695388,55.6150000000001,1.22453880297244));
#49319=CARTESIAN_POINT('Ctrl Pts',(0.823318307788889,55.6150000000001,1.18753622257729));
#49320=CARTESIAN_POINT('Ctrl Pts',(0.865917011406816,55.6150000000001,1.14773425046169));
#49321=CARTESIAN_POINT('Ctrl Pts',(0.888709815422025,55.6150000000001,1.12643786177376));
#49322=CARTESIAN_POINT('Ctrl Pts',(0.910813233033345,55.615,1.10433948889784));
#49323=CARTESIAN_POINT('Ctrl Pts',(0.932198075962424,55.615,1.08148531314));
#49324=CARTESIAN_POINT('Ctrl Pts',(0.941182403063221,55.615,1.07188368121272));
#49325=CARTESIAN_POINT('Ctrl Pts',(0.950034495504371,55.615,1.06215426440287));
#49326=CARTESIAN_POINT('Ctrl Pts',(0.958748320582393,55.615,1.05230580285939));
#49327=CARTESIAN_POINT('Ctrl Pts',(0.996890648209955,55.615,1.00919692203433));
#49328=CARTESIAN_POINT('Ctrl Pts',(1.03241482205307,55.615,0.963779887246079));
#49329=CARTESIAN_POINT('Ctrl Pts',(1.06516729256736,55.615,0.916365584833226));
#49330=CARTESIAN_POINT('Ctrl Pts',(1.08673802125298,55.615,0.885138595323546));
#49331=CARTESIAN_POINT('Ctrl Pts',(1.10710560412785,55.615,0.853044676706417));
#49332=CARTESIAN_POINT('Ctrl Pts',(1.1262143987642,55.615,0.820168902777738));
#49333=CARTESIAN_POINT('Ctrl Pts',(1.13494907220612,55.615,0.805141311823826));
#49334=CARTESIAN_POINT('Ctrl Pts',(1.143420596016,55.615,0.789950335051207));
#49335=CARTESIAN_POINT('Ctrl Pts',(1.15162295132403,55.615,0.7746040391249));
#49336=CARTESIAN_POINT('Ctrl Pts',(1.15676325047072,55.615,0.764986734229843));
#49337=CARTESIAN_POINT('Ctrl Pts',(1.161795159293,55.615,0.755313303870316));
#49338=CARTESIAN_POINT('Ctrl Pts',(1.16671416235182,55.615,0.74559275360192));
#49339=CARTESIAN_POINT('Ctrl Pts',(1.19208713322841,55.615,0.695452667101675));
#49340=CARTESIAN_POINT('Ctrl Pts',(1.21449001188561,55.615,0.64400430683225));
#49341=CARTESIAN_POINT('Ctrl Pts',(1.23377743082302,55.615,0.591534933891794));
#49342=CARTESIAN_POINT('Ctrl Pts',(1.25260516103681,55.615,0.540316095258442));
#49343=CARTESIAN_POINT('Ctrl Pts',(1.26846429964751,55.615,0.488123297443767));
#49344=CARTESIAN_POINT('Ctrl Pts',(1.28117110996631,55.615,0.435218704777426));
#49345=CARTESIAN_POINT('Ctrl Pts',(1.28851312999605,55.615,0.404650326933115));
#49346=CARTESIAN_POINT('Ctrl Pts',(1.29480181489721,55.615,0.373844300548893));
#49347=CARTESIAN_POINT('Ctrl Pts',(1.29999379066505,55.615,0.342852380337404));
#49348=CARTESIAN_POINT('Ctrl Pts',(1.30253195104456,55.615,0.327701603931069));
#49349=CARTESIAN_POINT('Ctrl Pts',(1.30480792213547,55.615,0.312506423403815));
#49350=CARTESIAN_POINT('Ctrl Pts',(1.30681610317096,55.615,0.29727304558529));
#49351=CARTESIAN_POINT('Ctrl Pts',(1.30817917115221,55.615,0.286933275821725));
#49352=CARTESIAN_POINT('Ctrl Pts',(1.30941904387809,55.615,0.276574159451665));
#49353=CARTESIAN_POINT('Ctrl Pts',(1.31053329015515,55.615,0.266203176480421));
#49354=CARTESIAN_POINT('Ctrl Pts',(1.31618011679077,55.615,0.213644649621809));
#49355=CARTESIAN_POINT('Ctrl Pts',(1.31858293691913,55.615,0.160993037389023));
#49356=CARTESIAN_POINT('Ctrl Pts',(1.31758756847756,55.615,0.108492899597445));
#49357=CARTESIAN_POINT('Ctrl Pts',(1.31729118832992,55.615,0.0928604986286303));
#49358=CARTESIAN_POINT('Ctrl Pts',(1.31669317679049,55.615,0.0772415590078096));
#49359=CARTESIAN_POINT('Ctrl Pts',(1.31578856736902,55.615,0.0616426741714474));
#49360=CARTESIAN_POINT('Ctrl Pts',(1.31260574726313,55.615,0.00675882805143094));
#49361=CARTESIAN_POINT('Ctrl Pts',(1.30563135996479,55.615,-0.0478787267712015));
#49362=CARTESIAN_POINT('Ctrl Pts',(1.29503867980794,55.615,-0.101964033927055));
#49363=CARTESIAN_POINT('Ctrl Pts',(1.29017588246939,55.615,-0.126793055836274));
#49364=CARTESIAN_POINT('Ctrl Pts',(1.28454982057433,55.615,-0.151505335923803));
#49365=CARTESIAN_POINT('Ctrl Pts',(1.2781739397107,55.615,-0.176068982586533));
#49366=CARTESIAN_POINT('Ctrl Pts',(1.27368851673344,55.615,-0.193349472530278));
#49367=CARTESIAN_POINT('Ctrl Pts',(1.26883195876927,55.615,-0.210556370160557));
#49368=CARTESIAN_POINT('Ctrl Pts',(1.26360842526702,55.615,-0.227678015327403));
#49369=CARTESIAN_POINT('Ctrl Pts',(1.26060788187359,55.615,-0.237513166048233));
#49370=CARTESIAN_POINT('Ctrl Pts',(1.25748861719013,55.615,-0.247312236830595));
#49371=CARTESIAN_POINT('Ctrl Pts',(1.25425381366423,55.615,-0.257067869314174));
#49372=CARTESIAN_POINT('Ctrl Pts',(1.23770844736276,55.615,-0.306965957915593));
#49373=CARTESIAN_POINT('Ctrl Pts',(1.21813026885531,55.615,-0.355775530682368));
#49374=CARTESIAN_POINT('Ctrl Pts',(1.19569149061526,55.615,-0.403236927123455));
#49375=CARTESIAN_POINT('Ctrl Pts',(1.17340656245797,55.615,-0.450372907461588));
#49376=CARTESIAN_POINT('Ctrl Pts',(1.1482993237225,55.615,-0.496180019253271));
#49377=CARTESIAN_POINT('Ctrl Pts',(1.12049946060564,55.615,-0.540371229951903));
#49378=CARTESIAN_POINT('Ctrl Pts',(1.10656068523074,55.615,-0.562528582197986));
#49379=CARTESIAN_POINT('Ctrl Pts',(1.09194444731789,55.615,-0.584279101420356));
#49380=CARTESIAN_POINT('Ctrl Pts',(1.07666430994254,55.615,-0.605582436250956));
#49381=CARTESIAN_POINT('Ctrl Pts',(1.0654084494325,55.615,-0.621275185560824));
#49382=CARTESIAN_POINT('Ctrl Pts',(1.05379230002795,55.615,-0.636725221388357));
#49383=CARTESIAN_POINT('Ctrl Pts',(1.04182078348874,55.615,-0.651915270109351));
#49384=CARTESIAN_POINT('Ctrl Pts',(1.0360343607354,55.615,-0.659257367767205));
#49385=CARTESIAN_POINT('Ctrl Pts',(1.03016546377772,55.615,-0.666537854073461));
#49386=CARTESIAN_POINT('Ctrl Pts',(1.02422302488534,55.615,-0.673745045559676));
#49387=CARTESIAN_POINT('Ctrl Pts',(0.992143122081392,55.615,-0.712652639992629));
#49388=CARTESIAN_POINT('Ctrl Pts',(0.9578608316653,55.615,-0.749506601960801));
#49389=CARTESIAN_POINT('Ctrl Pts',(0.921505700618096,55.615,-0.784054535932657));
#49390=CARTESIAN_POINT('Ctrl Pts',(0.885885294343576,55.615,-0.817904267967041));
#49391=CARTESIAN_POINT('Ctrl Pts',(0.848274239084723,55.615,-0.849540819064814));
#49392=CARTESIAN_POINT('Ctrl Pts',(0.808770632805465,55.615,-0.878683193575754));
#49393=CARTESIAN_POINT('Ctrl Pts',(0.769267026526212,55.615,-0.90782556808669));
#49394=CARTESIAN_POINT('Ctrl Pts',(0.727870244441854,55.615,-0.934474448336147));
#49395=CARTESIAN_POINT('Ctrl Pts',(0.684664424539371,55.615,-0.958295198918462));
#49396=CARTESIAN_POINT('Origin',(0.,55.615,0.));
#49397=CARTESIAN_POINT('Ctrl Pts',(0.851547439304115,55.7810496121231,-1.19249201555124));
#49398=CARTESIAN_POINT('Ctrl Pts',(1.24813648739576,55.7545848791926,-0.909303082791228));
#49399=CARTESIAN_POINT('Ctrl Pts',(1.72948988737955,55.7016619155239,0.0790533067026992));
#49400=CARTESIAN_POINT('Ctrl Pts',(0.870312231128513,55.6222807211175,1.49856009322968));
#49401=CARTESIAN_POINT('Ctrl Pts',(-0.786234575314587,55.5429060289032,
1.54266863466831));
#49402=CARTESIAN_POINT('Ctrl Pts',(-1.72276977183862,55.4635313366891,0.17699222243158));
#49403=CARTESIAN_POINT('Ctrl Pts',(-1.08304583280362,55.3841566444748,-1.35162590392847));
#49404=CARTESIAN_POINT('Ctrl Pts',(0.54791983081442,55.3047819522607,-1.64286170370572));
#49405=CARTESIAN_POINT('Ctrl Pts',(1.67740951839998,55.2254072600464,-0.43094974572187));
#49406=CARTESIAN_POINT('Ctrl Pts',(1.27191930029928,55.1460325678324,1.17545715863903));
#49407=CARTESIAN_POINT('Ctrl Pts',(-0.297535369309862,55.0666578756181,
1.70612562639131));
#49408=CARTESIAN_POINT('Ctrl Pts',(-1.59470324002085,54.987283183404,0.675534000334254));
#49409=CARTESIAN_POINT('Ctrl Pts',(-1.43254616815791,54.9079084911898,-0.97326276475906));
#49410=CARTESIAN_POINT('Ctrl Pts',(0.0405511939472471,54.8285337989756,
-1.73140800565394));
#49411=CARTESIAN_POINT('Ctrl Pts',(1.47653853778323,54.7491591067614,-0.905128112763759));
#49412=CARTESIAN_POINT('Ctrl Pts',(1.56133067791224,54.6697844145472,0.749446188461003));
#49413=CARTESIAN_POINT('Ctrl Pts',(0.217332522504072,54.590409722333,1.71819333027979));
#49414=CARTESIAN_POINT('Ctrl Pts',(-1.32554873260254,54.5110350301189,1.11460441681919));
#49415=CARTESIAN_POINT('Ctrl Pts',(-1.65540659994225,54.4316603379047,-0.508970916374371));
#49416=CARTESIAN_POINT('Ctrl Pts',(-0.470384583918035,54.3522856456905,
-1.66678150637739));
#49417=CARTESIAN_POINT('Ctrl Pts',(1.14509124923834,54.2729109534763,-1.29930303482708));
#49418=CARTESIAN_POINT('Ctrl Pts',(1.71268214966027,54.1935362612622,0.257181232075015));
#49419=CARTESIAN_POINT('Ctrl Pts',(0.712979749441727,54.114161569048,1.57831625179607));
#49420=CARTESIAN_POINT('Ctrl Pts',(-0.939177851791401,54.0347868768338,
1.45511762067378));
#49421=CARTESIAN_POINT('Ctrl Pts',(-1.73188400837484,53.9554121846196,0.000325675578953457));
#49422=CARTESIAN_POINT('Ctrl Pts',(-0.939725047858023,53.8760374924055,
-1.45476429602388));
#49423=CARTESIAN_POINT('Ctrl Pts',(0.712386103172446,53.7966628001912,-1.57858429118273));
#49424=CARTESIAN_POINT('Ctrl Pts',(1.71258530251459,53.7172881079772,-0.257825339110466));
#49425=CARTESIAN_POINT('Ctrl Pts',(1.1455798323574,53.6379134157629,1.29887226907537));
#49426=CARTESIAN_POINT('Ctrl Pts',(-0.46975768860566,53.5585387235487,1.66695831918764));
#49427=CARTESIAN_POINT('Ctrl Pts',(-1.6552150500525,53.4791640313345,0.509593428052268));
#49428=CARTESIAN_POINT('Ctrl Pts',(-1.32596785837452,53.3997893391204,-1.11410572315841));
#49429=CARTESIAN_POINT('Ctrl Pts',(0.216686347870187,53.3204146469062,-1.71827510908279));
#49430=CARTESIAN_POINT('Ctrl Pts',(1.56104861754719,53.241039954692,-0.75003302426545));
#49431=CARTESIAN_POINT('Ctrl Pts',(1.47687901847619,53.1616652624778,0.904572102498378));
#49432=CARTESIAN_POINT('Ctrl Pts',(0.0412020285017384,53.0822905702637,
1.73139386526713));
#49433=CARTESIAN_POINT('Ctrl Pts',(-1.43217936741558,53.0029158780494,0.97379904671594));
#49434=CARTESIAN_POINT('Ctrl Pts',(-1.5949584892478,52.9235411858353,-0.674929434394221));
#49435=CARTESIAN_POINT('Ctrl Pts',(-0.298174465124138,52.8441664936211,
-1.7060229518338));
#49436=CARTESIAN_POINT('Ctrl Pts',(1.27147212143958,52.7647918014069,-1.17591707540933));
#49437=CARTESIAN_POINT('Ctrl Pts',(1.67758131058698,52.6854171091927,0.430282779347293));
#49438=CARTESIAN_POINT('Ctrl Pts',(0.548518348371223,52.6060424169786,1.64272637567395));
#49439=CARTESIAN_POINT('Ctrl Pts',(-1.08249947446898,52.5266677247644,1.35189393504859));
#49440=CARTESIAN_POINT('Ctrl Pts',(-1.72291073975908,52.4472930325502,-0.176070743280815));
#49441=CARTESIAN_POINT('Ctrl Pts',(-0.78666842036735,52.367918340336,-1.54291124833255));
#49442=CARTESIAN_POINT('Ctrl Pts',(0.869462374029881,52.2885436481219,-1.49781758036796));
#49443=CARTESIAN_POINT('Ctrl Pts',(1.72993908299856,52.2091689559076,-0.082055425117027));
#49444=CARTESIAN_POINT('Ctrl Pts',(1.0073304972326,52.1297942636935,1.40879650525601));
#49445=CARTESIAN_POINT('Ctrl Pts',(-0.637096731444034,52.0504195714793,
1.61044406271855));
#49446=CARTESIAN_POINT('Ctrl Pts',(-1.69851009683004,51.9710448792651,0.338357464117524));
#49447=CARTESIAN_POINT('Ctrl Pts',(-1.2055991615173,51.8916701870509,-1.24336357767062));
#49448=CARTESIAN_POINT('Ctrl Pts',(0.390568141023166,51.8122954948368,-1.68726964487261));
#49449=CARTESIAN_POINT('Ctrl Pts',(1.62932246015966,51.7329208026226,-0.587137662407102));
#49450=CARTESIAN_POINT('Ctrl Pts',(1.37706681435153,51.6535461104084,1.05029011263948));
#49451=CARTESIAN_POINT('Ctrl Pts',(-0.135357051476193,51.5741714181942,
1.72658646294032));
#49452=CARTESIAN_POINT('Ctrl Pts',(-1.52391423268581,51.4947967259801,0.822865516477053));
#49453=CARTESIAN_POINT('Ctrl Pts',(-1.51792167730218,51.4154220337658,-0.833868206866928));
#49454=CARTESIAN_POINT('Ctrl Pts',(-0.122863029744826,51.3360473415517,
-1.72752051345823));
#49455=CARTESIAN_POINT('Ctrl Pts',(1.38462859005561,51.2566726493375,-1.04030063594932));
#49456=CARTESIAN_POINT('Ctrl Pts',(1.62503267349089,51.1772979571234,0.598908912336164));
#49457=CARTESIAN_POINT('Ctrl Pts',(0.378351379082027,51.0979232649091,1.69005123828274));
#49458=CARTESIAN_POINT('Ctrl Pts',(-1.21456118004716,51.018548572695,1.23460893456007));
#49459=CARTESIAN_POINT('Ctrl Pts',(-1.69602012104765,50.9391738804808,-0.350634684781572));
#49460=CARTESIAN_POINT('Ctrl Pts',(-0.62542553811471,50.8597991882666,-1.61501315957936));
#49461=CARTESIAN_POINT('Ctrl Pts',(1.01748710575982,50.7804244960525,-1.40146778009058));
#49462=CARTESIAN_POINT('Ctrl Pts',(1.72931688329718,50.7010498038382,0.0945587405418702));
#49463=CARTESIAN_POINT('Ctrl Pts',(0.858571433328937,50.6216751116241,1.50408625737625));
#49464=CARTESIAN_POINT('Ctrl Pts',(-0.797745172198436,50.5423004194099,
1.53714454711868));
#49465=CARTESIAN_POINT('Ctrl Pts',(-1.72426574129088,50.4629257271957,0.163671969299396));
#49466=CARTESIAN_POINT('Ctrl Pts',(-1.07244305206445,50.3835510349816,-1.35982639834679));
#49467=CARTESIAN_POINT('Ctrl Pts',(0.559899301331203,50.3041763427673,-1.63844563418453));
#49468=CARTESIAN_POINT('Ctrl Pts',(1.68161745751345,50.2248016505532,-0.418674646065943));
#49469=CARTESIAN_POINT('Ctrl Pts',(1.26094450061532,50.145426958339,1.18624560473938));
#49470=CARTESIAN_POINT('Ctrl Pts',(0.216585201145672,50.0925104968629,1.52892814110574));
#49471=CARTESIAN_POINT('Ctrl Pts',(-0.262716677134921,50.0660522661248,
1.44157906696032));
#49472=CARTESIAN_POINT('Ctrl Pts',(0.795430237244947,55.7252976988069,-1.11390647550743));
#49473=CARTESIAN_POINT('Ctrl Pts',(1.16588396190188,55.6988329658764,-0.849379768510902));
#49474=CARTESIAN_POINT('Ctrl Pts',(1.61551604518388,55.6459100022078,0.073843672828042));
#49475=CARTESIAN_POINT('Ctrl Pts',(0.812958424312154,55.5665288078012,1.39980458570529));
#49476=CARTESIAN_POINT('Ctrl Pts',(-0.734421508311664,55.487154115587,1.44100636256662));
#49477=CARTESIAN_POINT('Ctrl Pts',(-1.6092387870391,55.4077794233728,0.165328388039434));
#49478=CARTESIAN_POINT('Ctrl Pts',(-1.01167282522525,55.3284047311586,-1.26255339844229));
#49479=CARTESIAN_POINT('Ctrl Pts',(0.511811768669154,55.2490300389445,-1.53459668178578));
#49480=CARTESIAN_POINT('Ctrl Pts',(1.56686778633048,55.1696553467303,-0.402550043201726));
#49481=CARTESIAN_POINT('Ctrl Pts',(1.18809948112844,55.0902806545161,1.09799422018295));
#49482=CARTESIAN_POINT('Ctrl Pts',(-0.27792770957343,55.010905962302,1.59369149519038));
#49483=CARTESIAN_POINT('Ctrl Pts',(-1.48961187362816,54.9315312700877,0.631016130577541));
#49484=CARTESIAN_POINT('Ctrl Pts',(-1.33814099580097,54.8521565778736,-0.909124490476559));
#49485=CARTESIAN_POINT('Ctrl Pts',(0.0378788595129698,54.7727818856594,
-1.61730775895534));
#49486=CARTESIAN_POINT('Ctrl Pts',(1.37923425660231,54.6934071934452,-0.845479930115339));
#49487=CARTESIAN_POINT('Ctrl Pts',(1.45843857221207,54.614032501231,0.700057485907088));
#49488=CARTESIAN_POINT('Ctrl Pts',(0.203010251639913,54.5346578090168,1.60496393419256));
#49489=CARTESIAN_POINT('Ctrl Pts',(-1.23819471962175,54.4552831168027,1.04115169018566));
#49490=CARTESIAN_POINT('Ctrl Pts',(-1.54631486603372,54.3759084245884,-0.475429598018979));
#49491=CARTESIAN_POINT('Ctrl Pts',(-0.439386115103633,54.2965337323744,
-1.55694016311845));
#49492=CARTESIAN_POINT('Ctrl Pts',(1.06962943226405,54.2171590401601,-1.21367862028938));
#49493=CARTESIAN_POINT('Ctrl Pts',(1.59981594183729,54.137784347946,0.24023292068326));
#49494=CARTESIAN_POINT('Ctrl Pts',(0.665994194889158,54.0584096557318,1.47430479227282));
#49495=CARTESIAN_POINT('Ctrl Pts',(-0.877285782311934,53.9790349635176,
1.35922498361067));
#49496=CARTESIAN_POINT('Ctrl Pts',(-1.61775239297073,53.8996602713034,0.000304213471934397));
#49497=CARTESIAN_POINT('Ctrl Pts',(-0.877796918012653,53.8202855790893,
-1.35889494314889));
#49498=CARTESIAN_POINT('Ctrl Pts',(0.665439670066453,53.740910886875,-1.47455516779282));
#49499=CARTESIAN_POINT('Ctrl Pts',(1.5997254769442,53.661536194661,-0.240834580894265));
#49500=CARTESIAN_POINT('Ctrl Pts',(1.070085817626,53.5821615024466,1.21327624211495));
#49501=CARTESIAN_POINT('Ctrl Pts',(-0.438800532358591,53.5027868102325,
1.55710532391762));
#49502=CARTESIAN_POINT('Ctrl Pts',(-1.54613593933251,53.4234121180183,0.476011086012218));
#49503=CARTESIAN_POINT('Ctrl Pts',(-1.23858622489422,53.3440374258042,-1.04068586056936));
#49504=CARTESIAN_POINT('Ctrl Pts',(0.202406660085762,53.26466273359,-1.60504032375076));
#49505=CARTESIAN_POINT('Ctrl Pts',(1.45817509969987,53.1852880413758,-0.700605649076399));
#49506=CARTESIAN_POINT('Ctrl Pts',(1.37955229952733,53.1059133491616,0.844960561073897));
#49507=CARTESIAN_POINT('Ctrl Pts',(0.0384868038977224,53.0265386569474,
1.61729455042378));
#49508=CARTESIAN_POINT('Ctrl Pts',(-1.33779836732483,52.9471639647332,0.909625431310262));
#49509=CARTESIAN_POINT('Ctrl Pts',(-1.48985030186337,52.8677892725191,-0.630451405693282));
#49510=CARTESIAN_POINT('Ctrl Pts',(-0.278524688804058,52.7884145803049,
-1.59359558691344));
#49511=CARTESIAN_POINT('Ctrl Pts',(1.18768177147418,52.7090398880908,-1.09842382831613));
#49512=CARTESIAN_POINT('Ctrl Pts',(1.56702825736679,52.6296651958765,0.401927030088108));
#49513=CARTESIAN_POINT('Ctrl Pts',(0.512370843760241,52.5502905036624,1.53447027190719));
#49514=CARTESIAN_POINT('Ctrl Pts',(-1.01116247204977,52.4709158114481,1.26280376624051));
#49515=CARTESIAN_POINT('Ctrl Pts',(-1.60937046513623,52.391541119234,-0.164467634609069));
#49516=CARTESIAN_POINT('Ctrl Pts',(-0.734826762860395,52.3121664270198,
-1.44123298792605));
#49517=CARTESIAN_POINT('Ctrl Pts',(0.812164573021694,52.2327917348056,-1.39911100463804));
#49518=CARTESIAN_POINT('Ctrl Pts',(1.61593563869248,52.1534170425915,-0.0766479508427663));
#49519=CARTESIAN_POINT('Ctrl Pts',(0.940947150346172,52.0740423503773,1.31595644198213));
#49520=CARTESIAN_POINT('Ctrl Pts',(-0.595111887899797,51.9946676581631,
1.50431537193601));
#49521=CARTESIAN_POINT('Ctrl Pts',(-1.58657783104664,51.9152929659489,0.316059617508257));
#49522=CARTESIAN_POINT('Ctrl Pts',(-1.12614985707864,51.8359182737347,-1.16142558819327));
#49523=CARTESIAN_POINT('Ctrl Pts',(0.364829596960867,51.7565435815206,-1.5760781278539));
#49524=CARTESIAN_POINT('Ctrl Pts',(1.52194967797967,51.6771688893063,-0.548445134760282));
#49525=CARTESIAN_POINT('Ctrl Pts',(1.28631774612217,51.5977941970922,0.981075715705936));
#49526=CARTESIAN_POINT('Ctrl Pts',(-0.126436985890621,51.5184195048781,
1.61280395718511));
#49527=CARTESIAN_POINT('Ctrl Pts',(-1.42348788064797,51.4390448126638,0.768638460737906));
#49528=CARTESIAN_POINT('Ctrl Pts',(-1.41789023625319,51.3596701204497,-0.77891607091346));
#49529=CARTESIAN_POINT('Ctrl Pts',(-0.114766323504441,51.2802954282355,
-1.6136764535262));
#49530=CARTESIAN_POINT('Ctrl Pts',(1.29338119880216,51.2009207360213,-0.971744548178601));
#49531=CARTESIAN_POINT('Ctrl Pts',(1.51794258938992,51.1215460438071,0.559440656197589));
#49532=CARTESIAN_POINT('Ctrl Pts',(0.353417922871217,51.0421713515929,1.57867641352069));
#49533=CARTESIAN_POINT('Ctrl Pts',(-1.13452127621088,50.9627966593788,1.15324787838522));
#49534=CARTESIAN_POINT('Ctrl Pts',(-1.58425194532859,50.8834219671646,-0.327527766074945));
#49535=CARTESIAN_POINT('Ctrl Pts',(-0.584209829305774,50.8040472749504,
-1.50858336410208));
#49536=CARTESIAN_POINT('Ctrl Pts',(0.950434435678181,50.7246725827362,-1.30911068174848));
#49537=CARTESIAN_POINT('Ctrl Pts',(1.61535444211641,50.6452978905221,0.0883272944655598));
#49538=CARTESIAN_POINT('Ctrl Pts',(0.801991348200938,50.5659231983079,1.4049665741692));
#49539=CARTESIAN_POINT('Ctrl Pts',(-0.745173553808545,50.4865485060937,
1.43584631385136));
#49540=CARTESIAN_POINT('Ctrl Pts',(-1.61063617170777,50.4071738138795,0.152885943120856));
#49541=CARTESIAN_POINT('Ctrl Pts',(-1.00176877054839,50.3277991216654,-1.27021347810388));
#49542=CARTESIAN_POINT('Ctrl Pts',(0.523001788902224,50.2484244294511,-1.53047163241706));
#49543=CARTESIAN_POINT('Ctrl Pts',(1.57079842114053,50.169049737237,-0.391083875868172));
#49544=CARTESIAN_POINT('Ctrl Pts',(1.1778479236539,50.0896750450228,1.10807170482447));
#49545=CARTESIAN_POINT('Ctrl Pts',(0.202312178957201,50.0367585835467,1.42817137117346));
#49546=CARTESIAN_POINT('Ctrl Pts',(-0.245403578445858,50.0103003528086,
1.34657862417702));
#49547=CARTESIAN_POINT('Ctrl Pts',(0.739313035185779,55.6695457854907,-1.03532093546362));
#49548=CARTESIAN_POINT('Ctrl Pts',(1.083631436408,55.6430810525602,-0.789456454230577));
#49549=CARTESIAN_POINT('Ctrl Pts',(1.50154220298821,55.5901580888916,0.0686340389533847));
#49550=CARTESIAN_POINT('Ctrl Pts',(0.755604617495797,55.5107768944851,1.30104907818089));
#49551=CARTESIAN_POINT('Ctrl Pts',(-0.68260844130874,55.4314022022709,1.33934409046493));
#49552=CARTESIAN_POINT('Ctrl Pts',(-1.49570780223958,55.3520275100567,0.153664553647287));
#49553=CARTESIAN_POINT('Ctrl Pts',(-0.94029981764689,55.2726528178425,-1.1734808929561));
#49554=CARTESIAN_POINT('Ctrl Pts',(0.475703706523887,55.1932781256284,-1.42633165986584));
#49555=CARTESIAN_POINT('Ctrl Pts',(1.45632605426098,55.1139034334141,-0.374150340681581));
#49556=CARTESIAN_POINT('Ctrl Pts',(1.10427966195761,55.0345287411999,1.02053128172687));
#49557=CARTESIAN_POINT('Ctrl Pts',(-0.258320049836994,54.9551540489857,
1.48125736398945));
#49558=CARTESIAN_POINT('Ctrl Pts',(-1.38452050723547,54.8757793567716,0.586498260820829));
#49559=CARTESIAN_POINT('Ctrl Pts',(-1.24373582344404,54.7964046645574,-0.844986216194058));
#49560=CARTESIAN_POINT('Ctrl Pts',(0.0352065250786907,54.7170299723433,
-1.50320751225676));
#49561=CARTESIAN_POINT('Ctrl Pts',(1.2819299754214,54.6376552801291,-0.785831747466921));
#49562=CARTESIAN_POINT('Ctrl Pts',(1.3555464665119,54.5582805879149,0.650668783353174));
#49563=CARTESIAN_POINT('Ctrl Pts',(0.188687980775752,54.4789058957007,1.49173453810533));
#49564=CARTESIAN_POINT('Ctrl Pts',(-1.15084070664095,54.3995312034865,0.967698963552123));
#49565=CARTESIAN_POINT('Ctrl Pts',(-1.4372231321252,54.3201565112723,-0.441888279663587));
#49566=CARTESIAN_POINT('Ctrl Pts',(-0.408387646289231,54.2407818190582,
-1.44709881985952));
#49567=CARTESIAN_POINT('Ctrl Pts',(0.994167615289757,54.161407126844,-1.12805420575169));
#49568=CARTESIAN_POINT('Ctrl Pts',(1.48694973401431,54.0820324346299,0.223284609291508));
#49569=CARTESIAN_POINT('Ctrl Pts',(0.619008640336589,54.0026577424155,1.37029333274956));
#49570=CARTESIAN_POINT('Ctrl Pts',(-0.815393712832464,53.9232830502014,
1.26333234654755));
#49571=CARTESIAN_POINT('Ctrl Pts',(-1.5036207775666,53.8439083579873,0.00028275136491501));
#49572=CARTESIAN_POINT('Ctrl Pts',(-0.815868788167283,53.7645336657731,
-1.2630255902739));
#49573=CARTESIAN_POINT('Ctrl Pts',(0.61849323696046,53.6851589735588,-1.37052604440289));
#49574=CARTESIAN_POINT('Ctrl Pts',(1.48686565137381,53.6057842813446,-0.223843822678064));
#49575=CARTESIAN_POINT('Ctrl Pts',(0.994591802894592,53.5264095891306,1.12768021515453));
#49576=CARTESIAN_POINT('Ctrl Pts',(-0.407843376111522,53.4470348969164,
1.4472523286476));
#49577=CARTESIAN_POINT('Ctrl Pts',(-1.43705682861252,53.3676602047021,0.442428743972167));
#49578=CARTESIAN_POINT('Ctrl Pts',(-1.1512045914139,53.2882855124879,-0.967265997980326));
#49579=CARTESIAN_POINT('Ctrl Pts',(0.188126972301334,53.2089108202738,-1.49180553841872));
#49580=CARTESIAN_POINT('Ctrl Pts',(1.35530158185256,53.1295361280597,-0.651178273887347));
#49581=CARTESIAN_POINT('Ctrl Pts',(1.28222558057846,53.0501614358455,0.785349019649418));
#49582=CARTESIAN_POINT('Ctrl Pts',(0.0357715792937075,52.9707867436312,
1.50319523558043));
#49583=CARTESIAN_POINT('Ctrl Pts',(-1.2434173672341,52.8914120514171,0.845451815904586));
#49584=CARTESIAN_POINT('Ctrl Pts',(-1.38474211447894,52.812037359203,-0.585973376992345));
#49585=CARTESIAN_POINT('Ctrl Pts',(-0.25887491248398,52.7326626669888,-1.48116822199308));
#49586=CARTESIAN_POINT('Ctrl Pts',(1.1038914215088,52.6532879747745,-1.02093058122293));
#49587=CARTESIAN_POINT('Ctrl Pts',(1.45647520414661,52.5739132825604,0.37357128082892));
#49588=CARTESIAN_POINT('Ctrl Pts',(0.476223339149259,52.4945385903463,1.42621416814043));
#49589=CARTESIAN_POINT('Ctrl Pts',(-0.939825469630544,52.4151638981321,
1.17371359743243));
#49590=CARTESIAN_POINT('Ctrl Pts',(-1.49583019051336,52.3357892059178,-0.152864525937322));
#49591=CARTESIAN_POINT('Ctrl Pts',(-0.682985105353439,52.2564145137037,
-1.33955472751957));
#49592=CARTESIAN_POINT('Ctrl Pts',(0.754866772013506,52.1770398214895,-1.30040442890812));
#49593=CARTESIAN_POINT('Ctrl Pts',(1.50193219438641,52.0976651292753,-0.0712404765685076));
#49594=CARTESIAN_POINT('Ctrl Pts',(0.874563803459747,52.0182904370612,1.22311637870825));
#49595=CARTESIAN_POINT('Ctrl Pts',(-0.55312704435556,51.938915744847,1.39818668115346));
#49596=CARTESIAN_POINT('Ctrl Pts',(-1.47464556526325,51.8595410526328,0.29376177089899));
#49597=CARTESIAN_POINT('Ctrl Pts',(-1.04670055263997,51.7801663604186,-1.07948759871594));
#49598=CARTESIAN_POINT('Ctrl Pts',(0.339091052898566,51.7007916682045,-1.46488661083518));
#49599=CARTESIAN_POINT('Ctrl Pts',(1.41457689579969,51.6214169759902,-0.509752607113461));
#49600=CARTESIAN_POINT('Ctrl Pts',(1.19556867789281,51.5420422837761,0.911861318772394));
#49601=CARTESIAN_POINT('Ctrl Pts',(-0.117516920305048,51.4626675915619,
1.4990214514299));
#49602=CARTESIAN_POINT('Ctrl Pts',(-1.32306152861013,51.3832928993478,0.714411404998759));
#49603=CARTESIAN_POINT('Ctrl Pts',(-1.3178587952042,51.3039182071334,-0.723963934959992));
#49604=CARTESIAN_POINT('Ctrl Pts',(-0.106669617264056,51.2245435149194,
-1.49983239359417));
#49605=CARTESIAN_POINT('Ctrl Pts',(1.20213380754871,51.1451688227052,-0.90318846040789));
#49606=CARTESIAN_POINT('Ctrl Pts',(1.41085250528894,51.065794130491,0.519972400059012));
#49607=CARTESIAN_POINT('Ctrl Pts',(0.328484466660406,50.9864194382767,1.46730158875865));
#49608=CARTESIAN_POINT('Ctrl Pts',(-1.0544813723746,50.9070447460626,1.07188682221037));
#49609=CARTESIAN_POINT('Ctrl Pts',(-1.47248376960954,50.8276700538485,-0.304420847368318));
#49610=CARTESIAN_POINT('Ctrl Pts',(-0.542994120496838,50.7482953616341,
-1.40215356862481));
#49611=CARTESIAN_POINT('Ctrl Pts',(0.883381765596545,50.6689206694202,-1.2167535834064));
#49612=CARTESIAN_POINT('Ctrl Pts',(1.50139200093565,50.5895459772059,0.0820958483892505));
#49613=CARTESIAN_POINT('Ctrl Pts',(0.745411263072938,50.5101712849918,1.30584689096214));
#49614=CARTESIAN_POINT('Ctrl Pts',(-0.692601935418653,50.4307965927775,
1.33454808058404));
#49615=CARTESIAN_POINT('Ctrl Pts',(-1.49700660212466,50.3514219005633,0.142099916942318));
#49616=CARTESIAN_POINT('Ctrl Pts',(-0.93109448903233,50.2720472083492,-1.18060055786096));
#49617=CARTESIAN_POINT('Ctrl Pts',(0.486104276473247,50.192672516135,-1.4224976306496));
#49618=CARTESIAN_POINT('Ctrl Pts',(1.4599793847676,50.1132978239209,-0.363493105670402));
#49619=CARTESIAN_POINT('Ctrl Pts',(1.09475134669248,50.0339231317067,1.02989780490955));
#49620=CARTESIAN_POINT('Ctrl Pts',(0.188039156768732,49.9810066702304,1.32741460124119));
#49621=CARTESIAN_POINT('Ctrl Pts',(-0.228090479756796,49.9545484394925,
1.2515781813937));
#49622=CARTESIAN_POINT('Ctrl Pts',(0.68319583312661,55.6137938721746,-0.956735395419802));
#49623=CARTESIAN_POINT('Ctrl Pts',(1.00137891091411,55.5873291392441,-0.729533139950251));
#49624=CARTESIAN_POINT('Ctrl Pts',(1.38756836079254,55.5344061755755,0.0634244050787278));
#49625=CARTESIAN_POINT('Ctrl Pts',(0.69825081067944,55.4550249811689,1.20229357065649));
#49626=CARTESIAN_POINT('Ctrl Pts',(-0.630795374305817,55.3756502889546,
1.23768181836324));
#49627=CARTESIAN_POINT('Ctrl Pts',(-1.38217681744006,55.2962755967406,0.14200071925514));
#49628=CARTESIAN_POINT('Ctrl Pts',(-0.868926810068525,55.2169009045263,
-1.08440838746992));
#49629=CARTESIAN_POINT('Ctrl Pts',(0.43959564437862,55.1375262123122,-1.31806663794589));
#49630=CARTESIAN_POINT('Ctrl Pts',(1.34578432219146,55.0581515200979,-0.345750638161437));
#49631=CARTESIAN_POINT('Ctrl Pts',(1.02045984278677,54.9787768278838,0.943068343270797));
#49632=CARTESIAN_POINT('Ctrl Pts',(-0.238712390100558,54.8994021356696,
1.36882323278852));
#49633=CARTESIAN_POINT('Ctrl Pts',(-1.27942914084278,54.8200274434554,0.541980391064116));
#49634=CARTESIAN_POINT('Ctrl Pts',(-1.1493306510871,54.7406527512412,-0.780847941911555));
#49635=CARTESIAN_POINT('Ctrl Pts',(0.0325341906444134,54.661278059027,-1.38910726555817));
#49636=CARTESIAN_POINT('Ctrl Pts',(1.18462569424049,54.5819033668129,-0.726183564818503));
#49637=CARTESIAN_POINT('Ctrl Pts',(1.25265436081173,54.5025286745987,0.601280080799261));
#49638=CARTESIAN_POINT('Ctrl Pts',(0.174365709911593,54.4231539823845,1.3785051420181));
#49639=CARTESIAN_POINT('Ctrl Pts',(-1.06348669366016,54.3437792901703,0.894246236918589));
#49640=CARTESIAN_POINT('Ctrl Pts',(-1.32813139821668,54.2644045979561,-0.408346961308196));
#49641=CARTESIAN_POINT('Ctrl Pts',(-0.377389177474829,54.185029905742,-1.33725747660058));
#49642=CARTESIAN_POINT('Ctrl Pts',(0.918705798315464,54.1056552135278,-1.04242979121399));
#49643=CARTESIAN_POINT('Ctrl Pts',(1.37408352619134,54.0262805213136,0.206336297899756));
#49644=CARTESIAN_POINT('Ctrl Pts',(0.572023085784021,53.9469058290994,1.26628187322631));
#49645=CARTESIAN_POINT('Ctrl Pts',(-0.753501643352997,53.8675311368853,
1.16743970948443));
#49646=CARTESIAN_POINT('Ctrl Pts',(-1.38948916216248,53.7881564446711,0.00026128925789496));
#49647=CARTESIAN_POINT('Ctrl Pts',(-0.753940658321912,53.7087817524569,
-1.16715623739892));
#49648=CARTESIAN_POINT('Ctrl Pts',(0.571546803854467,53.6294070602427,-1.26649692101297));
#49649=CARTESIAN_POINT('Ctrl Pts',(1.3740058258034,53.5500323680285,-0.206853064461862));
#49650=CARTESIAN_POINT('Ctrl Pts',(0.919097788163184,53.4706576758144,1.0420841881941));
#49651=CARTESIAN_POINT('Ctrl Pts',(-0.376886219864453,53.3912829836002,
1.33739933337758));
#49652=CARTESIAN_POINT('Ctrl Pts',(-1.32797771789253,53.311908291386,0.408846401932117));
#49653=CARTESIAN_POINT('Ctrl Pts',(-1.06382295793358,53.2325335991718,-0.893846135391286));
#49654=CARTESIAN_POINT('Ctrl Pts',(0.173847284516908,53.1531589069577,-1.37857075308668));
#49655=CARTESIAN_POINT('Ctrl Pts',(1.25242806400526,53.0737842147435,-0.601750898698296));
#49656=CARTESIAN_POINT('Ctrl Pts',(1.18489886162958,52.9944095225293,0.725737478224937));
#49657=CARTESIAN_POINT('Ctrl Pts',(0.033056354689693,52.9150348303151,1.38909592073708));
#49658=CARTESIAN_POINT('Ctrl Pts',(-1.14903636714335,52.835660138101,0.781278200498908));
#49659=CARTESIAN_POINT('Ctrl Pts',(-1.27963392709449,52.7562854458867,-0.541495348291405));
#49660=CARTESIAN_POINT('Ctrl Pts',(-0.239225136163902,52.6769107536726,
-1.36874085707271));
#49661=CARTESIAN_POINT('Ctrl Pts',(1.0201010715434,52.5975360614583,-0.943437334129717));
#49662=CARTESIAN_POINT('Ctrl Pts',(1.34592215092642,52.5181613692442,0.345215531569735));
#49663=CARTESIAN_POINT('Ctrl Pts',(0.440075834538276,52.43878667703,1.31795806437367));
#49664=CARTESIAN_POINT('Ctrl Pts',(-0.868488467211321,52.3594119848159,
1.08462342862434));
#49665=CARTESIAN_POINT('Ctrl Pts',(-1.38228991589051,52.2800372926017,-0.141261417265575));
#49666=CARTESIAN_POINT('Ctrl Pts',(-0.631143447846485,52.2006626003875,
-1.23787646711307));
#49667=CARTESIAN_POINT('Ctrl Pts',(0.69756897100532,52.1212879081734,-1.2016978531782));
#49668=CARTESIAN_POINT('Ctrl Pts',(1.38792875008033,52.0419132159591,-0.065833002294249));
#49669=CARTESIAN_POINT('Ctrl Pts',(0.808180456573323,51.962538523745,1.13027631543437));
#49670=CARTESIAN_POINT('Ctrl Pts',(-0.511142200811324,51.8831638315307,
1.29205799037093));
#49671=CARTESIAN_POINT('Ctrl Pts',(-1.36271329947986,51.8037891393167,0.271463924289723));
#49672=CARTESIAN_POINT('Ctrl Pts',(-0.967251248201307,51.7244144471024,
-0.9975496092386));
#49673=CARTESIAN_POINT('Ctrl Pts',(0.313352508836268,51.6450397548883,-1.35369509381647));
#49674=CARTESIAN_POINT('Ctrl Pts',(1.30720411361969,51.565665062674,-0.471060079466639));
#49675=CARTESIAN_POINT('Ctrl Pts',(1.10481960966345,51.4862903704599,0.84264692183885));
#49676=CARTESIAN_POINT('Ctrl Pts',(-0.108596854719476,51.4069156782457,
1.38523894567469));
#49677=CARTESIAN_POINT('Ctrl Pts',(-1.22263517657228,51.3275409860315,0.660184349259611));
#49678=CARTESIAN_POINT('Ctrl Pts',(-1.21782735415521,51.2481662938174,-0.669011799006525));
#49679=CARTESIAN_POINT('Ctrl Pts',(-0.0985729110236722,51.1687916016031,
-1.38598833366215));
#49680=CARTESIAN_POINT('Ctrl Pts',(1.11088641629526,51.089416909389,-0.83463237263718));
#49681=CARTESIAN_POINT('Ctrl Pts',(1.30376242118797,51.0100422171748,0.480504143920437));
#49682=CARTESIAN_POINT('Ctrl Pts',(0.303551010449595,50.9306675249606,1.3559267639966));
#49683=CARTESIAN_POINT('Ctrl Pts',(-0.97444146853832,50.8512928327465,0.990525766035526));
#49684=CARTESIAN_POINT('Ctrl Pts',(-1.36071559389048,50.7719181405323,-0.281313928661689));
#49685=CARTESIAN_POINT('Ctrl Pts',(-0.501778411687899,50.6925434483181,
-1.29572377314753));
#49686=CARTESIAN_POINT('Ctrl Pts',(0.816329095514904,50.6131687561039,-1.12439648506431));
#49687=CARTESIAN_POINT('Ctrl Pts',(1.38742955975489,50.5337940638897,0.0758644023129377));
#49688=CARTESIAN_POINT('Ctrl Pts',(0.688831177944937,50.4544193716755,1.20672720775508));
#49689=CARTESIAN_POINT('Ctrl Pts',(-0.640030317028762,50.3750446794614,
1.23324984731672));
#49690=CARTESIAN_POINT('Ctrl Pts',(-1.38337703254154,50.2956699872472,0.131313890763781));
#49691=CARTESIAN_POINT('Ctrl Pts',(-0.860420207516269,50.216295295033,-1.09098763761804));
#49692=CARTESIAN_POINT('Ctrl Pts',(0.449206764044268,50.1369206028188,-1.31452362888213));
#49693=CARTESIAN_POINT('Ctrl Pts',(1.34916034839469,50.0575459106046,-0.335902335472633));
#49694=CARTESIAN_POINT('Ctrl Pts',(1.01165476973106,49.9781712183904,0.951723904994636));
#49695=CARTESIAN_POINT('Ctrl Pts',(0.173766134580262,49.9252547569143,1.22665783130891));
#49696=CARTESIAN_POINT('Ctrl Pts',(-0.210777381067733,49.8987965261763,
1.15657773861039));
#49697=CARTESIAN_POINT('Ctrl Pts',(0.634286466388226,55.615,1.31890595895111));
#49698=CARTESIAN_POINT('Ctrl Pts',(0.642198332342847,55.615,1.31501256253275));
#49699=CARTESIAN_POINT('Ctrl Pts',(0.650110198297467,55.615,1.3111191661144));
#49700=CARTESIAN_POINT('Ctrl Pts',(0.658022064252088,55.615,1.30722576969605));
#49701=CARTESIAN_POINT('Origin',(0.,55.615,0.));
#49702=CARTESIAN_POINT('',(-1.91473527046689E-16,55.715,-1.5635));
#49703=CARTESIAN_POINT('Origin',(0.,55.715,0.));
#49704=CARTESIAN_POINT('Origin',(-1.91473527046689E-16,55.615,-1.5635));
#49705=CARTESIAN_POINT('Origin',(0.,55.715,0.));
#49706=CARTESIAN_POINT('',(-3.12284933782575E-16,55.715,-2.55));
#49707=CARTESIAN_POINT('Origin',(0.,55.715,0.));
#49708=CARTESIAN_POINT('Origin',(0.,49.89,0.));
#49709=CARTESIAN_POINT('',(-1.1135,49.715,1.36364421085058E-16));
#49710=CARTESIAN_POINT('',(-1.2885,49.89,1.57795740070136E-16));
#49711=CARTESIAN_POINT('Origin',(0.,49.715,0.));
#49712=CARTESIAN_POINT('Origin',(0.,49.715,0.));
#49713=CARTESIAN_POINT('Origin',(2.56050015783174,58.715,-0.451485261934019));
#49714=CARTESIAN_POINT('',(2.56050015783174,58.565,-0.451485261934019));
#49715=CARTESIAN_POINT('',(2.69848592069234,58.415,-0.529786500229296));
#49716=CARTESIAN_POINT('Ctrl Pts',(2.56050015783174,58.565,-0.451485261934019));
#49717=CARTESIAN_POINT('Ctrl Pts',(2.62755865940943,58.4923524443611,-0.489538200171299));
#49718=CARTESIAN_POINT('Ctrl Pts',(2.69848592069235,58.415,-0.529786500229297));
#49719=CARTESIAN_POINT('',(2.56050015783174,56.315,-0.451485261934019));
#49720=CARTESIAN_POINT('',(2.56050015783174,58.715,-0.451485261934019));
#49721=CARTESIAN_POINT('',(2.69848592069234,56.315,-0.529786500229296));
#49722=CARTESIAN_POINT('',(2.56050015783174,56.315,-0.451485261934019));
#49723=CARTESIAN_POINT('',(2.69848592069234,55.715,-0.529786500229296));
#49724=CARTESIAN_POINT('Origin',(2.78208190225949,56.315,-0.490556101909078));
#49725=CARTESIAN_POINT('',(2.71694496170969,56.315,-0.425100076500034));
#49726=CARTESIAN_POINT('Origin',(0.,56.315,0.));
#49727=CARTESIAN_POINT('',(3.03144735511394,56.315,-0.372057701402184));
#49728=CARTESIAN_POINT('Origin',(3.03144735511394,58.715,-0.372057701402184));
#49729=CARTESIAN_POINT('',(2.71694496170969,58.415,-0.425100076500034));
#49730=CARTESIAN_POINT('Ctrl Pts',(2.71694496170969,58.415,-0.425100076500033));
#49731=CARTESIAN_POINT('Ctrl Pts',(2.63652940831481,58.4923524443615,-0.438662554994084));
#49732=CARTESIAN_POINT('Ctrl Pts',(2.56050015783174,58.565,-0.451485261934019));
#49733=CARTESIAN_POINT('',(2.71694496170969,55.715,-0.425100076500034));
#49734=CARTESIAN_POINT('Origin',(0.,55.715,0.));
#49735=CARTESIAN_POINT('',(-2.74948631640946,56.315,0.0531506902789203));
#49736=CARTESIAN_POINT('',(-2.75,56.315,3.36777869765522E-16));
#49737=CARTESIAN_POINT('Origin',(0.,56.315,0.));
#49738=CARTESIAN_POINT('',(-2.75,55.915,3.36777869765522E-16));
#49739=CARTESIAN_POINT('',(-2.75,55.715,3.36777869765522E-16));
#49740=CARTESIAN_POINT('',(-3.36777869765522E-16,55.915,-2.75));
#49741=CARTESIAN_POINT('Origin',(0.,55.915,0.));
#49742=CARTESIAN_POINT('Origin',(0.,55.915,0.));
#49743=CARTESIAN_POINT('',(-2.74948631640946,56.315,-0.0531506902789196));
#49744=CARTESIAN_POINT('Origin',(0.,56.315,0.));
#49745=CARTESIAN_POINT('',(-2.74948631640946,58.415,-0.0531506902789196));
#49746=CARTESIAN_POINT('',(-2.74948631640946,55.715,-0.0531506902789196));
#49747=CARTESIAN_POINT('',(-2.71694496170969,58.415,-0.425100076500032));
#49748=CARTESIAN_POINT('Origin',(0.,58.415,0.));
#49749=CARTESIAN_POINT('',(-2.71694496170969,56.315,-0.425100076500032));
#49750=CARTESIAN_POINT('',(-2.71694496170969,55.715,-0.425100076500032));
#49751=CARTESIAN_POINT('',(-2.69848592069234,56.315,-0.529786500229295));
#49752=CARTESIAN_POINT('Origin',(0.,56.315,0.));
#49753=CARTESIAN_POINT('',(-2.69848592069234,58.415,-0.529786500229295));
#49754=CARTESIAN_POINT('',(-2.69848592069234,55.715,-0.529786500229295));
#49755=CARTESIAN_POINT('',(-2.60185060918886,58.415,-0.890434392565551));
#49756=CARTESIAN_POINT('Origin',(0.,58.415,0.));
#49757=CARTESIAN_POINT('',(-2.60185060918886,56.315,-0.890434392565551));
#49758=CARTESIAN_POINT('',(-2.60185060918886,55.715,-0.890434392565551));
#49759=CARTESIAN_POINT('',(-2.56549339577475,56.315,-0.990325015455108));
#49760=CARTESIAN_POINT('Origin',(0.,56.315,0.));
#49761=CARTESIAN_POINT('',(-2.56549339577475,58.415,-0.990325015455107));
#49762=CARTESIAN_POINT('',(-2.56549339577475,55.715,-0.990325015455107));
#49763=CARTESIAN_POINT('',(-2.40770034250775,58.415,-1.32871331019451));
#49764=CARTESIAN_POINT('Origin',(0.,58.415,0.));
#49765=CARTESIAN_POINT('',(-2.40770034250775,56.315,-1.32871331019451));
#49766=CARTESIAN_POINT('',(-2.40770034250775,55.715,-1.32871331019451));
#49767=CARTESIAN_POINT('',(-2.35454965222883,56.315,-1.42077300621495));
#49768=CARTESIAN_POINT('Origin',(0.,56.315,0.));
#49769=CARTESIAN_POINT('',(-2.35454965222883,58.415,-1.42077300621495));
#49770=CARTESIAN_POINT('',(-2.35454965222883,55.715,-1.42077300621495));
#49771=CARTESIAN_POINT('',(-2.14039331927471,58.415,-1.72661994625458));
#49772=CARTESIAN_POINT('Origin',(0.,58.415,0.));
#49773=CARTESIAN_POINT('',(-2.14039331927471,56.315,-1.72661994625458));
#49774=CARTESIAN_POINT('',(-2.14039331927471,55.715,-1.72661994625458));
#49775=CARTESIAN_POINT('',(-2.07206410895956,56.315,-1.80805152812679));
#49776=CARTESIAN_POINT('Origin',(0.,56.315,0.));
#49777=CARTESIAN_POINT('',(-2.07206410895956,58.415,-1.80805152812679));
#49778=CARTESIAN_POINT('',(-2.07206410895956,55.715,-1.80805152812679));
#49779=CARTESIAN_POINT('',(-1.80805152812679,58.415,-2.07206410895956));
#49780=CARTESIAN_POINT('Origin',(0.,58.415,0.));
#49781=CARTESIAN_POINT('',(-1.80805152812679,56.315,-2.07206410895956));
#49782=CARTESIAN_POINT('',(-1.80805152812679,55.715,-2.07206410895956));
#49783=CARTESIAN_POINT('',(-1.72661994625458,56.315,-2.14039331927471));
#49784=CARTESIAN_POINT('Origin',(0.,56.315,0.));
#49785=CARTESIAN_POINT('',(-1.72661994625458,58.415,-2.14039331927471));
#49786=CARTESIAN_POINT('',(-1.72661994625458,55.715,-2.14039331927471));
#49787=CARTESIAN_POINT('',(-1.42077300621496,58.415,-2.35454965222883));
#49788=CARTESIAN_POINT('Origin',(0.,58.415,0.));
#49789=CARTESIAN_POINT('',(-1.42077300621496,56.315,-2.35454965222883));
#49790=CARTESIAN_POINT('',(-1.42077300621496,55.715,-2.35454965222883));
#49791=CARTESIAN_POINT('',(-1.32871331019451,56.315,-2.40770034250775));
#49792=CARTESIAN_POINT('Origin',(0.,56.315,0.));
#49793=CARTESIAN_POINT('',(-1.32871331019451,58.415,-2.40770034250775));
#49794=CARTESIAN_POINT('',(-1.32871331019451,55.715,-2.40770034250775));
#49795=CARTESIAN_POINT('',(-0.99032501545511,58.415,-2.56549339577475));
#49796=CARTESIAN_POINT('Origin',(0.,58.415,0.));
#49797=CARTESIAN_POINT('',(-0.99032501545511,56.315,-2.56549339577475));
#49798=CARTESIAN_POINT('',(-0.99032501545511,55.715,-2.56549339577475));
#49799=CARTESIAN_POINT('',(-0.890434392565553,56.315,-2.60185060918886));
#49800=CARTESIAN_POINT('Origin',(0.,56.315,0.));
#49801=CARTESIAN_POINT('',(-0.890434392565553,58.415,-2.60185060918885));
#49802=CARTESIAN_POINT('',(-0.890434392565553,55.715,-2.60185060918885));
#49803=CARTESIAN_POINT('',(-0.529786500229296,58.415,-2.69848592069234));
#49804=CARTESIAN_POINT('Origin',(0.,58.415,0.));
#49805=CARTESIAN_POINT('',(-0.529786500229296,56.315,-2.69848592069234));
#49806=CARTESIAN_POINT('',(-0.529786500229296,55.715,-2.69848592069234));
#49807=CARTESIAN_POINT('',(-0.425100076500033,56.315,-2.71694496170969));
#49808=CARTESIAN_POINT('Origin',(0.,56.315,0.));
#49809=CARTESIAN_POINT('',(-0.425100076500033,58.415,-2.71694496170969));
#49810=CARTESIAN_POINT('',(-0.425100076500033,55.715,-2.71694496170969));
#49811=CARTESIAN_POINT('',(-0.0531506902789204,58.415,-2.74948631640946));
#49812=CARTESIAN_POINT('Origin',(0.,58.415,0.));
#49813=CARTESIAN_POINT('',(-0.0531506902789204,56.315,-2.74948631640946));
#49814=CARTESIAN_POINT('',(-0.0531506902789204,55.715,-2.74948631640946));
#49815=CARTESIAN_POINT('',(0.0531506902789194,56.315,-2.74948631640946));
#49816=CARTESIAN_POINT('Origin',(0.,56.315,0.));
#49817=CARTESIAN_POINT('',(0.0531506902789194,58.415,-2.74948631640946));
#49818=CARTESIAN_POINT('',(0.0531506902789194,55.715,-2.74948631640946));
#49819=CARTESIAN_POINT('',(0.425100076500032,58.415,-2.71694496170969));
#49820=CARTESIAN_POINT('Origin',(0.,58.415,0.));
#49821=CARTESIAN_POINT('',(0.425100076500032,56.315,-2.71694496170969));
#49822=CARTESIAN_POINT('',(0.425100076500032,55.715,-2.71694496170969));
#49823=CARTESIAN_POINT('',(0.529786500229294,56.315,-2.69848592069234));
#49824=CARTESIAN_POINT('Origin',(0.,56.315,0.));
#49825=CARTESIAN_POINT('',(0.529786500229294,58.415,-2.69848592069234));
#49826=CARTESIAN_POINT('',(0.529786500229294,55.715,-2.69848592069234));
#49827=CARTESIAN_POINT('',(0.890434392565549,58.415,-2.60185060918886));
#49828=CARTESIAN_POINT('Origin',(0.,58.415,0.));
#49829=CARTESIAN_POINT('',(0.890434392565549,56.315,-2.60185060918886));
#49830=CARTESIAN_POINT('',(0.890434392565549,55.715,-2.60185060918886));
#49831=CARTESIAN_POINT('',(0.990325015455106,56.315,-2.56549339577475));
#49832=CARTESIAN_POINT('Origin',(0.,56.315,0.));
#49833=CARTESIAN_POINT('',(0.990325015455106,58.415,-2.56549339577475));
#49834=CARTESIAN_POINT('',(0.990325015455106,55.715,-2.56549339577475));
#49835=CARTESIAN_POINT('',(1.32871331019451,58.415,-2.40770034250775));
#49836=CARTESIAN_POINT('Origin',(0.,58.415,0.));
#49837=CARTESIAN_POINT('',(1.32871331019451,56.315,-2.40770034250775));
#49838=CARTESIAN_POINT('',(1.32871331019451,55.715,-2.40770034250775));
#49839=CARTESIAN_POINT('',(1.42077300621496,56.315,-2.35454965222883));
#49840=CARTESIAN_POINT('Origin',(0.,56.315,0.));
#49841=CARTESIAN_POINT('',(1.42077300621495,58.415,-2.35454965222883));
#49842=CARTESIAN_POINT('',(1.42077300621495,55.715,-2.35454965222883));
#49843=CARTESIAN_POINT('',(1.72661994625458,58.415,-2.14039331927471));
#49844=CARTESIAN_POINT('Origin',(0.,58.415,0.));
#49845=CARTESIAN_POINT('',(1.72661994625458,56.315,-2.14039331927471));
#49846=CARTESIAN_POINT('',(1.72661994625458,55.715,-2.14039331927471));
#49847=CARTESIAN_POINT('',(1.80805152812679,56.315,-2.07206410895956));
#49848=CARTESIAN_POINT('Origin',(0.,56.315,0.));
#49849=CARTESIAN_POINT('',(1.80805152812679,58.415,-2.07206410895956));
#49850=CARTESIAN_POINT('',(1.80805152812679,55.715,-2.07206410895956));
#49851=CARTESIAN_POINT('',(2.07206410895956,58.415,-1.80805152812679));
#49852=CARTESIAN_POINT('Origin',(0.,58.415,0.));
#49853=CARTESIAN_POINT('',(2.07206410895956,56.315,-1.80805152812679));
#49854=CARTESIAN_POINT('',(2.07206410895956,55.715,-1.80805152812679));
#49855=CARTESIAN_POINT('',(2.14039331927471,56.315,-1.72661994625458));
#49856=CARTESIAN_POINT('Origin',(0.,56.315,0.));
#49857=CARTESIAN_POINT('',(2.14039331927471,58.415,-1.72661994625458));
#49858=CARTESIAN_POINT('',(2.14039331927471,55.715,-1.72661994625458));
#49859=CARTESIAN_POINT('',(2.35454965222883,58.415,-1.42077300621496));
#49860=CARTESIAN_POINT('Origin',(0.,58.415,0.));
#49861=CARTESIAN_POINT('',(2.35454965222883,56.315,-1.42077300621496));
#49862=CARTESIAN_POINT('',(2.35454965222883,55.715,-1.42077300621496));
#49863=CARTESIAN_POINT('',(2.40770034250775,56.315,-1.32871331019451));
#49864=CARTESIAN_POINT('Origin',(0.,56.315,0.));
#49865=CARTESIAN_POINT('',(2.40770034250775,58.415,-1.32871331019451));
#49866=CARTESIAN_POINT('',(2.40770034250775,55.715,-1.32871331019451));
#49867=CARTESIAN_POINT('',(2.56549339577475,58.415,-0.99032501545511));
#49868=CARTESIAN_POINT('Origin',(0.,58.415,0.));
#49869=CARTESIAN_POINT('',(2.56549339577475,56.315,-0.99032501545511));
#49870=CARTESIAN_POINT('',(2.56549339577475,55.715,-0.99032501545511));
#49871=CARTESIAN_POINT('',(2.60185060918885,56.315,-0.890434392565553));
#49872=CARTESIAN_POINT('Origin',(0.,56.315,0.));
#49873=CARTESIAN_POINT('',(2.60185060918885,58.415,-0.890434392565553));
#49874=CARTESIAN_POINT('',(2.60185060918885,55.715,-0.890434392565553));
#49875=CARTESIAN_POINT('Origin',(0.,58.415,0.));
#49876=CARTESIAN_POINT('',(2.74948631640946,58.415,-0.0531506902789199));
#49877=CARTESIAN_POINT('Origin',(0.,58.415,0.));
#49878=CARTESIAN_POINT('',(2.74948631640946,56.315,-0.0531506902789199));
#49879=CARTESIAN_POINT('',(2.74948631640946,55.715,-0.0531506902789199));
#49880=CARTESIAN_POINT('',(2.74948631640946,56.315,0.0531506902789197));
#49881=CARTESIAN_POINT('Origin',(0.,56.315,0.));
#49882=CARTESIAN_POINT('',(2.74948631640946,58.415,0.0531506902789197));
#49883=CARTESIAN_POINT('',(2.74948631640946,55.715,0.0531506902789197));
#49884=CARTESIAN_POINT('',(2.71694496170969,58.415,0.425100076500033));
#49885=CARTESIAN_POINT('Origin',(0.,58.415,0.));
#49886=CARTESIAN_POINT('',(2.71694496170969,56.315,0.425100076500033));
#49887=CARTESIAN_POINT('',(2.71694496170969,55.715,0.425100076500033));
#49888=CARTESIAN_POINT('',(2.69848592069234,56.315,0.529786500229295));
#49889=CARTESIAN_POINT('Origin',(0.,56.315,0.));
#49890=CARTESIAN_POINT('',(2.69848592069234,58.415,0.529786500229295));
#49891=CARTESIAN_POINT('',(2.69848592069234,55.715,0.529786500229295));
#49892=CARTESIAN_POINT('',(2.60185060918886,58.415,0.890434392565551));
#49893=CARTESIAN_POINT('Origin',(0.,58.415,0.));
#49894=CARTESIAN_POINT('',(2.60185060918886,56.315,0.890434392565551));
#49895=CARTESIAN_POINT('',(2.60185060918886,55.715,0.890434392565551));
#49896=CARTESIAN_POINT('',(2.56549339577475,56.315,0.990325015455108));
#49897=CARTESIAN_POINT('Origin',(0.,56.315,0.));
#49898=CARTESIAN_POINT('',(2.56549339577475,58.415,0.990325015455108));
#49899=CARTESIAN_POINT('',(2.56549339577475,55.715,0.990325015455108));
#49900=CARTESIAN_POINT('',(2.40770034250775,58.415,1.32871331019451));
#49901=CARTESIAN_POINT('Origin',(0.,58.415,0.));
#49902=CARTESIAN_POINT('',(2.40770034250775,56.315,1.32871331019451));
#49903=CARTESIAN_POINT('',(2.40770034250775,55.715,1.32871331019451));
#49904=CARTESIAN_POINT('',(2.35454965222883,56.315,1.42077300621495));
#49905=CARTESIAN_POINT('Origin',(0.,56.315,0.));
#49906=CARTESIAN_POINT('',(2.35454965222883,58.415,1.42077300621495));
#49907=CARTESIAN_POINT('',(2.35454965222883,55.715,1.42077300621495));
#49908=CARTESIAN_POINT('',(2.14039331927471,58.415,1.72661994625458));
#49909=CARTESIAN_POINT('Origin',(0.,58.415,0.));
#49910=CARTESIAN_POINT('',(2.14039331927471,56.315,1.72661994625458));
#49911=CARTESIAN_POINT('',(2.14039331927471,55.715,1.72661994625458));
#49912=CARTESIAN_POINT('',(2.07206410895956,56.315,1.80805152812679));
#49913=CARTESIAN_POINT('Origin',(0.,56.315,0.));
#49914=CARTESIAN_POINT('',(2.07206410895956,58.415,1.80805152812679));
#49915=CARTESIAN_POINT('',(2.07206410895956,55.715,1.80805152812679));
#49916=CARTESIAN_POINT('',(1.80805152812679,58.415,2.07206410895956));
#49917=CARTESIAN_POINT('Origin',(0.,58.415,0.));
#49918=CARTESIAN_POINT('',(1.80805152812679,56.315,2.07206410895956));
#49919=CARTESIAN_POINT('',(1.80805152812679,55.715,2.07206410895956));
#49920=CARTESIAN_POINT('',(1.72661994625458,56.315,2.14039331927471));
#49921=CARTESIAN_POINT('Origin',(0.,56.315,0.));
#49922=CARTESIAN_POINT('',(1.72661994625458,58.415,2.14039331927471));
#49923=CARTESIAN_POINT('',(1.72661994625458,55.715,2.14039331927471));
#49924=CARTESIAN_POINT('',(1.42077300621495,58.415,2.35454965222883));
#49925=CARTESIAN_POINT('Origin',(0.,58.415,0.));
#49926=CARTESIAN_POINT('',(1.42077300621496,56.315,2.35454965222883));
#49927=CARTESIAN_POINT('',(1.42077300621495,55.715,2.35454965222883));
#49928=CARTESIAN_POINT('',(1.32871331019451,56.315,2.40770034250775));
#49929=CARTESIAN_POINT('Origin',(0.,56.315,0.));
#49930=CARTESIAN_POINT('',(1.32871331019451,58.415,2.40770034250775));
#49931=CARTESIAN_POINT('',(1.32871331019451,55.715,2.40770034250775));
#49932=CARTESIAN_POINT('',(0.990325015455108,58.415,2.56549339577475));
#49933=CARTESIAN_POINT('Origin',(0.,58.415,0.));
#49934=CARTESIAN_POINT('',(0.990325015455108,56.315,2.56549339577475));
#49935=CARTESIAN_POINT('',(0.990325015455108,55.715,2.56549339577475));
#49936=CARTESIAN_POINT('',(0.890434392565551,56.315,2.60185060918886));
#49937=CARTESIAN_POINT('Origin',(0.,56.315,0.));
#49938=CARTESIAN_POINT('',(0.890434392565551,58.415,2.60185060918886));
#49939=CARTESIAN_POINT('',(0.890434392565551,55.715,2.60185060918886));
#49940=CARTESIAN_POINT('',(0.529786500229295,58.415,2.69848592069234));
#49941=CARTESIAN_POINT('Origin',(0.,58.415,0.));
#49942=CARTESIAN_POINT('',(0.529786500229296,56.315,2.69848592069234));
#49943=CARTESIAN_POINT('',(0.529786500229295,55.715,2.69848592069234));
#49944=CARTESIAN_POINT('',(0.425100076500034,56.315,2.71694496170969));
#49945=CARTESIAN_POINT('Origin',(0.,56.315,0.));
#49946=CARTESIAN_POINT('',(0.425100076500033,58.415,2.71694496170969));
#49947=CARTESIAN_POINT('',(0.425100076500033,55.715,2.71694496170969));
#49948=CARTESIAN_POINT('',(0.05315069027892,58.415,2.74948631640946));
#49949=CARTESIAN_POINT('Origin',(0.,58.415,0.));
#49950=CARTESIAN_POINT('',(0.0531506902789201,56.315,2.74948631640946));
#49951=CARTESIAN_POINT('',(0.05315069027892,55.715,2.74948631640946));
#49952=CARTESIAN_POINT('',(-0.0531506902789196,56.315,2.74948631640946));
#49953=CARTESIAN_POINT('Origin',(0.,56.315,0.));
#49954=CARTESIAN_POINT('',(-0.0531506902789199,58.415,2.74948631640946));
#49955=CARTESIAN_POINT('',(-0.0531506902789199,55.715,2.74948631640946));
#49956=CARTESIAN_POINT('',(-0.425100076500033,58.415,2.71694496170969));
#49957=CARTESIAN_POINT('Origin',(0.,58.415,0.));
#49958=CARTESIAN_POINT('',(-0.425100076500033,56.315,2.71694496170969));
#49959=CARTESIAN_POINT('',(-0.425100076500033,55.715,2.71694496170969));
#49960=CARTESIAN_POINT('',(-0.529786500229295,56.315,2.69848592069234));
#49961=CARTESIAN_POINT('Origin',(0.,56.315,0.));
#49962=CARTESIAN_POINT('',(-0.529786500229295,58.415,2.69848592069234));
#49963=CARTESIAN_POINT('',(-0.529786500229295,55.715,2.69848592069234));
#49964=CARTESIAN_POINT('',(-0.890434392565551,58.415,2.60185060918886));
#49965=CARTESIAN_POINT('Origin',(0.,58.415,0.));
#49966=CARTESIAN_POINT('',(-0.890434392565551,56.315,2.60185060918886));
#49967=CARTESIAN_POINT('',(-0.890434392565551,55.715,2.60185060918886));
#49968=CARTESIAN_POINT('',(-0.990325015455108,56.315,2.56549339577475));
#49969=CARTESIAN_POINT('Origin',(0.,56.315,0.));
#49970=CARTESIAN_POINT('',(-0.990325015455108,58.415,2.56549339577475));
#49971=CARTESIAN_POINT('',(-0.990325015455108,55.715,2.56549339577475));
#49972=CARTESIAN_POINT('',(-1.32871331019451,58.415,2.40770034250775));
#49973=CARTESIAN_POINT('Origin',(0.,58.415,0.));
#49974=CARTESIAN_POINT('',(-1.32871331019451,56.315,2.40770034250775));
#49975=CARTESIAN_POINT('',(-1.32871331019451,55.715,2.40770034250775));
#49976=CARTESIAN_POINT('',(-1.42077300621495,56.315,2.35454965222883));
#49977=CARTESIAN_POINT('Origin',(0.,56.315,0.));
#49978=CARTESIAN_POINT('',(-1.42077300621495,58.415,2.35454965222883));
#49979=CARTESIAN_POINT('',(-1.42077300621495,55.715,2.35454965222883));
#49980=CARTESIAN_POINT('',(-1.72661994625458,58.415,2.14039331927471));
#49981=CARTESIAN_POINT('Origin',(0.,58.415,0.));
#49982=CARTESIAN_POINT('',(-1.72661994625458,56.315,2.14039331927471));
#49983=CARTESIAN_POINT('',(-1.72661994625458,55.715,2.14039331927471));
#49984=CARTESIAN_POINT('',(-1.80805152812679,56.315,2.07206410895956));
#49985=CARTESIAN_POINT('Origin',(0.,56.315,0.));
#49986=CARTESIAN_POINT('',(-1.80805152812679,58.415,2.07206410895956));
#49987=CARTESIAN_POINT('',(-1.80805152812679,55.715,2.07206410895956));
#49988=CARTESIAN_POINT('',(-2.07206410895956,58.415,1.80805152812679));
#49989=CARTESIAN_POINT('Origin',(0.,58.415,0.));
#49990=CARTESIAN_POINT('',(-2.07206410895956,56.315,1.80805152812679));
#49991=CARTESIAN_POINT('',(-2.07206410895956,55.715,1.80805152812679));
#49992=CARTESIAN_POINT('',(-2.14039331927471,56.315,1.72661994625458));
#49993=CARTESIAN_POINT('Origin',(0.,56.315,0.));
#49994=CARTESIAN_POINT('',(-2.14039331927471,58.415,1.72661994625458));
#49995=CARTESIAN_POINT('',(-2.14039331927471,55.715,1.72661994625458));
#49996=CARTESIAN_POINT('',(-2.35454965222883,58.415,1.42077300621495));
#49997=CARTESIAN_POINT('Origin',(0.,58.415,0.));
#49998=CARTESIAN_POINT('',(-2.35454965222883,56.315,1.42077300621495));
#49999=CARTESIAN_POINT('',(-2.35454965222883,55.715,1.42077300621495));
#50000=CARTESIAN_POINT('',(-2.40770034250775,56.315,1.32871331019451));
#50001=CARTESIAN_POINT('Origin',(0.,56.315,0.));
#50002=CARTESIAN_POINT('',(-2.40770034250775,58.415,1.32871331019451));
#50003=CARTESIAN_POINT('',(-2.40770034250775,55.715,1.32871331019451));
#50004=CARTESIAN_POINT('',(-2.56549339577475,58.415,0.990325015455108));
#50005=CARTESIAN_POINT('Origin',(0.,58.415,0.));
#50006=CARTESIAN_POINT('',(-2.56549339577475,56.315,0.990325015455108));
#50007=CARTESIAN_POINT('',(-2.56549339577475,55.715,0.990325015455108));
#50008=CARTESIAN_POINT('',(-2.60185060918886,56.315,0.890434392565551));
#50009=CARTESIAN_POINT('Origin',(0.,56.315,0.));
#50010=CARTESIAN_POINT('',(-2.60185060918886,58.415,0.890434392565551));
#50011=CARTESIAN_POINT('',(-2.60185060918886,55.715,0.890434392565551));
#50012=CARTESIAN_POINT('',(-2.69848592069234,58.415,0.529786500229296));
#50013=CARTESIAN_POINT('Origin',(0.,58.415,0.));
#50014=CARTESIAN_POINT('',(-2.69848592069234,56.315,0.529786500229296));
#50015=CARTESIAN_POINT('',(-2.69848592069234,55.715,0.529786500229296));
#50016=CARTESIAN_POINT('',(-2.71694496170969,56.315,0.425100076500034));
#50017=CARTESIAN_POINT('Origin',(0.,56.315,0.));
#50018=CARTESIAN_POINT('',(-2.71694496170969,58.415,0.425100076500034));
#50019=CARTESIAN_POINT('',(-2.71694496170969,55.715,0.425100076500034));
#50020=CARTESIAN_POINT('',(-2.74948631640946,58.415,0.0531506902789201));
#50021=CARTESIAN_POINT('Origin',(0.,58.415,0.));
#50022=CARTESIAN_POINT('',(-2.74948631640946,55.715,0.0531506902789201));
#50023=CARTESIAN_POINT('Origin',(2.44320081404336,58.715,-0.889252372646741));
#50024=CARTESIAN_POINT('',(2.44320081404336,58.565,-0.88925237264674));
#50025=CARTESIAN_POINT('Ctrl Pts',(2.44320081404336,58.565,-0.88925237264674));
#50026=CARTESIAN_POINT('Ctrl Pts',(2.50263272292269,58.4923524443611,-0.938371787843764));
#50027=CARTESIAN_POINT('Ctrl Pts',(2.56549339577475,58.415,-0.990325015455113));
#50028=CARTESIAN_POINT('',(2.44320081404336,56.315,-0.889252372646741));
#50029=CARTESIAN_POINT('',(2.44320081404336,58.715,-0.889252372646741));
#50030=CARTESIAN_POINT('',(2.44320081404336,56.315,-0.889252372646741));
#50031=CARTESIAN_POINT('Origin',(2.65463165372019,56.315,-0.966206904895016));
#50032=CARTESIAN_POINT('',(2.92078571632913,56.315,-0.892810617817547));
#50033=CARTESIAN_POINT('Origin',(2.92078571632913,58.715,-0.892810617817547));
#50034=CARTESIAN_POINT('Ctrl Pts',(2.60185060918886,58.415,-0.890434392565553));
#50035=CARTESIAN_POINT('Ctrl Pts',(2.52030164906794,58.4923524443612,-0.889826812233457));
#50036=CARTESIAN_POINT('Ctrl Pts',(2.44320081404336,58.565,-0.88925237264674));
#50037=CARTESIAN_POINT('Origin',(2.25166604983954,58.715,-1.3));
#50038=CARTESIAN_POINT('',(2.25166604983954,58.565,-1.3));
#50039=CARTESIAN_POINT('Ctrl Pts',(2.25166604983954,58.565,-1.3));
#50040=CARTESIAN_POINT('Ctrl Pts',(2.301665557543,58.4923524443614,-1.3586934235814));
#50041=CARTESIAN_POINT('Ctrl Pts',(2.35454965222884,58.415,-1.42077300621496));
#50042=CARTESIAN_POINT('',(2.25166604983954,56.315,-1.3));
#50043=CARTESIAN_POINT('',(2.25166604983954,58.715,-1.3));
#50044=CARTESIAN_POINT('',(2.25166604983954,56.315,-1.3));
#50045=CARTESIAN_POINT('Origin',(2.44652176569104,56.315,-1.4125));
#50046=CARTESIAN_POINT('',(2.72137748154254,56.315,-1.38643593539449));
#50047=CARTESIAN_POINT('Origin',(2.72137748154254,58.715,-1.38643593539449));
#50048=CARTESIAN_POINT('Ctrl Pts',(2.40770034250776,58.415,-1.32871331019451));
#50049=CARTESIAN_POINT('Ctrl Pts',(2.32749579954827,58.492352444361,-1.31395413205729));
#50050=CARTESIAN_POINT('Ctrl Pts',(2.25166604983954,58.565,-1.3));
#50051=CARTESIAN_POINT('Origin',(1.99171555210934,58.715,-1.671247785185));
#50052=CARTESIAN_POINT('',(1.99171555210934,58.565,-1.671247785185));
#50053=CARTESIAN_POINT('Ctrl Pts',(1.99171555210934,58.565,-1.671247785185));
#50054=CARTESIAN_POINT('Ctrl Pts',(2.03076344889672,58.4923524443611,-1.73773184717601));
#50055=CARTESIAN_POINT('Ctrl Pts',(2.07206410895956,58.415,-1.8080515281268));
#50056=CARTESIAN_POINT('',(1.99171555210934,56.315,-1.671247785185));
#50057=CARTESIAN_POINT('',(1.99171555210934,58.715,-1.671247785185));
#50058=CARTESIAN_POINT('',(1.99171555210934,56.315,-1.671247785185));
#50059=CARTESIAN_POINT('Origin',(2.16407555181111,56.315,-1.81587499736447));
#50060=CARTESIAN_POINT('',(2.43928156906273,56.315,-1.83793509864491));
#50061=CARTESIAN_POINT('Origin',(2.43928156906273,58.715,-1.83793509864491));
#50062=CARTESIAN_POINT('Ctrl Pts',(2.14039331927472,58.415,-1.72661994625458));
#50063=CARTESIAN_POINT('Ctrl Pts',(2.06397016792854,58.4923524443612,-1.69815762047134));
#50064=CARTESIAN_POINT('Ctrl Pts',(1.99171555210934,58.565,-1.671247785185));
#50065=CARTESIAN_POINT('Origin',(1.671247785185,58.715,-1.99171555210934));
#50066=CARTESIAN_POINT('',(1.671247785185,58.565,-1.99171555210934));
#50067=CARTESIAN_POINT('Ctrl Pts',(1.671247785185,58.565,-1.99171555210934));
#50068=CARTESIAN_POINT('Ctrl Pts',(1.69815762047149,58.4923524443608,-2.06397016792894));
#50069=CARTESIAN_POINT('Ctrl Pts',(1.72661994625458,58.415,-2.14039331927472));
#50070=CARTESIAN_POINT('',(1.671247785185,56.315,-1.99171555210934));
#50071=CARTESIAN_POINT('',(1.671247785185,58.715,-1.99171555210934));
#50072=CARTESIAN_POINT('',(1.671247785185,56.315,-1.99171555210934));
#50073=CARTESIAN_POINT('Origin',(1.81587499736447,56.315,-2.16407555181111));
#50074=CARTESIAN_POINT('',(2.08306932044298,56.315,-2.23358953396304));
#50075=CARTESIAN_POINT('Origin',(2.08306932044298,58.715,-2.23358953396304));
#50076=CARTESIAN_POINT('Ctrl Pts',(1.80805152812679,58.415,-2.07206410895956));
#50077=CARTESIAN_POINT('Ctrl Pts',(1.73773184717629,58.4923524443608,-2.03076344889689));
#50078=CARTESIAN_POINT('Ctrl Pts',(1.671247785185,58.565,-1.99171555210934));
#50079=CARTESIAN_POINT('Origin',(1.3,58.715,-2.25166604983954));
#50080=CARTESIAN_POINT('',(1.3,58.565,-2.25166604983954));
#50081=CARTESIAN_POINT('Ctrl Pts',(1.3,58.565,-2.25166604983954));
#50082=CARTESIAN_POINT('Ctrl Pts',(1.31395413205732,58.4923524443609,-2.32749579954839));
#50083=CARTESIAN_POINT('Ctrl Pts',(1.32871331019451,58.415,-2.40770034250776));
#50084=CARTESIAN_POINT('',(1.3,56.315,-2.25166604983954));
#50085=CARTESIAN_POINT('',(1.3,58.715,-2.25166604983954));
#50086=CARTESIAN_POINT('',(1.3,56.315,-2.25166604983954));
#50087=CARTESIAN_POINT('Origin',(1.4125,56.315,-2.44652176569104));
#50088=CARTESIAN_POINT('',(1.66356406460551,56.315,-2.56137748154254));
#50089=CARTESIAN_POINT('Origin',(1.66356406460551,58.715,-2.56137748154254));
#50090=CARTESIAN_POINT('Ctrl Pts',(1.42077300621496,58.415,-2.35454965222884));
#50091=CARTESIAN_POINT('Ctrl Pts',(1.35869342358154,58.4923524443612,-2.30166555754312));
#50092=CARTESIAN_POINT('Ctrl Pts',(1.3,58.565,-2.25166604983954));
#50093=CARTESIAN_POINT('Origin',(0.889252372646737,58.715,-2.44320081404336));
#50094=CARTESIAN_POINT('',(0.889252372646737,58.565,-2.44320081404336));
#50095=CARTESIAN_POINT('Ctrl Pts',(0.889252372646737,58.565,-2.44320081404336));
#50096=CARTESIAN_POINT('Ctrl Pts',(0.889826812233453,58.4923524443614,-2.52030164906772));
#50097=CARTESIAN_POINT('Ctrl Pts',(0.890434392565549,58.415,-2.60185060918886));
#50098=CARTESIAN_POINT('',(0.889252372646737,56.315,-2.44320081404336));
#50099=CARTESIAN_POINT('',(0.889252372646737,58.715,-2.44320081404336));
#50100=CARTESIAN_POINT('',(0.889252372646737,56.315,-2.44320081404336));
#50101=CARTESIAN_POINT('Origin',(0.966206904895013,56.315,-2.65463165372019));
#50102=CARTESIAN_POINT('',(1.19351225646903,56.315,-2.81133927046491));
#50103=CARTESIAN_POINT('Origin',(1.19351225646903,58.715,-2.81133927046491));
#50104=CARTESIAN_POINT('Ctrl Pts',(0.990325015455109,58.415,-2.56549339577475));
#50105=CARTESIAN_POINT('Ctrl Pts',(0.938371787843648,58.4923524443613,-2.50263272292255));
#50106=CARTESIAN_POINT('Ctrl Pts',(0.889252372646737,58.565,-2.44320081404336));
#50107=CARTESIAN_POINT('Origin',(0.451485261934018,58.715,-2.56050015783174));
#50108=CARTESIAN_POINT('',(0.451485261934018,58.565,-2.56050015783174));
#50109=CARTESIAN_POINT('Ctrl Pts',(0.451485261934018,58.565,-2.56050015783174));
#50110=CARTESIAN_POINT('Ctrl Pts',(0.438662554994094,58.4923524443615,-2.63652940831474));
#50111=CARTESIAN_POINT('Ctrl Pts',(0.425100076500031,58.415,-2.71694496170969));
#50112=CARTESIAN_POINT('',(0.451485261934018,56.315,-2.56050015783174));
#50113=CARTESIAN_POINT('',(0.451485261934018,58.715,-2.56050015783174));
#50114=CARTESIAN_POINT('',(0.451485261934018,56.315,-2.56050015783174));
#50115=CARTESIAN_POINT('Origin',(0.490556101909077,56.315,-2.78208190225949));
#50116=CARTESIAN_POINT('',(0.68719618236609,56.315,-2.97587993826053));
#50117=CARTESIAN_POINT('Origin',(0.68719618236609,58.715,-2.97587993826053));
#50118=CARTESIAN_POINT('Ctrl Pts',(0.529786500229297,58.415,-2.69848592069235));
#50119=CARTESIAN_POINT('Ctrl Pts',(0.48953820017136,58.492352444361,-2.62755865940953));
#50120=CARTESIAN_POINT('Ctrl Pts',(0.451485261934018,58.565,-2.56050015783174));
#50121=CARTESIAN_POINT('Origin',(-4.77612251667468E-16,58.715,-2.6));
#50122=CARTESIAN_POINT('',(-4.77612251667468E-16,58.565,-2.6));
#50123=CARTESIAN_POINT('Ctrl Pts',(-4.77612251667468E-16,58.565,-2.6));
#50124=CARTESIAN_POINT('Ctrl Pts',(-0.0258302420049523,58.4923524443611,
-2.67264755563893));
#50125=CARTESIAN_POINT('Ctrl Pts',(-0.053150690278922,58.415,-2.74948631640947));
#50126=CARTESIAN_POINT('',(-4.77612251667468E-16,56.315,-2.6));
#50127=CARTESIAN_POINT('',(-4.77612251667468E-16,58.715,-2.6));
#50128=CARTESIAN_POINT('',(-4.77612251667468E-16,56.315,-2.6));
#50129=CARTESIAN_POINT('Origin',(-5.18944081138691E-16,56.315,-2.825));
#50130=CARTESIAN_POINT('',(0.159999999999999,56.315,-3.05));
#50131=CARTESIAN_POINT('Origin',(0.159999999999999,58.715,-3.05));
#50132=CARTESIAN_POINT('Ctrl Pts',(0.0531506902789212,58.415,-2.74948631640947));
#50133=CARTESIAN_POINT('Ctrl Pts',(0.0258302420049448,58.4923524443611,
-2.67264755563891));
#50134=CARTESIAN_POINT('Ctrl Pts',(-4.77612251667468E-16,58.565,-2.6));
#50135=CARTESIAN_POINT('Origin',(-0.451485261934019,58.715,-2.56050015783174));
#50136=CARTESIAN_POINT('',(-0.451485261934019,58.565,-2.56050015783174));
#50137=CARTESIAN_POINT('Ctrl Pts',(-0.451485261934019,58.565,-2.56050015783174));
#50138=CARTESIAN_POINT('Ctrl Pts',(-0.489538200171262,58.4923524443612,
-2.62755865940936));
#50139=CARTESIAN_POINT('Ctrl Pts',(-0.529786500229298,58.415,-2.69848592069235));
#50140=CARTESIAN_POINT('',(-0.451485261934019,56.315,-2.56050015783174));
#50141=CARTESIAN_POINT('',(-0.451485261934019,58.715,-2.56050015783174));
#50142=CARTESIAN_POINT('',(-0.451485261934019,56.315,-2.56050015783174));
#50143=CARTESIAN_POINT('Origin',(-0.490556101909078,56.315,-2.78208190225949));
#50144=CARTESIAN_POINT('',(-0.372057701402184,56.315,-3.03144735511394));
#50145=CARTESIAN_POINT('Origin',(-0.372057701402184,58.715,-3.03144735511394));
#50146=CARTESIAN_POINT('Ctrl Pts',(-0.425100076500033,58.415,-2.71694496170969));
#50147=CARTESIAN_POINT('Ctrl Pts',(-0.438662554993996,58.4923524443609,
-2.63652940831532));
#50148=CARTESIAN_POINT('Ctrl Pts',(-0.451485261934019,58.565,-2.56050015783174));
#50149=CARTESIAN_POINT('Origin',(-0.88925237264674,58.715,-2.44320081404336));
#50150=CARTESIAN_POINT('',(-0.88925237264674,58.565,-2.44320081404336));
#50151=CARTESIAN_POINT('Ctrl Pts',(-0.889252372646741,58.565,-2.44320081404336));
#50152=CARTESIAN_POINT('Ctrl Pts',(-0.938371787843537,58.4923524443615,
-2.50263272292241));
#50153=CARTESIAN_POINT('Ctrl Pts',(-0.990325015455113,58.415,-2.56549339577475));
#50154=CARTESIAN_POINT('',(-0.88925237264674,56.315,-2.44320081404336));
#50155=CARTESIAN_POINT('',(-0.88925237264674,58.715,-2.44320081404336));
#50156=CARTESIAN_POINT('',(-0.88925237264674,56.315,-2.44320081404336));
#50157=CARTESIAN_POINT('Origin',(-0.966206904895016,56.315,-2.65463165372019));
#50158=CARTESIAN_POINT('',(-0.892810617817546,56.315,-2.92078571632913));
#50159=CARTESIAN_POINT('Origin',(-0.892810617817546,58.715,-2.92078571632913));
#50160=CARTESIAN_POINT('Ctrl Pts',(-0.890434392565553,58.415,-2.60185060918886));
#50161=CARTESIAN_POINT('Ctrl Pts',(-0.88982681223346,58.4923524443608,-2.52030164906832));
#50162=CARTESIAN_POINT('Ctrl Pts',(-0.88925237264674,58.565,-2.44320081404336));
#50163=CARTESIAN_POINT('Origin',(-1.3,58.715,-2.25166604983954));
#50164=CARTESIAN_POINT('',(-1.3,58.565,-2.25166604983954));
#50165=CARTESIAN_POINT('Ctrl Pts',(-1.3,58.565,-2.25166604983954));
#50166=CARTESIAN_POINT('Ctrl Pts',(-1.35869342358187,58.4923524443608,-2.30166555754341));
#50167=CARTESIAN_POINT('Ctrl Pts',(-1.42077300621496,58.415,-2.35454965222884));
#50168=CARTESIAN_POINT('',(-1.3,56.315,-2.25166604983954));
#50169=CARTESIAN_POINT('',(-1.3,58.715,-2.25166604983954));
#50170=CARTESIAN_POINT('',(-1.3,56.315,-2.25166604983954));
#50171=CARTESIAN_POINT('Origin',(-1.4125,56.315,-2.44652176569104));
#50172=CARTESIAN_POINT('',(-1.38643593539449,56.315,-2.72137748154254));
#50173=CARTESIAN_POINT('Origin',(-1.38643593539449,58.715,-2.72137748154254));
#50174=CARTESIAN_POINT('Ctrl Pts',(-1.32871331019451,58.415,-2.40770034250776));
#50175=CARTESIAN_POINT('Ctrl Pts',(-1.31395413205734,58.4923524443608,-2.3274957995485));
#50176=CARTESIAN_POINT('Ctrl Pts',(-1.3,58.565,-2.25166604983954));
#50177=CARTESIAN_POINT('Origin',(-1.671247785185,58.715,-1.99171555210934));
#50178=CARTESIAN_POINT('',(-1.671247785185,58.565,-1.99171555210934));
#50179=CARTESIAN_POINT('Ctrl Pts',(-1.671247785185,58.565,-1.99171555210934));
#50180=CARTESIAN_POINT('Ctrl Pts',(-1.7377318471757,58.4923524443614,-2.03076344889654));
#50181=CARTESIAN_POINT('Ctrl Pts',(-1.8080515281268,58.415,-2.07206410895956));
#50182=CARTESIAN_POINT('',(-1.671247785185,56.315,-1.99171555210934));
#50183=CARTESIAN_POINT('',(-1.671247785185,58.715,-1.99171555210934));
#50184=CARTESIAN_POINT('',(-1.671247785185,56.315,-1.99171555210934));
#50185=CARTESIAN_POINT('Origin',(-1.81587499736447,56.315,-2.16407555181111));
#50186=CARTESIAN_POINT('',(-1.83793509864491,56.315,-2.43928156906273));
#50187=CARTESIAN_POINT('Origin',(-1.83793509864491,58.715,-2.43928156906273));
#50188=CARTESIAN_POINT('Ctrl Pts',(-1.72661994625458,58.415,-2.14039331927472));
#50189=CARTESIAN_POINT('Ctrl Pts',(-1.69815762047141,58.4923524443611,-2.0639701679287));
#50190=CARTESIAN_POINT('Ctrl Pts',(-1.671247785185,58.565,-1.99171555210934));
#50191=CARTESIAN_POINT('Origin',(-1.99171555210934,58.715,-1.671247785185));
#50192=CARTESIAN_POINT('',(-1.99171555210934,58.565,-1.671247785185));
#50193=CARTESIAN_POINT('Ctrl Pts',(-1.99171555210934,58.565,-1.671247785185));
#50194=CARTESIAN_POINT('Ctrl Pts',(-2.06397016792865,58.4923524443611,-1.69815762047139));
#50195=CARTESIAN_POINT('Ctrl Pts',(-2.14039331927472,58.415,-1.72661994625458));
#50196=CARTESIAN_POINT('',(-1.99171555210934,56.315,-1.671247785185));
#50197=CARTESIAN_POINT('',(-1.99171555210934,58.715,-1.671247785185));
#50198=CARTESIAN_POINT('',(-1.99171555210934,56.315,-1.671247785185));
#50199=CARTESIAN_POINT('Origin',(-2.16407555181111,56.315,-1.81587499736447));
#50200=CARTESIAN_POINT('',(-2.23358953396304,56.315,-2.08306932044298));
#50201=CARTESIAN_POINT('Origin',(-2.23358953396304,58.715,-2.08306932044298));
#50202=CARTESIAN_POINT('Ctrl Pts',(-2.07206410895956,58.415,-1.8080515281268));
#50203=CARTESIAN_POINT('Ctrl Pts',(-2.03076344889677,58.492352444361,-1.73773184717609));
#50204=CARTESIAN_POINT('Ctrl Pts',(-1.99171555210934,58.565,-1.671247785185));
#50205=CARTESIAN_POINT('Origin',(-2.25166604983954,58.715,-1.3));
#50206=CARTESIAN_POINT('',(-2.25166604983954,58.565,-1.3));
#50207=CARTESIAN_POINT('Ctrl Pts',(-2.25166604983954,58.565,-1.3));
#50208=CARTESIAN_POINT('Ctrl Pts',(-2.32749579954808,58.4923524443612,-1.31395413205726));
#50209=CARTESIAN_POINT('Ctrl Pts',(-2.40770034250776,58.415,-1.32871331019451));
#50210=CARTESIAN_POINT('',(-2.25166604983954,56.315,-1.3));
#50211=CARTESIAN_POINT('',(-2.25166604983954,58.715,-1.3));
#50212=CARTESIAN_POINT('',(-2.25166604983954,56.315,-1.3));
#50213=CARTESIAN_POINT('Origin',(-2.44652176569104,56.315,-1.4125));
#50214=CARTESIAN_POINT('',(-2.56137748154254,56.315,-1.66356406460551));
#50215=CARTESIAN_POINT('Origin',(-2.56137748154254,58.715,-1.66356406460551));
#50216=CARTESIAN_POINT('Ctrl Pts',(-2.35454965222884,58.415,-1.42077300621496));
#50217=CARTESIAN_POINT('Ctrl Pts',(-2.30166555754322,58.4923524443611,-1.35869342358165));
#50218=CARTESIAN_POINT('Ctrl Pts',(-2.25166604983954,58.565,-1.3));
#50219=CARTESIAN_POINT('Origin',(-2.44320081404336,58.715,-0.889252372646739));
#50220=CARTESIAN_POINT('',(-2.44320081404336,58.565,-0.889252372646739));
#50221=CARTESIAN_POINT('Ctrl Pts',(-2.44320081404336,58.565,-0.889252372646739));
#50222=CARTESIAN_POINT('Ctrl Pts',(-2.52030164906835,58.4923524443608,-0.889826812233458));
#50223=CARTESIAN_POINT('Ctrl Pts',(-2.60185060918886,58.415,-0.890434392565551));
#50224=CARTESIAN_POINT('',(-2.44320081404336,56.315,-0.889252372646739));
#50225=CARTESIAN_POINT('',(-2.44320081404336,58.715,-0.889252372646739));
#50226=CARTESIAN_POINT('',(-2.44320081404336,56.315,-0.889252372646739));
#50227=CARTESIAN_POINT('Origin',(-2.65463165372019,56.315,-0.966206904895014));
#50228=CARTESIAN_POINT('',(-2.81133927046491,56.315,-1.19351225646903));
#50229=CARTESIAN_POINT('Origin',(-2.81133927046491,58.715,-1.19351225646903));
#50230=CARTESIAN_POINT('Ctrl Pts',(-2.56549339577475,58.415,-0.99032501545511));
#50231=CARTESIAN_POINT('Ctrl Pts',(-2.50263272292257,58.4923524443613,-0.938371787843666));
#50232=CARTESIAN_POINT('Ctrl Pts',(-2.44320081404336,58.565,-0.889252372646739));
#50233=CARTESIAN_POINT('Origin',(-2.56050015783174,58.715,-0.451485261934018));
#50234=CARTESIAN_POINT('',(-2.56050015783174,58.565,-0.451485261934018));
#50235=CARTESIAN_POINT('Ctrl Pts',(-2.56050015783174,58.565,-0.451485261934018));
#50236=CARTESIAN_POINT('Ctrl Pts',(-2.63652940831505,58.4923524443612,-0.438662554994041));
#50237=CARTESIAN_POINT('Ctrl Pts',(-2.71694496170969,58.415,-0.425100076500032));
#50238=CARTESIAN_POINT('',(-2.56050015783174,56.315,-0.451485261934018));
#50239=CARTESIAN_POINT('',(-2.56050015783174,58.715,-0.451485261934018));
#50240=CARTESIAN_POINT('',(-2.56050015783174,56.315,-0.451485261934018));
#50241=CARTESIAN_POINT('Origin',(-2.78208190225949,56.315,-0.490556101909077));
#50242=CARTESIAN_POINT('',(-2.97587993826053,56.315,-0.68719618236609));
#50243=CARTESIAN_POINT('Origin',(-2.97587993826053,58.715,-0.68719618236609));
#50244=CARTESIAN_POINT('Ctrl Pts',(-2.69848592069235,58.415,-0.529786500229297));
#50245=CARTESIAN_POINT('Ctrl Pts',(-2.62755865940921,58.4923524443614,-0.489538200171177));
#50246=CARTESIAN_POINT('Ctrl Pts',(-2.56050015783174,58.565,-0.451485261934018));
#50247=CARTESIAN_POINT('Origin',(-2.6,58.715,3.18408167778312E-16));
#50248=CARTESIAN_POINT('',(-2.6,58.565,3.18408167778312E-16));
#50249=CARTESIAN_POINT('Ctrl Pts',(-2.6,58.565,3.18408167778312E-16));
#50250=CARTESIAN_POINT('Ctrl Pts',(-2.67264755563861,58.4923524443614,0.0258302420048414));
#50251=CARTESIAN_POINT('Ctrl Pts',(-2.74948631640947,58.415,0.0531506902789219));
#50252=CARTESIAN_POINT('',(-2.6,56.315,3.18408167778312E-16));
#50253=CARTESIAN_POINT('',(-2.6,58.715,3.18408167778312E-16));
#50254=CARTESIAN_POINT('',(-2.6,56.315,3.18408167778312E-16));
#50255=CARTESIAN_POINT('Origin',(-2.825,56.315,3.45962720759127E-16));
#50256=CARTESIAN_POINT('',(-3.05,56.315,-0.16));
#50257=CARTESIAN_POINT('Origin',(-3.05,58.715,-0.16));
#50258=CARTESIAN_POINT('Ctrl Pts',(-2.74948631640947,58.415,-0.0531506902789213));
#50259=CARTESIAN_POINT('Ctrl Pts',(-2.67264755563921,58.4923524443608,-0.0258302420050519));
#50260=CARTESIAN_POINT('Ctrl Pts',(-2.6,58.565,3.18408167778312E-16));
#50261=CARTESIAN_POINT('Origin',(-2.56050015783174,58.715,0.45148526193402));
#50262=CARTESIAN_POINT('',(-2.56050015783174,58.565,0.45148526193402));
#50263=CARTESIAN_POINT('Ctrl Pts',(-2.56050015783174,58.565,0.45148526193402));
#50264=CARTESIAN_POINT('Ctrl Pts',(-2.62755865940922,58.4923524443614,0.489538200171184));
#50265=CARTESIAN_POINT('Ctrl Pts',(-2.69848592069235,58.415,0.529786500229298));
#50266=CARTESIAN_POINT('',(-2.56050015783174,56.315,0.45148526193402));
#50267=CARTESIAN_POINT('',(-2.56050015783174,58.715,0.45148526193402));
#50268=CARTESIAN_POINT('',(-2.56050015783174,56.315,0.45148526193402));
#50269=CARTESIAN_POINT('Origin',(-2.78208190225949,56.315,0.490556101909079));
#50270=CARTESIAN_POINT('',(-3.03144735511394,56.315,0.372057701402185));
#50271=CARTESIAN_POINT('Origin',(-3.03144735511394,58.715,0.372057701402185));
#50272=CARTESIAN_POINT('Ctrl Pts',(-2.71694496170969,58.415,0.425100076500033));
#50273=CARTESIAN_POINT('Ctrl Pts',(-2.63652940831533,58.4923524443609,0.438662554993998));
#50274=CARTESIAN_POINT('Ctrl Pts',(-2.56050015783174,58.565,0.45148526193402));
#50275=CARTESIAN_POINT('Origin',(-2.44320081404336,58.715,0.889252372646739));
#50276=CARTESIAN_POINT('',(-2.44320081404336,58.565,0.889252372646739));
#50277=CARTESIAN_POINT('Ctrl Pts',(-2.44320081404336,58.565,0.889252372646739));
#50278=CARTESIAN_POINT('Ctrl Pts',(-2.50263272292248,58.4923524443614,0.938371787843588));
#50279=CARTESIAN_POINT('Ctrl Pts',(-2.56549339577475,58.415,0.990325015455111));
#50280=CARTESIAN_POINT('',(-2.44320081404336,56.315,0.889252372646739));
#50281=CARTESIAN_POINT('',(-2.44320081404336,58.715,0.889252372646739));
#50282=CARTESIAN_POINT('',(-2.44320081404336,56.315,0.889252372646739));
#50283=CARTESIAN_POINT('Origin',(-2.65463165372019,56.315,0.966206904895015));
#50284=CARTESIAN_POINT('',(-2.92078571632913,56.315,0.892810617817545));
#50285=CARTESIAN_POINT('Origin',(-2.92078571632913,58.715,0.892810617817545));
#50286=CARTESIAN_POINT('Ctrl Pts',(-2.60185060918886,58.415,0.890434392565552));
#50287=CARTESIAN_POINT('Ctrl Pts',(-2.52030164906805,58.4923524443611,0.889826812233457));
#50288=CARTESIAN_POINT('Ctrl Pts',(-2.44320081404336,58.565,0.889252372646739));
#50289=CARTESIAN_POINT('Origin',(-2.25166604983954,58.715,1.3));
#50290=CARTESIAN_POINT('',(-2.25166604983954,58.565,1.3));
#50291=CARTESIAN_POINT('Ctrl Pts',(-2.25166604983954,58.565,1.3));
#50292=CARTESIAN_POINT('Ctrl Pts',(-2.30166555754319,58.4923524443611,1.35869342358162));
#50293=CARTESIAN_POINT('Ctrl Pts',(-2.35454965222884,58.415,1.42077300621496));
#50294=CARTESIAN_POINT('',(-2.25166604983954,56.315,1.3));
#50295=CARTESIAN_POINT('',(-2.25166604983954,58.715,1.3));
#50296=CARTESIAN_POINT('',(-2.25166604983954,56.315,1.3));
#50297=CARTESIAN_POINT('Origin',(-2.44652176569104,56.315,1.4125));
#50298=CARTESIAN_POINT('',(-2.72137748154254,56.315,1.38643593539449));
#50299=CARTESIAN_POINT('Origin',(-2.72137748154254,58.715,1.38643593539449));
#50300=CARTESIAN_POINT('Ctrl Pts',(-2.40770034250776,58.415,1.32871331019451));
#50301=CARTESIAN_POINT('Ctrl Pts',(-2.32749579954805,58.4923524443612,1.31395413205725));
#50302=CARTESIAN_POINT('Ctrl Pts',(-2.25166604983954,58.565,1.3));
#50303=CARTESIAN_POINT('Origin',(-1.99171555210934,58.715,1.671247785185));
#50304=CARTESIAN_POINT('',(-1.99171555210934,58.565,1.671247785185));
#50305=CARTESIAN_POINT('Ctrl Pts',(-1.99171555210934,58.565,1.671247785185));
#50306=CARTESIAN_POINT('Ctrl Pts',(-2.03076344889688,58.4923524443608,1.73773184717629));
#50307=CARTESIAN_POINT('Ctrl Pts',(-2.07206410895956,58.415,1.8080515281268));
#50308=CARTESIAN_POINT('',(-1.99171555210934,56.315,1.671247785185));
#50309=CARTESIAN_POINT('',(-1.99171555210934,58.715,1.671247785185));
#50310=CARTESIAN_POINT('',(-1.99171555210934,56.315,1.671247785185));
#50311=CARTESIAN_POINT('Origin',(-2.16407555181111,56.315,1.81587499736447));
#50312=CARTESIAN_POINT('',(-2.43928156906273,56.315,1.83793509864491));
#50313=CARTESIAN_POINT('Origin',(-2.43928156906273,58.715,1.83793509864491));
#50314=CARTESIAN_POINT('Ctrl Pts',(-2.14039331927472,58.415,1.72661994625458));
#50315=CARTESIAN_POINT('Ctrl Pts',(-2.06397016792831,58.4923524443615,1.69815762047126));
#50316=CARTESIAN_POINT('Ctrl Pts',(-1.99171555210934,58.565,1.671247785185));
#50317=CARTESIAN_POINT('Origin',(-1.671247785185,58.715,1.99171555210934));
#50318=CARTESIAN_POINT('',(-1.671247785185,58.565,1.99171555210934));
#50319=CARTESIAN_POINT('Ctrl Pts',(-1.671247785185,58.565,1.99171555210934));
#50320=CARTESIAN_POINT('Ctrl Pts',(-1.69815762047144,58.492352444361,2.06397016792879));
#50321=CARTESIAN_POINT('Ctrl Pts',(-1.72661994625458,58.415,2.14039331927472));
#50322=CARTESIAN_POINT('',(-1.671247785185,56.315,1.99171555210934));
#50323=CARTESIAN_POINT('',(-1.671247785185,58.715,1.99171555210934));
#50324=CARTESIAN_POINT('',(-1.671247785185,56.315,1.99171555210934));
#50325=CARTESIAN_POINT('Origin',(-1.81587499736447,56.315,2.16407555181111));
#50326=CARTESIAN_POINT('',(-2.08306932044298,56.315,2.23358953396304));
#50327=CARTESIAN_POINT('Origin',(-2.08306932044298,58.715,2.23358953396304));
#50328=CARTESIAN_POINT('Ctrl Pts',(-1.8080515281268,58.415,2.07206410895956));
#50329=CARTESIAN_POINT('Ctrl Pts',(-1.73773184717619,58.4923524443609,2.03076344889682));
#50330=CARTESIAN_POINT('Ctrl Pts',(-1.671247785185,58.565,1.99171555210934));
#50331=CARTESIAN_POINT('Origin',(-1.3,58.715,2.25166604983954));
#50332=CARTESIAN_POINT('',(-1.3,58.565,2.25166604983954));
#50333=CARTESIAN_POINT('Ctrl Pts',(-1.3,58.565,2.25166604983954));
#50334=CARTESIAN_POINT('Ctrl Pts',(-1.31395413205728,58.4923524443611,2.32749579954818));
#50335=CARTESIAN_POINT('Ctrl Pts',(-1.32871331019451,58.415,2.40770034250776));
#50336=CARTESIAN_POINT('',(-1.3,56.315,2.25166604983954));
#50337=CARTESIAN_POINT('',(-1.3,58.715,2.25166604983954));
#50338=CARTESIAN_POINT('',(-1.3,56.315,2.25166604983954));
#50339=CARTESIAN_POINT('Origin',(-1.4125,56.315,2.44652176569104));
#50340=CARTESIAN_POINT('',(-1.66356406460551,56.315,2.56137748154254));
#50341=CARTESIAN_POINT('Origin',(-1.66356406460551,58.715,2.56137748154254));
#50342=CARTESIAN_POINT('Ctrl Pts',(-1.42077300621496,58.415,2.35454965222884));
#50343=CARTESIAN_POINT('Ctrl Pts',(-1.35869342358169,58.492352444361,2.30166555754325));
#50344=CARTESIAN_POINT('Ctrl Pts',(-1.3,58.565,2.25166604983954));
#50345=CARTESIAN_POINT('Origin',(-0.889252372646739,58.715,2.44320081404336));
#50346=CARTESIAN_POINT('',(-0.889252372646739,58.565,2.44320081404336));
#50347=CARTESIAN_POINT('Ctrl Pts',(-0.889252372646739,58.565,2.44320081404336));
#50348=CARTESIAN_POINT('Ctrl Pts',(-0.889826812233454,58.4923524443614,
2.52030164906776));
#50349=CARTESIAN_POINT('Ctrl Pts',(-0.890434392565551,58.415,2.60185060918886));
#50350=CARTESIAN_POINT('',(-0.889252372646739,56.315,2.44320081404336));
#50351=CARTESIAN_POINT('',(-0.889252372646739,58.715,2.44320081404336));
#50352=CARTESIAN_POINT('',(-0.889252372646739,56.315,2.44320081404336));
#50353=CARTESIAN_POINT('Origin',(-0.966206904895014,56.315,2.65463165372019));
#50354=CARTESIAN_POINT('',(-1.19351225646904,56.315,2.81133927046491));
#50355=CARTESIAN_POINT('Origin',(-1.19351225646904,58.715,2.81133927046491));
#50356=CARTESIAN_POINT('Ctrl Pts',(-0.99032501545511,58.415,2.56549339577475));
#50357=CARTESIAN_POINT('Ctrl Pts',(-0.938371787843834,58.492352444361,2.50263272292277));
#50358=CARTESIAN_POINT('Ctrl Pts',(-0.889252372646739,58.565,2.44320081404336));
#50359=CARTESIAN_POINT('Origin',(-0.451485261934019,58.715,2.56050015783174));
#50360=CARTESIAN_POINT('',(-0.451485261934019,58.565,2.56050015783174));
#50361=CARTESIAN_POINT('Ctrl Pts',(-0.451485261934019,58.565,2.56050015783174));
#50362=CARTESIAN_POINT('Ctrl Pts',(-0.438662554993981,58.4923524443609,
2.63652940831541));
#50363=CARTESIAN_POINT('Ctrl Pts',(-0.425100076500032,58.415,2.71694496170969));
#50364=CARTESIAN_POINT('',(-0.451485261934019,56.315,2.56050015783174));
#50365=CARTESIAN_POINT('',(-0.451485261934019,58.715,2.56050015783174));
#50366=CARTESIAN_POINT('',(-0.451485261934019,56.315,2.56050015783174));
#50367=CARTESIAN_POINT('Origin',(-0.490556101909078,56.315,2.78208190225949));
#50368=CARTESIAN_POINT('',(-0.687196182366091,56.315,2.97587993826053));
#50369=CARTESIAN_POINT('Origin',(-0.687196182366091,58.715,2.97587993826053));
#50370=CARTESIAN_POINT('Ctrl Pts',(-0.529786500229298,58.415,2.69848592069235));
#50371=CARTESIAN_POINT('Ctrl Pts',(-0.489538200171253,58.4923524443612,
2.62755865940935));
#50372=CARTESIAN_POINT('Ctrl Pts',(-0.451485261934019,58.565,2.56050015783174));
#50373=CARTESIAN_POINT('Origin',(1.59204083889156E-16,58.715,2.6));
#50374=CARTESIAN_POINT('',(1.59204083889156E-16,58.565,2.6));
#50375=CARTESIAN_POINT('Ctrl Pts',(1.59204083889156E-16,58.565,2.6));
#50376=CARTESIAN_POINT('Ctrl Pts',(0.0258302420049794,58.492352444361,2.67264755563901));
#50377=CARTESIAN_POINT('Ctrl Pts',(0.0531506902789217,58.415,2.74948631640947));
#50378=CARTESIAN_POINT('',(1.59204083889156E-16,56.315,2.6));
#50379=CARTESIAN_POINT('',(1.59204083889156E-16,58.715,2.6));
#50380=CARTESIAN_POINT('',(1.59204083889156E-16,56.315,2.6));
#50381=CARTESIAN_POINT('Origin',(1.72981360379564E-16,56.315,2.825));
#50382=CARTESIAN_POINT('',(-0.16,56.315,3.05));
#50383=CARTESIAN_POINT('Origin',(-0.16,58.715,3.05));
#50384=CARTESIAN_POINT('Ctrl Pts',(-0.0531506902789213,58.415,2.74948631640947));
#50385=CARTESIAN_POINT('Ctrl Pts',(-0.0258302420049886,58.492352444361,
2.67264755563903));
#50386=CARTESIAN_POINT('Ctrl Pts',(1.59204083889156E-16,58.565,2.6));
#50387=CARTESIAN_POINT('Origin',(0.451485261934019,58.715,2.56050015783174));
#50388=CARTESIAN_POINT('',(0.451485261934019,58.565,2.56050015783174));
#50389=CARTESIAN_POINT('Ctrl Pts',(0.451485261934019,58.565,2.56050015783174));
#50390=CARTESIAN_POINT('Ctrl Pts',(0.489538200171364,58.492352444361,2.62755865940954));
#50391=CARTESIAN_POINT('Ctrl Pts',(0.529786500229298,58.415,2.69848592069235));
#50392=CARTESIAN_POINT('',(0.451485261934019,56.315,2.56050015783174));
#50393=CARTESIAN_POINT('',(0.451485261934019,58.715,2.56050015783174));
#50394=CARTESIAN_POINT('',(0.451485261934019,56.315,2.56050015783174));
#50395=CARTESIAN_POINT('Origin',(0.490556101909078,56.315,2.78208190225949));
#50396=CARTESIAN_POINT('',(0.372057701402184,56.315,3.03144735511394));
#50397=CARTESIAN_POINT('Origin',(0.372057701402184,58.715,3.03144735511394));
#50398=CARTESIAN_POINT('Ctrl Pts',(0.425100076500033,58.415,2.71694496170969));
#50399=CARTESIAN_POINT('Ctrl Pts',(0.438662554994009,58.492352444361,2.63652940831525));
#50400=CARTESIAN_POINT('Ctrl Pts',(0.451485261934019,58.565,2.56050015783174));
#50401=CARTESIAN_POINT('Origin',(0.889252372646739,58.715,2.44320081404336));
#50402=CARTESIAN_POINT('',(0.889252372646739,58.565,2.44320081404336));
#50403=CARTESIAN_POINT('Ctrl Pts',(0.889252372646739,58.565,2.44320081404336));
#50404=CARTESIAN_POINT('Ctrl Pts',(0.938371787844005,58.4923524443608,2.50263272292298));
#50405=CARTESIAN_POINT('Ctrl Pts',(0.990325015455111,58.415,2.56549339577475));
#50406=CARTESIAN_POINT('',(0.889252372646739,56.315,2.44320081404336));
#50407=CARTESIAN_POINT('',(0.889252372646739,58.715,2.44320081404336));
#50408=CARTESIAN_POINT('',(0.889252372646739,56.315,2.44320081404336));
#50409=CARTESIAN_POINT('Origin',(0.966206904895014,56.315,2.65463165372019));
#50410=CARTESIAN_POINT('',(0.892810617817545,56.315,2.92078571632913));
#50411=CARTESIAN_POINT('Origin',(0.892810617817545,58.715,2.92078571632913));
#50412=CARTESIAN_POINT('Ctrl Pts',(0.890434392565551,58.415,2.60185060918886));
#50413=CARTESIAN_POINT('Ctrl Pts',(0.889826812233459,58.4923524443609,2.52030164906829));
#50414=CARTESIAN_POINT('Ctrl Pts',(0.889252372646739,58.565,2.44320081404336));
#50415=CARTESIAN_POINT('Origin',(1.3,58.715,2.25166604983954));
#50416=CARTESIAN_POINT('',(1.3,58.565,2.25166604983954));
#50417=CARTESIAN_POINT('Ctrl Pts',(1.3,58.565,2.25166604983954));
#50418=CARTESIAN_POINT('Ctrl Pts',(1.35869342358162,58.4923524443611,2.30166555754319));
#50419=CARTESIAN_POINT('Ctrl Pts',(1.42077300621496,58.415,2.35454965222884));
#50420=CARTESIAN_POINT('',(1.3,56.315,2.25166604983954));
#50421=CARTESIAN_POINT('',(1.3,58.715,2.25166604983954));
#50422=CARTESIAN_POINT('',(1.3,56.315,2.25166604983954));
#50423=CARTESIAN_POINT('Origin',(1.4125,56.315,2.44652176569104));
#50424=CARTESIAN_POINT('',(1.38643593539449,56.315,2.72137748154254));
#50425=CARTESIAN_POINT('Origin',(1.38643593539449,58.715,2.72137748154254));
#50426=CARTESIAN_POINT('Ctrl Pts',(1.32871331019451,58.415,2.40770034250776));
#50427=CARTESIAN_POINT('Ctrl Pts',(1.31395413205722,58.4923524443614,2.32749579954787));
#50428=CARTESIAN_POINT('Ctrl Pts',(1.3,58.565,2.25166604983954));
#50429=CARTESIAN_POINT('Origin',(1.671247785185,58.715,1.99171555210934));
#50430=CARTESIAN_POINT('',(1.671247785185,58.565,1.99171555210934));
#50431=CARTESIAN_POINT('Ctrl Pts',(1.671247785185,58.565,1.99171555210934));
#50432=CARTESIAN_POINT('Ctrl Pts',(1.73773184717615,58.4923524443609,2.0307634488968));
#50433=CARTESIAN_POINT('Ctrl Pts',(1.8080515281268,58.415,2.07206410895956));
#50434=CARTESIAN_POINT('',(1.671247785185,56.315,1.99171555210934));
#50435=CARTESIAN_POINT('',(1.671247785185,58.715,1.99171555210934));
#50436=CARTESIAN_POINT('',(1.671247785185,56.315,1.99171555210934));
#50437=CARTESIAN_POINT('Origin',(1.81587499736447,56.315,2.16407555181111));
#50438=CARTESIAN_POINT('',(1.83793509864491,56.315,2.43928156906273));
#50439=CARTESIAN_POINT('Origin',(1.83793509864491,58.715,2.43928156906273));
#50440=CARTESIAN_POINT('Ctrl Pts',(1.72661994625458,58.415,2.14039331927472));
#50441=CARTESIAN_POINT('Ctrl Pts',(1.69815762047144,58.492352444361,2.06397016792879));
#50442=CARTESIAN_POINT('Ctrl Pts',(1.671247785185,58.565,1.99171555210934));
#50443=CARTESIAN_POINT('Origin',(1.99171555210934,58.715,1.671247785185));
#50444=CARTESIAN_POINT('',(1.99171555210934,58.565,1.671247785185));
#50445=CARTESIAN_POINT('Ctrl Pts',(1.99171555210934,58.565,1.671247785185));
#50446=CARTESIAN_POINT('Ctrl Pts',(2.06397016792865,58.4923524443611,1.69815762047139));
#50447=CARTESIAN_POINT('Ctrl Pts',(2.14039331927472,58.415,1.72661994625458));
#50448=CARTESIAN_POINT('',(1.99171555210934,56.315,1.671247785185));
#50449=CARTESIAN_POINT('',(1.99171555210934,58.715,1.671247785185));
#50450=CARTESIAN_POINT('',(1.99171555210934,56.315,1.671247785185));
#50451=CARTESIAN_POINT('Origin',(2.16407555181111,56.315,1.81587499736447));
#50452=CARTESIAN_POINT('',(2.23358953396304,56.315,2.08306932044298));
#50453=CARTESIAN_POINT('Origin',(2.23358953396304,58.715,2.08306932044298));
#50454=CARTESIAN_POINT('Ctrl Pts',(2.07206410895956,58.415,1.8080515281268));
#50455=CARTESIAN_POINT('Ctrl Pts',(2.03076344889677,58.492352444361,1.73773184717609));
#50456=CARTESIAN_POINT('Ctrl Pts',(1.99171555210934,58.565,1.671247785185));
#50457=CARTESIAN_POINT('Origin',(2.25166604983954,58.715,1.3));
#50458=CARTESIAN_POINT('',(2.25166604983954,58.565,1.3));
#50459=CARTESIAN_POINT('Ctrl Pts',(2.25166604983954,58.565,1.3));
#50460=CARTESIAN_POINT('Ctrl Pts',(2.32749579954822,58.492352444361,1.31395413205728));
#50461=CARTESIAN_POINT('Ctrl Pts',(2.40770034250776,58.415,1.32871331019451));
#50462=CARTESIAN_POINT('',(2.25166604983954,56.315,1.3));
#50463=CARTESIAN_POINT('',(2.25166604983954,58.715,1.3));
#50464=CARTESIAN_POINT('',(2.25166604983954,56.315,1.3));
#50465=CARTESIAN_POINT('Origin',(2.44652176569104,56.315,1.4125));
#50466=CARTESIAN_POINT('',(2.56137748154254,56.315,1.66356406460551));
#50467=CARTESIAN_POINT('Origin',(2.56137748154254,58.715,1.66356406460551));
#50468=CARTESIAN_POINT('Ctrl Pts',(2.35454965222884,58.415,1.42077300621496));
#50469=CARTESIAN_POINT('Ctrl Pts',(2.30166555754331,58.4923524443609,1.35869342358176));
#50470=CARTESIAN_POINT('Ctrl Pts',(2.25166604983954,58.565,1.3));
#50471=CARTESIAN_POINT('Origin',(2.44320081404336,58.715,0.889252372646739));
#50472=CARTESIAN_POINT('',(2.44320081404336,58.565,0.889252372646739));
#50473=CARTESIAN_POINT('Ctrl Pts',(2.44320081404336,58.565,0.889252372646739));
#50474=CARTESIAN_POINT('Ctrl Pts',(2.52030164906804,58.4923524443611,0.889826812233456));
#50475=CARTESIAN_POINT('Ctrl Pts',(2.60185060918886,58.415,0.890434392565551));
#50476=CARTESIAN_POINT('',(2.44320081404336,56.315,0.889252372646739));
#50477=CARTESIAN_POINT('',(2.44320081404336,58.715,0.889252372646739));
#50478=CARTESIAN_POINT('',(2.44320081404336,56.315,0.889252372646739));
#50479=CARTESIAN_POINT('Origin',(2.65463165372019,56.315,0.966206904895014));
#50480=CARTESIAN_POINT('',(2.81133927046491,56.315,1.19351225646904));
#50481=CARTESIAN_POINT('Origin',(2.81133927046491,58.715,1.19351225646904));
#50482=CARTESIAN_POINT('Ctrl Pts',(2.56549339577475,58.415,0.99032501545511));
#50483=CARTESIAN_POINT('Ctrl Pts',(2.50263272292278,58.492352444361,0.93837178784384));
#50484=CARTESIAN_POINT('Ctrl Pts',(2.44320081404336,58.565,0.889252372646739));
#50485=CARTESIAN_POINT('Origin',(2.56050015783174,58.715,0.451485261934019));
#50486=CARTESIAN_POINT('',(2.56050015783174,58.565,0.451485261934019));
#50487=CARTESIAN_POINT('Ctrl Pts',(2.56050015783174,58.565,0.451485261934019));
#50488=CARTESIAN_POINT('Ctrl Pts',(2.63652940831479,58.4923524443615,0.438662554994086));
#50489=CARTESIAN_POINT('Ctrl Pts',(2.71694496170969,58.415,0.425100076500033));
#50490=CARTESIAN_POINT('',(2.56050015783174,56.315,0.451485261934019));
#50491=CARTESIAN_POINT('',(2.56050015783174,58.715,0.451485261934019));
#50492=CARTESIAN_POINT('',(2.56050015783174,56.315,0.451485261934019));
#50493=CARTESIAN_POINT('Origin',(2.78208190225949,56.315,0.490556101909078));
#50494=CARTESIAN_POINT('',(2.97587993826053,56.315,0.687196182366091));
#50495=CARTESIAN_POINT('Origin',(2.97587993826053,58.715,0.687196182366091));
#50496=CARTESIAN_POINT('Ctrl Pts',(2.69848592069235,58.415,0.529786500229298));
#50497=CARTESIAN_POINT('Ctrl Pts',(2.62755865940969,58.4923524443609,0.489538200171446));
#50498=CARTESIAN_POINT('Ctrl Pts',(2.56050015783174,58.565,0.451485261934019));
#50499=CARTESIAN_POINT('Origin',(2.6,58.715,0.));
#50500=CARTESIAN_POINT('',(2.6,58.565,0.));
#50501=CARTESIAN_POINT('Ctrl Pts',(2.6,58.565,0.));
#50502=CARTESIAN_POINT('Ctrl Pts',(2.67264755563906,58.4923524443609,-0.0258302420049978));
#50503=CARTESIAN_POINT('Ctrl Pts',(2.74948631640947,58.415,-0.0531506902789213));
#50504=CARTESIAN_POINT('',(2.6,56.315,0.));
#50505=CARTESIAN_POINT('',(2.6,58.715,0.));
#50506=CARTESIAN_POINT('',(2.6,56.315,0.));
#50507=CARTESIAN_POINT('Origin',(2.825,56.315,0.));
#50508=CARTESIAN_POINT('',(3.05,56.315,0.16));
#50509=CARTESIAN_POINT('Origin',(3.05,58.715,0.16));
#50510=CARTESIAN_POINT('Ctrl Pts',(2.74948631640947,58.415,0.0531506902789213));
#50511=CARTESIAN_POINT('Ctrl Pts',(2.67264755563908,58.4923524443609,0.0258302420050066));
#50512=CARTESIAN_POINT('Ctrl Pts',(2.6,58.565,0.));
#50513=CARTESIAN_POINT('Origin',(0.,55.915,0.));
#50514=CARTESIAN_POINT('Origin',(-3.12284933782575E-16,55.915,-2.55));
#50515=CARTESIAN_POINT('Origin',(0.,58.565,0.));
#50516=CARTESIAN_POINT('',(-2.45,58.715,-3.00038465791102E-16));
#50517=CARTESIAN_POINT('',(-2.6,58.565,-3.18408167778312E-16));
#50518=CARTESIAN_POINT('Origin',(0.,58.715,0.));
#50519=CARTESIAN_POINT('Origin',(0.,58.715,0.));
#50520=CARTESIAN_POINT('',(-1.59337567297407,58.715,-1.95132241774696E-16));
#50521=CARTESIAN_POINT('Origin',(0.,58.715,0.));
#50522=CARTESIAN_POINT('Origin',(0.,58.615,0.));
#50523=CARTESIAN_POINT('',(-1.39034491479519,58.515,-0.0918519675297062));
#50524=CARTESIAN_POINT('',(-1.44337567297406,58.565,1.76762539787484E-16));
#50525=CARTESIAN_POINT('Ctrl Pts',(-1.39034491479519,58.515,-0.0918519675297066));
#50526=CARTESIAN_POINT('Ctrl Pts',(-1.41639293922685,58.5380172662528,-0.0467354657772785));
#50527=CARTESIAN_POINT('Ctrl Pts',(-1.44337567297406,58.565,1.76762539787484E-16));
#50528=CARTESIAN_POINT('',(-0.774718594665906,58.515,-1.15814803247029));
#50529=CARTESIAN_POINT('Origin',(0.,58.515,0.));
#50530=CARTESIAN_POINT('',(-0.721687836487033,58.565,-1.25));
#50531=CARTESIAN_POINT('Ctrl Pts',(-0.721687836487033,58.565,-1.25));
#50532=CARTESIAN_POINT('Ctrl Pts',(-0.748670570234245,58.5380172662528,
-1.20326453422273));
#50533=CARTESIAN_POINT('Ctrl Pts',(-0.774718594665906,58.515,-1.15814803247029));
#50534=CARTESIAN_POINT('',(-0.615626320129288,58.515,-1.25));
#50535=CARTESIAN_POINT('Ctrl Pts',(-0.615626320129287,58.515,-1.25));
#50536=CARTESIAN_POINT('Ctrl Pts',(-0.667722368992606,58.5380172662528,
-1.25));
#50537=CARTESIAN_POINT('Ctrl Pts',(-0.721687836487033,58.565,-1.25));
#50538=CARTESIAN_POINT('',(0.615626320129287,58.515,-1.25));
#50539=CARTESIAN_POINT('Origin',(0.,58.515,0.));
#50540=CARTESIAN_POINT('',(0.721687836487032,58.565,-1.25));
#50541=CARTESIAN_POINT('Ctrl Pts',(0.721687836487032,58.565,-1.25));
#50542=CARTESIAN_POINT('Ctrl Pts',(0.667722368992606,58.5380172662528,-1.25));
#50543=CARTESIAN_POINT('Ctrl Pts',(0.615626320129287,58.515,-1.25));
#50544=CARTESIAN_POINT('',(0.774718594665905,58.515,-1.15814803247029));
#50545=CARTESIAN_POINT('Ctrl Pts',(0.774718594665906,58.515,-1.15814803247029));
#50546=CARTESIAN_POINT('Ctrl Pts',(0.748670570234245,58.5380172662528,-1.20326453422273));
#50547=CARTESIAN_POINT('Ctrl Pts',(0.721687836487032,58.565,-1.25));
#50548=CARTESIAN_POINT('',(1.39034491479519,58.515,-0.0918519675297066));
#50549=CARTESIAN_POINT('Origin',(0.,58.515,0.));
#50550=CARTESIAN_POINT('',(1.44337567297406,58.565,0.));
#50551=CARTESIAN_POINT('Ctrl Pts',(1.44337567297406,58.565,0.));
#50552=CARTESIAN_POINT('Ctrl Pts',(1.41639293922685,58.5380172662528,-0.0467354657772708));
#50553=CARTESIAN_POINT('Ctrl Pts',(1.39034491479519,58.515,-0.0918519675297073));
#50554=CARTESIAN_POINT('',(1.39034491479519,58.515,0.0918519675297068));
#50555=CARTESIAN_POINT('Ctrl Pts',(1.39034491479519,58.515,0.0918519675297077));
#50556=CARTESIAN_POINT('Ctrl Pts',(1.41639293922685,58.5380172662528,0.0467354657772747));
#50557=CARTESIAN_POINT('Ctrl Pts',(1.44337567297406,58.565,0.));
#50558=CARTESIAN_POINT('',(0.774718594665905,58.515,1.15814803247029));
#50559=CARTESIAN_POINT('Origin',(0.,58.515,0.));
#50560=CARTESIAN_POINT('',(0.721687836487032,58.565,1.25));
#50561=CARTESIAN_POINT('Ctrl Pts',(0.721687836487032,58.565,1.25));
#50562=CARTESIAN_POINT('Ctrl Pts',(0.748670570234242,58.5380172662528,1.20326453422273));
#50563=CARTESIAN_POINT('Ctrl Pts',(0.774718594665906,58.515,1.15814803247029));
#50564=CARTESIAN_POINT('',(0.615626320129287,58.515,1.25));
#50565=CARTESIAN_POINT('Ctrl Pts',(0.615626320129287,58.515,1.25));
#50566=CARTESIAN_POINT('Ctrl Pts',(0.667722368992607,58.5380172662528,1.25));
#50567=CARTESIAN_POINT('Ctrl Pts',(0.721687836487032,58.565,1.25));
#50568=CARTESIAN_POINT('',(-0.615626320129287,58.515,1.25));
#50569=CARTESIAN_POINT('Origin',(0.,58.515,0.));
#50570=CARTESIAN_POINT('',(-0.721687836487032,58.565,1.25));
#50571=CARTESIAN_POINT('Ctrl Pts',(-0.721687836487032,58.565,1.25));
#50572=CARTESIAN_POINT('Ctrl Pts',(-0.667722368992609,58.5380172662528,
1.25));
#50573=CARTESIAN_POINT('Ctrl Pts',(-0.615626320129286,58.515,1.25));
#50574=CARTESIAN_POINT('',(-0.774718594665904,58.515,1.15814803247029));
#50575=CARTESIAN_POINT('Ctrl Pts',(-0.774718594665905,58.515,1.15814803247029));
#50576=CARTESIAN_POINT('Ctrl Pts',(-0.748670570234242,58.5380172662528,
1.20326453422273));
#50577=CARTESIAN_POINT('Ctrl Pts',(-0.721687836487032,58.565,1.25));
#50578=CARTESIAN_POINT('',(-1.39034491479519,58.515,0.0918519675297067));
#50579=CARTESIAN_POINT('Origin',(0.,58.515,0.));
#50580=CARTESIAN_POINT('Ctrl Pts',(-1.44337567297406,58.565,1.76762539787484E-16));
#50581=CARTESIAN_POINT('Ctrl Pts',(-1.41639293922685,58.5380172662528,0.0467354657772748));
#50582=CARTESIAN_POINT('Ctrl Pts',(-1.39034491479519,58.515,0.0918519675297071));
#50583=CARTESIAN_POINT('',(-1.49337567297406,58.615,1.82885773783221E-16));
#50584=CARTESIAN_POINT('Origin',(0.,58.615,0.));
#50585=CARTESIAN_POINT('',(0.615626320129287,58.715,-1.25));
#50586=CARTESIAN_POINT('',(0.615626320129287,58.615,-1.25));
#50587=CARTESIAN_POINT('',(-0.615626320129288,58.715,-1.25));
#50588=CARTESIAN_POINT('',(-0.615626320129288,58.615,-1.25));
#50589=CARTESIAN_POINT('Origin',(0.,58.715,0.));
#50590=CARTESIAN_POINT('Origin',(0.,58.615,0.));
#50591=CARTESIAN_POINT('',(1.39034491479519,58.715,-0.0918519675297066));
#50592=CARTESIAN_POINT('',(1.39034491479519,58.615,-0.0918519675297066));
#50593=CARTESIAN_POINT('',(0.774718594665905,58.715,-1.15814803247029));
#50594=CARTESIAN_POINT('',(0.774718594665905,58.615,-1.15814803247029));
#50595=CARTESIAN_POINT('Origin',(0.,58.715,0.));
#50596=CARTESIAN_POINT('Origin',(0.,58.615,0.));
#50597=CARTESIAN_POINT('',(-1.39034491479519,58.715,-0.0918519675297062));
#50598=CARTESIAN_POINT('',(-1.39034491479519,58.615,-0.0918519675297062));
#50599=CARTESIAN_POINT('',(-0.774718594665906,58.715,-1.15814803247029));
#50600=CARTESIAN_POINT('Origin',(0.,58.715,0.));
#50601=CARTESIAN_POINT('',(-0.774718594665906,58.615,-1.15814803247029));
#50602=CARTESIAN_POINT('Origin',(0.,58.615,0.));
#50603=CARTESIAN_POINT('',(0.774718594665905,58.715,1.15814803247029));
#50604=CARTESIAN_POINT('',(0.774718594665905,58.615,1.15814803247029));
#50605=CARTESIAN_POINT('',(1.39034491479519,58.715,0.0918519675297068));
#50606=CARTESIAN_POINT('',(1.39034491479519,58.615,0.0918519675297068));
#50607=CARTESIAN_POINT('Origin',(0.,58.715,0.));
#50608=CARTESIAN_POINT('Origin',(0.,58.615,0.));
#50609=CARTESIAN_POINT('',(-0.774718594665904,58.715,1.15814803247029));
#50610=CARTESIAN_POINT('',(-0.774718594665904,58.615,1.15814803247029));
#50611=CARTESIAN_POINT('',(-1.39034491479519,58.715,0.0918519675297067));
#50612=CARTESIAN_POINT('Origin',(0.,58.715,0.));
#50613=CARTESIAN_POINT('',(-1.39034491479519,58.615,0.0918519675297067));
#50614=CARTESIAN_POINT('Origin',(0.,58.615,0.));
#50615=CARTESIAN_POINT('',(0.615626320129287,58.715,1.25));
#50616=CARTESIAN_POINT('',(0.615626320129287,58.615,1.25));
#50617=CARTESIAN_POINT('',(-0.615626320129287,58.715,1.25));
#50618=CARTESIAN_POINT('Origin',(0.,58.715,0.));
#50619=CARTESIAN_POINT('',(-0.615626320129287,58.615,1.25));
#50620=CARTESIAN_POINT('Origin',(1.44337567297406,58.715,0.));
#50621=CARTESIAN_POINT('',(1.26295371385231,58.715,0.3125));
#50622=CARTESIAN_POINT('',(1.44337567297406,57.415,0.));
#50623=CARTESIAN_POINT('',(1.44337567297406,58.715,0.));
#50624=CARTESIAN_POINT('',(0.721687836487032,57.415,1.25));
#50625=CARTESIAN_POINT('',(1.44337567297406,57.415,0.));
#50626=CARTESIAN_POINT('',(0.721687836487032,58.715,1.25));
#50627=CARTESIAN_POINT('Origin',(0.721687836487032,58.715,-1.25));
#50628=CARTESIAN_POINT('',(0.902109795608791,58.715,-0.9375));
#50629=CARTESIAN_POINT('',(0.721687836487032,57.415,-1.25));
#50630=CARTESIAN_POINT('',(0.721687836487032,58.715,-1.25));
#50631=CARTESIAN_POINT('',(0.721687836487032,57.415,-1.25));
#50632=CARTESIAN_POINT('Origin',(-0.721687836487033,58.715,-1.25));
#50633=CARTESIAN_POINT('',(-0.360843918243517,58.715,-1.25));
#50634=CARTESIAN_POINT('',(-0.721687836487033,57.415,-1.25));
#50635=CARTESIAN_POINT('',(-0.721687836487033,58.715,-1.25));
#50636=CARTESIAN_POINT('',(-0.721687836487033,57.415,-1.25));
#50637=CARTESIAN_POINT('Origin',(0.,58.715,0.));
#50638=CARTESIAN_POINT('Origin',(0.,58.715,0.));
#50639=CARTESIAN_POINT('Origin',(0.,58.715,0.));
#50640=CARTESIAN_POINT('',(-1.26295371385231,58.715,-0.3125));
#50641=CARTESIAN_POINT('Origin',(0.,58.715,0.));
#50642=CARTESIAN_POINT('Origin',(0.,58.715,0.));
#50643=CARTESIAN_POINT('',(-0.90210979560879,58.715,0.9375));
#50644=CARTESIAN_POINT('Origin',(0.,58.715,0.));
#50645=CARTESIAN_POINT('',(0.360843918243516,58.715,1.25));
#50646=CARTESIAN_POINT('Origin',(1.44337567297406,57.415,0.));
#50647=CARTESIAN_POINT('',(-1.44337567297406,57.415,1.38777878078145E-16));
#50648=CARTESIAN_POINT('',(-1.44337567297406,57.415,1.76762539787484E-16));
#50649=CARTESIAN_POINT('Origin',(0.,57.415,0.));
#50650=CARTESIAN_POINT('Origin',(1.44337567297406,57.415,0.));
#50651=CARTESIAN_POINT('Origin',(0.,57.415,0.));
#50652=CARTESIAN_POINT('Origin',(1.44337567297406,57.415,0.));
#50653=CARTESIAN_POINT('Origin',(0.,57.415,0.));
#50654=CARTESIAN_POINT('Origin',(1.44337567297406,57.415,0.));
#50655=CARTESIAN_POINT('Origin',(0.,57.415,0.));
#50656=CARTESIAN_POINT('Origin',(1.44337567297406,57.415,0.));
#50657=CARTESIAN_POINT('',(-0.721687836487032,57.415,1.25));
#50658=CARTESIAN_POINT('',(0.721687836487032,57.415,1.25));
#50659=CARTESIAN_POINT('Origin',(0.,57.415,0.));
#50660=CARTESIAN_POINT('Origin',(1.44337567297406,57.415,0.));
#50661=CARTESIAN_POINT('',(-0.721687836487032,57.415,1.25));
#50662=CARTESIAN_POINT('Origin',(0.,57.415,0.));
#50663=CARTESIAN_POINT('Origin',(0.,57.415,0.));
#50664=CARTESIAN_POINT('',(0.,56.5477323996475,0.));
#50665=CARTESIAN_POINT('',(-1.44337567297406,57.415,1.76762539787484E-16));
#50666=CARTESIAN_POINT('Origin',(-1.44337567297406,58.715,1.76762539787484E-16));
#50667=CARTESIAN_POINT('',(-1.44337567297406,58.715,1.76762539787484E-16));
#50668=CARTESIAN_POINT('Origin',(-0.721687836487032,58.715,1.25));
#50669=CARTESIAN_POINT('',(-0.721687836487032,58.715,1.25));
#50670=CARTESIAN_POINT('Origin',(0.721687836487032,58.715,1.25));
#83193=UNCERTAINTY_MEASURE_WITH_UNIT(LENGTH_MEASURE(0.01),#83220,
'DISTANCE_ACCURACY_VALUE',
'Maximum model space distance between geometric entities at asserted c
onnectivities');
#83203=UNCERTAINTY_MEASURE_WITH_UNIT(LENGTH_MEASURE(0.01),#83220,
'DISTANCE_ACCURACY_VALUE',
'Maximum model space distance between geometric entities at asserted c
onnectivities');
#83209=(
GEOMETRIC_REPRESENTATION_CONTEXT(3)
GLOBAL_UNCERTAINTY_ASSIGNED_CONTEXT((#83193))
GLOBAL_UNIT_ASSIGNED_CONTEXT((#83220,#83222,#83223))
REPRESENTATION_CONTEXT('','3D')
);
#83219=(
GEOMETRIC_REPRESENTATION_CONTEXT(3)
GLOBAL_UNCERTAINTY_ASSIGNED_CONTEXT((#83203))
GLOBAL_UNIT_ASSIGNED_CONTEXT((#83220,#83222,#83223))
REPRESENTATION_CONTEXT('','3D')
);
#83220=(
LENGTH_UNIT()
NAMED_UNIT(*)
SI_UNIT(.MILLI.,.METRE.)
);
#83222=(
NAMED_UNIT(*)
PLANE_ANGLE_UNIT()
SI_UNIT($,.RADIAN.)
);
#83223=(
NAMED_UNIT(*)
SI_UNIT($,.STERADIAN.)
SOLID_ANGLE_UNIT()
);
#83229=SHAPE_DEFINITION_REPRESENTATION(#83244,#83304);
#83244=PRODUCT_DEFINITION_SHAPE('',$,#83320);
#83304=SHAPE_REPRESENTATION('',(#27595),#83209);
#83314=PRODUCT_DEFINITION_CONTEXT('part definition',#83361,'design');
#83320=PRODUCT_DEFINITION('ISO 4762 - M3 x 6 - Servo Gear Screw',
'ISO 4762 - M3 x 6 - Servo Gear Screw',#83335,#83314);
#83335=PRODUCT_DEFINITION_FORMATION('',$,#83368);
#83361=APPLICATION_CONTEXT(
'Core Data for Automotive Mechanical Design Process');
#83362=PRODUCT_CONTEXT('part definition',#83361,'mechanical');
#83368=PRODUCT('ISO 4762 - M3 x 6 - Servo Gear Screw',
'ISO 4762 - M3 x 6 - Servo Gear Screw',$,(#83362));
#83383=PRESENTATION_STYLE_ASSIGNMENT((#83398));
#83398=SURFACE_STYLE_USAGE(.BOTH.,#83413);
#83413=SURFACE_SIDE_STYLE('',(#83428));
#83428=SURFACE_STYLE_FILL_AREA(#83443);
#83443=FILL_AREA_STYLE('Opaque(196,201,207)',(#83458));
#83458=FILL_AREA_STYLE_COLOUR('Opaque(196,201,207)',#83473);
#83473=COLOUR_RGB('Opaque(196,201,207)', 0.08235294, 0.09019608, 0.10196078);
ENDSEC;
END-ISO-10303-21;
